ISO-10303-21;
HEADER;
/* Generated by software containing ST-Developer
 * from STEP Tools, Inc. (www.steptools.com) 
 */

FILE_DESCRIPTION(
/* description */ (''),
/* implementation_level */ '2;1');

FILE_NAME(
/* name */ '14_Cover_Bolt_ISO_4017_M10x30.step',
/* time_stamp */ '2026-10-26T04:15:57-07:00',
/* author */ (''),
/* organization */ (''),
/* preprocessor_version */ 'ST-DEVELOPER v20.2',
/* originating_system */ 'Autodesk Translation Framework v15.15.0.0',
/* authorisation */ '');

FILE_SCHEMA (('AUTOMOTIVE_DESIGN { 1 0 10303 214 3 1 1 }'));
ENDSEC;

DATA;
#10=MECHANICAL_DESIGN_GEOMETRIC_PRESENTATION_REPRESENTATION('',(#468),#55737);
#189=(
BOUNDED_CURVE()
B_SPLINE_CURVE(2,(#49665,#49666,#49667),.UNSPECIFIED.,.F.,.F.)
B_SPLINE_CURVE_WITH_KNOTS((3,3),(0.15318694727023,1.15036825851539),
 .UNSPECIFIED.)
CURVE()
GEOMETRIC_REPRESENTATION_ITEM()
RATIONAL_B_SPLINE_CURVE((1.05801270189225,1.221687836487,1.05801270189225))
REPRESENTATION_ITEM('')
);
#190=(
BOUNDED_CURVE()
B_SPLINE_CURVE(2,(#49669,#49670,#49671),.UNSPECIFIED.,.F.,.F.)
B_SPLINE_CURVE_WITH_KNOTS((3,3),(0.15318694727023,1.15036825851539),
 .UNSPECIFIED.)
CURVE()
GEOMETRIC_REPRESENTATION_ITEM()
RATIONAL_B_SPLINE_CURVE((1.05801270189225,1.221687836487,1.05801270189225))
REPRESENTATION_ITEM('')
);
#191=(
BOUNDED_CURVE()
B_SPLINE_CURVE(2,(#49673,#49674,#49675),.UNSPECIFIED.,.F.,.F.)
B_SPLINE_CURVE_WITH_KNOTS((3,3),(0.15318694727023,1.15036825851539),
 .UNSPECIFIED.)
CURVE()
GEOMETRIC_REPRESENTATION_ITEM()
RATIONAL_B_SPLINE_CURVE((1.05801270189225,1.221687836487,1.05801270189225))
REPRESENTATION_ITEM('')
);
#192=(
BOUNDED_CURVE()
B_SPLINE_CURVE(2,(#49677,#49678,#49679),.UNSPECIFIED.,.F.,.F.)
B_SPLINE_CURVE_WITH_KNOTS((3,3),(0.15318694727023,1.15036825851539),
 .UNSPECIFIED.)
CURVE()
GEOMETRIC_REPRESENTATION_ITEM()
RATIONAL_B_SPLINE_CURVE((1.05801270189225,1.221687836487,1.05801270189225))
REPRESENTATION_ITEM('')
);
#193=(
BOUNDED_CURVE()
B_SPLINE_CURVE(2,(#49681,#49682,#49683),.UNSPECIFIED.,.F.,.F.)
B_SPLINE_CURVE_WITH_KNOTS((3,3),(0.651777602892793,1.15036825851539),
 .UNSPECIFIED.)
CURVE()
GEOMETRIC_REPRESENTATION_ITEM()
RATIONAL_B_SPLINE_CURVE((1.13985026918963,1.13985026918963,1.05801270189225))
REPRESENTATION_ITEM('')
);
#194=(
BOUNDED_CURVE()
B_SPLINE_CURVE(2,(#49688,#49689,#49690),.UNSPECIFIED.,.F.,.F.)
B_SPLINE_CURVE_WITH_KNOTS((3,3),(0.15318694727023,0.651777602892793),
 .UNSPECIFIED.)
CURVE()
GEOMETRIC_REPRESENTATION_ITEM()
RATIONAL_B_SPLINE_CURVE((1.05801270189225,1.13985026918962,1.13985026918963))
REPRESENTATION_ITEM('')
);
#195=(
BOUNDED_CURVE()
B_SPLINE_CURVE(2,(#49691,#49692,#49693),.UNSPECIFIED.,.F.,.F.)
B_SPLINE_CURVE_WITH_KNOTS((3,3),(0.15318694727023,1.15036825851539),
 .UNSPECIFIED.)
CURVE()
GEOMETRIC_REPRESENTATION_ITEM()
RATIONAL_B_SPLINE_CURVE((1.05801270189225,1.221687836487,1.05801270189225))
REPRESENTATION_ITEM('')
);
#406=CONICAL_SURFACE('',#29545,8.83380215351701,1.04669145110647);
#407=CONICAL_SURFACE('',#29558,4.75,0.78539816339745);
#428=SHAPE_REPRESENTATION_RELATIONSHIP('SRR','None',#55837,#448);
#448=ADVANCED_BREP_SHAPE_REPRESENTATION('',(#488),#55733);
#468=STYLED_ITEM('',(#55998),#488);
#488=MANIFOLD_SOLID_BREP('Body1',#27237);
#578=B_SPLINE_SURFACE_WITH_KNOTS('',3,3,((#48148,#48149,#48150,#48151,#48152,
#48153,#48154,#48155,#48156,#48157,#48158,#48159,#48160,#48161,#48162,#48163,
#48164,#48165,#48166,#48167,#48168,#48169,#48170,#48171,#48172,#48173,#48174,
#48175,#48176,#48177,#48178,#48179,#48180,#48181,#48182,#48183,#48184,#48185,
#48186,#48187,#48188,#48189,#48190,#48191,#48192,#48193,#48194,#48195,#48196,
#48197,#48198,#48199,#48200,#48201,#48202,#48203,#48204,#48205,#48206,#48207,
#48208,#48209,#48210,#48211,#48212,#48213,#48214,#48215,#48216,#48217,#48218,
#48219,#48220,#48221,#48222,#48223,#48224,#48225,#48226,#48227,#48228,#48229,
#48230,#48231,#48232,#48233,#48234,#48235,#48236,#48237,#48238,#48239,#48240,
#48241,#48242,#48243,#48244,#48245,#48246,#48247,#48248,#48249,#48250,#48251,
#48252,#48253,#48254,#48255,#48256,#48257,#48258,#48259,#48260,#48261,#48262,
#48263,#48264,#48265,#48266,#48267,#48268,#48269,#48270,#48271,#48272,#48273,
#48274,#48275,#48276,#48277,#48278),(#48279,#48280,#48281,#48282,#48283,
#48284,#48285,#48286,#48287,#48288,#48289,#48290,#48291,#48292,#48293,#48294,
#48295,#48296,#48297,#48298,#48299,#48300,#48301,#48302,#48303,#48304,#48305,
#48306,#48307,#48308,#48309,#48310,#48311,#48312,#48313,#48314,#48315,#48316,
#48317,#48318,#48319,#48320,#48321,#48322,#48323,#48324,#48325,#48326,#48327,
#48328,#48329,#48330,#48331,#48332,#48333,#48334,#48335,#48336,#48337,#48338,
#48339,#48340,#48341,#48342,#48343,#48344,#48345,#48346,#48347,#48348,#48349,
#48350,#48351,#48352,#48353,#48354,#48355,#48356,#48357,#48358,#48359,#48360,
#48361,#48362,#48363,#48364,#48365,#48366,#48367,#48368,#48369,#48370,#48371,
#48372,#48373,#48374,#48375,#48376,#48377,#48378,#48379,#48380,#48381,#48382,
#48383,#48384,#48385,#48386,#48387,#48388,#48389,#48390,#48391,#48392,#48393,
#48394,#48395,#48396,#48397,#48398,#48399,#48400,#48401,#48402,#48403,#48404,
#48405,#48406,#48407,#48408,#48409),(#48410,#48411,#48412,#48413,#48414,
#48415,#48416,#48417,#48418,#48419,#48420,#48421,#48422,#48423,#48424,#48425,
#48426,#48427,#48428,#48429,#48430,#48431,#48432,#48433,#48434,#48435,#48436,
#48437,#48438,#48439,#48440,#48441,#48442,#48443,#48444,#48445,#48446,#48447,
#48448,#48449,#48450,#48451,#48452,#48453,#48454,#48455,#48456,#48457,#48458,
#48459,#48460,#48461,#48462,#48463,#48464,#48465,#48466,#48467,#48468,#48469,
#48470,#48471,#48472,#48473,#48474,#48475,#48476,#48477,#48478,#48479,#48480,
#48481,#48482,#48483,#48484,#48485,#48486,#48487,#48488,#48489,#48490,#48491,
#48492,#48493,#48494,#48495,#48496,#48497,#48498,#48499,#48500,#48501,#48502,
#48503,#48504,#48505,#48506,#48507,#48508,#48509,#48510,#48511,#48512,#48513,
#48514,#48515,#48516,#48517,#48518,#48519,#48520,#48521,#48522,#48523,#48524,
#48525,#48526,#48527,#48528,#48529,#48530,#48531,#48532,#48533,#48534,#48535,
#48536,#48537,#48538,#48539,#48540),(#48541,#48542,#48543,#48544,#48545,
#48546,#48547,#48548,#48549,#48550,#48551,#48552,#48553,#48554,#48555,#48556,
#48557,#48558,#48559,#48560,#48561,#48562,#48563,#48564,#48565,#48566,#48567,
#48568,#48569,#48570,#48571,#48572,#48573,#48574,#48575,#48576,#48577,#48578,
#48579,#48580,#48581,#48582,#48583,#48584,#48585,#48586,#48587,#48588,#48589,
#48590,#48591,#48592,#48593,#48594,#48595,#48596,#48597,#48598,#48599,#48600,
#48601,#48602,#48603,#48604,#48605,#48606,#48607,#48608,#48609,#48610,#48611,
#48612,#48613,#48614,#48615,#48616,#48617,#48618,#48619,#48620,#48621,#48622,
#48623,#48624,#48625,#48626,#48627,#48628,#48629,#48630,#48631,#48632,#48633,
#48634,#48635,#48636,#48637,#48638,#48639,#48640,#48641,#48642,#48643,#48644,
#48645,#48646,#48647,#48648,#48649,#48650,#48651,#48652,#48653,#48654,#48655,
#48656,#48657,#48658,#48659,#48660,#48661,#48662,#48663,#48664,#48665,#48666,
#48667,#48668,#48669,#48670,#48671)),.UNSPECIFIED.,.F.,.F.,.F.,(4,4),(4,
1,1,1,1,1,1,1,1,1,1,1,1,1,1,1,1,1,1,1,1,1,1,1,1,1,1,1,1,1,1,1,1,1,1,1,1,
1,1,1,1,1,1,1,1,1,1,1,1,1,1,1,1,1,1,1,1,1,1,1,1,1,1,1,1,1,1,1,1,1,1,1,1,
1,1,1,1,1,1,1,1,1,1,1,1,1,1,1,1,1,1,1,1,1,1,1,1,1,1,1,1,1,1,1,1,1,1,1,1,
1,1,1,1,1,1,1,1,1,1,1,1,1,1,1,1,1,1,1,4),(0.,0.0986691610045069),(8.3098959515533,
8.80969750862556,9.30949906569782,10.3091021798423,11.3087052939868,12.3083084081313,
13.3079115222759,14.3075146364204,15.3071177505649,16.3067208647094,17.3063239788539,
18.3059270929984,19.3055302071429,20.3051333212874,21.3047364354319,22.3043395495765,
23.303942663721,24.3035457778655,25.30314889201,26.3027520061545,27.302355120299,
28.3019582344435,29.301561348588,30.3011644627325,31.3007675768771,32.3003706910216,
33.2999738051661,34.2995769193106,35.2991800334551,36.2987831475996,37.2983862617441,
38.2979893758886,39.2975924900331,40.2971956041777,41.2967987183222,42.2964018324667,
43.2960049466112,44.2956080607557,45.2952111749002,46.2948142890447,47.2944174031892,
48.2940205173337,49.2936236314783,50.2932267456228,51.2928298597673,52.2924329739118,
53.2920360880563,54.2916392022008,55.2912423163453,56.2908454304898,57.2904485446343,
58.2900516587789,59.2896547729234,60.2892578870679,61.2888610012124,62.2884641153569,
63.2880672295014,64.2876703436459,65.2872734577904,66.2868765719349,67.2864796860794,
68.286082800224,69.2856859143685,70.285289028513,71.2848921426575,72.284495256802,
73.2840983709465,74.283701485091,75.2833045992355,76.28290771338,77.2825108275245,
78.2821139416691,79.2817170558136,80.2813201699581,81.2809232841026,82.2805263982471,
83.2801295123916,84.2797326265361,85.2793357406806,86.2789388548251,87.2785419689697,
88.2781450831142,89.2777481972587,90.2773513114032,91.2769544255477,92.2765575396922,
93.2761606538367,94.2757637679812,95.2753668821258,96.2749699962703,97.2745731104148,
98.2741762245593,99.2737793387038,100.273382452848,101.272985566993,102.272588681137,
103.272191795282,104.271794909426,105.271398023571,106.271001137715,107.27060425186,
108.270207366004,109.269810480149,110.269413594293,111.269016708438,112.268619822582,
113.268222936727,114.267826050871,115.267429165016,116.26703227916,117.266635393305,
118.26623850745,119.265841621594,120.265444735739,121.265047849883,122.264650964028,
123.264254078172,124.263857192317,125.263460306461,126.263063420606,127.26266653475,
128.262269648895,129.261872763039,130.261475877184,131.261078991328,132.260682105473,
133.260285219617,133.760086776689,134.259888333762),.UNSPECIFIED.);
#579=B_SPLINE_SURFACE_WITH_KNOTS('',3,3,((#49021,#49022,#49023,#49024,#49025,
#49026,#49027,#49028,#49029,#49030,#49031,#49032,#49033,#49034,#49035,#49036,
#49037,#49038,#49039,#49040,#49041,#49042,#49043,#49044,#49045,#49046,#49047,
#49048,#49049,#49050,#49051,#49052,#49053,#49054,#49055,#49056,#49057,#49058,
#49059,#49060,#49061,#49062,#49063,#49064,#49065,#49066,#49067,#49068,#49069,
#49070,#49071,#49072,#49073,#49074,#49075,#49076,#49077,#49078,#49079,#49080,
#49081,#49082,#49083,#49084,#49085,#49086,#49087,#49088,#49089,#49090,#49091,
#49092,#49093,#49094,#49095,#49096,#49097,#49098,#49099,#49100,#49101,#49102,
#49103,#49104,#49105,#49106,#49107,#49108,#49109,#49110,#49111,#49112,#49113,
#49114,#49115,#49116,#49117,#49118,#49119,#49120,#49121,#49122,#49123,#49124,
#49125,#49126,#49127,#49128,#49129,#49130,#49131,#49132,#49133,#49134,#49135,
#49136,#49137,#49138,#49139,#49140,#49141,#49142,#49143,#49144,#49145,#49146,
#49147,#49148,#49149,#49150,#49151),(#49152,#49153,#49154,#49155,#49156,
#49157,#49158,#49159,#49160,#49161,#49162,#49163,#49164,#49165,#49166,#49167,
#49168,#49169,#49170,#49171,#49172,#49173,#49174,#49175,#49176,#49177,#49178,
#49179,#49180,#49181,#49182,#49183,#49184,#49185,#49186,#49187,#49188,#49189,
#49190,#49191,#49192,#49193,#49194,#49195,#49196,#49197,#49198,#49199,#49200,
#49201,#49202,#49203,#49204,#49205,#49206,#49207,#49208,#49209,#49210,#49211,
#49212,#49213,#49214,#49215,#49216,#49217,#49218,#49219,#49220,#49221,#49222,
#49223,#49224,#49225,#49226,#49227,#49228,#49229,#49230,#49231,#49232,#49233,
#49234,#49235,#49236,#49237,#49238,#49239,#49240,#49241,#49242,#49243,#49244,
#49245,#49246,#49247,#49248,#49249,#49250,#49251,#49252,#49253,#49254,#49255,
#49256,#49257,#49258,#49259,#49260,#49261,#49262,#49263,#49264,#49265,#49266,
#49267,#49268,#49269,#49270,#49271,#49272,#49273,#49274,#49275,#49276,#49277,
#49278,#49279,#49280,#49281,#49282),(#49283,#49284,#49285,#49286,#49287,
#49288,#49289,#49290,#49291,#49292,#49293,#49294,#49295,#49296,#49297,#49298,
#49299,#49300,#49301,#49302,#49303,#49304,#49305,#49306,#49307,#49308,#49309,
#49310,#49311,#49312,#49313,#49314,#49315,#49316,#49317,#49318,#49319,#49320,
#49321,#49322,#49323,#49324,#49325,#49326,#49327,#49328,#49329,#49330,#49331,
#49332,#49333,#49334,#49335,#49336,#49337,#49338,#49339,#49340,#49341,#49342,
#49343,#49344,#49345,#49346,#49347,#49348,#49349,#49350,#49351,#49352,#49353,
#49354,#49355,#49356,#49357,#49358,#49359,#49360,#49361,#49362,#49363,#49364,
#49365,#49366,#49367,#49368,#49369,#49370,#49371,#49372,#49373,#49374,#49375,
#49376,#49377,#49378,#49379,#49380,#49381,#49382,#49383,#49384,#49385,#49386,
#49387,#49388,#49389,#49390,#49391,#49392,#49393,#49394,#49395,#49396,#49397,
#49398,#49399,#49400,#49401,#49402,#49403,#49404,#49405,#49406,#49407,#49408,
#49409,#49410,#49411,#49412,#49413),(#49414,#49415,#49416,#49417,#49418,
#49419,#49420,#49421,#49422,#49423,#49424,#49425,#49426,#49427,#49428,#49429,
#49430,#49431,#49432,#49433,#49434,#49435,#49436,#49437,#49438,#49439,#49440,
#49441,#49442,#49443,#49444,#49445,#49446,#49447,#49448,#49449,#49450,#49451,
#49452,#49453,#49454,#49455,#49456,#49457,#49458,#49459,#49460,#49461,#49462,
#49463,#49464,#49465,#49466,#49467,#49468,#49469,#49470,#49471,#49472,#49473,
#49474,#49475,#49476,#49477,#49478,#49479,#49480,#49481,#49482,#49483,#49484,
#49485,#49486,#49487,#49488,#49489,#49490,#49491,#49492,#49493,#49494,#49495,
#49496,#49497,#49498,#49499,#49500,#49501,#49502,#49503,#49504,#49505,#49506,
#49507,#49508,#49509,#49510,#49511,#49512,#49513,#49514,#49515,#49516,#49517,
#49518,#49519,#49520,#49521,#49522,#49523,#49524,#49525,#49526,#49527,#49528,
#49529,#49530,#49531,#49532,#49533,#49534,#49535,#49536,#49537,#49538,#49539,
#49540,#49541,#49542,#49543,#49544)),.UNSPECIFIED.,.F.,.F.,.F.,(4,4),(4,
1,1,1,1,1,1,1,1,1,1,1,1,1,1,1,1,1,1,1,1,1,1,1,1,1,1,1,1,1,1,1,1,1,1,1,1,
1,1,1,1,1,1,1,1,1,1,1,1,1,1,1,1,1,1,1,1,1,1,1,1,1,1,1,1,1,1,1,1,1,1,1,1,
1,1,1,1,1,1,1,1,1,1,1,1,1,1,1,1,1,1,1,1,1,1,1,1,1,1,1,1,1,1,1,1,1,1,1,1,
1,1,1,1,1,1,1,1,1,1,1,1,1,1,1,1,1,1,1,4),(0.,0.0986691610045069),(11.6147305479242,
12.1145321049964,12.6143336620687,13.6139367762132,14.6135398903577,15.6131430045022,
16.6127461186467,17.6123492327912,18.6119523469357,19.6115554610803,20.6111585752248,
21.6107616893693,22.6103648035138,23.6099679176583,24.6095710318028,25.6091741459473,
26.6087772600918,27.6083803742363,28.6079834883808,29.6075866025254,30.6071897166699,
31.6067928308144,32.6063959449589,33.6059990591034,34.6056021732479,35.6052052873924,
36.6048084015369,37.6044115156814,38.604014629826,39.6036177439705,40.603220858115,
41.6028239722595,42.602427086404,43.6020302005485,44.601633314693,45.6012364288375,
46.600839542982,47.6004426571266,48.6000457712711,49.5996488854156,50.5992519995601,
51.5988551137046,52.5984582278491,53.5980613419936,54.5976644561381,55.5972675702826,
56.5968706844272,57.5964737985717,58.5960769127162,59.5956800268607,60.5952831410052,
61.5948862551497,62.5944893692942,63.5940924834387,64.5936955975832,65.5932987117278,
66.5929018258723,67.5925049400168,68.5921080541613,69.5917111683058,70.5913142824503,
71.5909173965948,72.5905205107393,73.5901236248838,74.5897267390284,75.5893298531729,
76.5889329673174,77.5885360814619,78.5881391956064,79.5877423097509,80.5873454238954,
81.5869485380399,82.5865516521845,83.586154766329,84.5857578804735,85.585360994618,
86.5849641087625,87.584567222907,88.5841703370515,89.583773451196,90.5833765653405,
91.582979679485,92.5825827936296,93.5821859077741,94.5817890219186,95.5813921360631,
96.5809952502076,97.5805983643521,98.5802014784966,99.5798045926411,100.579407706786,
101.57901082093,102.578613935075,103.578217049219,104.577820163364,105.577423277508,
106.577026391653,107.576629505797,108.576232619942,109.575835734086,110.575438848231,
111.575041962375,112.57464507652,113.574248190664,114.573851304809,115.573454418953,
116.573057533098,117.572660647242,118.572263761387,119.571866875531,120.571469989676,
121.57107310382,122.570676217965,123.570279332109,124.569882446254,125.569485560398,
126.569088674543,127.568691788687,128.568294902832,129.567898016976,130.567501131121,
131.567104245265,132.56670735941,133.566310473554,134.565913587699,135.565516701844,
136.565119815988,137.06492137306,137.564722930133),.UNSPECIFIED.);
#716=FACE_BOUND('',#9786,.T.);
#1543=PLANE('',#29540);
#1544=PLANE('',#29547);
#1545=PLANE('',#29548);
#1546=PLANE('',#29549);
#1547=PLANE('',#29550);
#1548=PLANE('',#29552);
#1549=PLANE('',#29553);
#1550=PLANE('',#29554);
#1551=PLANE('',#29555);
#1552=PLANE('',#29556);
#3637=LINE('',#46704,#6008);
#3638=LINE('',#46731,#6009);
#3639=LINE('',#46779,#6010);
#3640=LINE('',#46827,#6011);
#3641=LINE('',#46875,#6012);
#3642=LINE('',#46929,#6013);
#3643=LINE('',#46977,#6014);
#3644=LINE('',#47025,#6015);
#3645=LINE('',#47079,#6016);
#3646=LINE('',#47127,#6017);
#3647=LINE('',#47175,#6018);
#3648=LINE('',#47223,#6019);
#3649=LINE('',#47277,#6020);
#3650=LINE('',#47325,#6021);
#3651=LINE('',#47373,#6022);
#3652=LINE('',#47427,#6023);
#3653=LINE('',#47475,#6024);
#3654=LINE('',#47523,#6025);
#3655=LINE('',#47571,#6026);
#3656=LINE('',#47625,#6027);
#3657=LINE('',#47673,#6028);
#3658=LINE('',#47683,#6029);
#3659=LINE('',#47709,#6030);
#3660=LINE('',#47734,#6031);
#3661=LINE('',#47759,#6032);
#3662=LINE('',#47783,#6033);
#3663=LINE('',#47807,#6034);
#3664=LINE('',#47832,#6035);
#3665=LINE('',#47857,#6036);
#3666=LINE('',#47881,#6037);
#3667=LINE('',#47906,#6038);
#3668=LINE('',#47931,#6039);
#3669=LINE('',#47955,#6040);
#3670=LINE('',#47979,#6041);
#3671=LINE('',#48004,#6042);
#3672=LINE('',#48029,#6043);
#3673=LINE('',#48053,#6044);
#3674=LINE('',#48078,#6045);
#3675=LINE('',#48103,#6046);
#3676=LINE('',#48127,#6047);
#3677=LINE('',#49685,#6048);
#3678=LINE('',#49696,#6049);
#3679=LINE('',#49698,#6050);
#3680=LINE('',#49699,#6051);
#3681=LINE('',#49702,#6052);
#3682=LINE('',#49703,#6053);
#3683=LINE('',#49706,#6054);
#3684=LINE('',#49707,#6055);
#3685=LINE('',#49710,#6056);
#3686=LINE('',#49712,#6057);
#3687=LINE('',#49713,#6058);
#3688=LINE('',#49716,#6059);
#3689=LINE('',#49718,#6060);
#3690=LINE('',#49725,#6061);
#6008=VECTOR('',#35927,5.);
#6009=VECTOR('',#35932,5.);
#6010=VECTOR('',#35935,5.);
#6011=VECTOR('',#35938,5.);
#6012=VECTOR('',#35941,5.);
#6013=VECTOR('',#35944,5.);
#6014=VECTOR('',#35947,5.);
#6015=VECTOR('',#35950,5.);
#6016=VECTOR('',#35953,5.);
#6017=VECTOR('',#35956,5.);
#6018=VECTOR('',#35959,5.);
#6019=VECTOR('',#35962,5.);
#6020=VECTOR('',#35965,5.);
#6021=VECTOR('',#35968,5.);
#6022=VECTOR('',#35971,5.);
#6023=VECTOR('',#35974,5.);
#6024=VECTOR('',#35977,5.);
#6025=VECTOR('',#35980,5.);
#6026=VECTOR('',#35983,5.);
#6027=VECTOR('',#35986,5.);
#6028=VECTOR('',#35989,4.0705);
#6029=VECTOR('',#35994,4.0705);
#6030=VECTOR('',#35999,4.0705);
#6031=VECTOR('',#36002,4.0705);
#6032=VECTOR('',#36005,4.0705);
#6033=VECTOR('',#36008,4.0705);
#6034=VECTOR('',#36011,4.0705);
#6035=VECTOR('',#36014,4.0705);
#6036=VECTOR('',#36017,4.0705);
#6037=VECTOR('',#36020,4.0705);
#6038=VECTOR('',#36023,4.0705);
#6039=VECTOR('',#36026,4.0705);
#6040=VECTOR('',#36029,4.0705);
#6041=VECTOR('',#36032,4.0705);
#6042=VECTOR('',#36035,4.0705);
#6043=VECTOR('',#36038,4.0705);
#6044=VECTOR('',#36041,4.0705);
#6045=VECTOR('',#36044,4.0705);
#6046=VECTOR('',#36047,4.0705);
#6047=VECTOR('',#36050,4.0705);
#6048=VECTOR('',#36063,8.83380215351701);
#6049=VECTOR('',#36068,10.);
#6050=VECTOR('',#36069,10.);
#6051=VECTOR('',#36070,10.);
#6052=VECTOR('',#36073,10.);
#6053=VECTOR('',#36074,10.);
#6054=VECTOR('',#36077,10.);
#6055=VECTOR('',#36078,10.);
#6056=VECTOR('',#36081,10.);
#6057=VECTOR('',#36082,10.);
#6058=VECTOR('',#36083,10.);
#6059=VECTOR('',#36088,10.);
#6060=VECTOR('',#36091,10.);
#6061=VECTOR('',#36102,4.75);
#6714=CYLINDRICAL_SURFACE('',#29497,4.925);
#6715=CYLINDRICAL_SURFACE('',#29499,4.925);
#6716=CYLINDRICAL_SURFACE('',#29500,4.925);
#6717=CYLINDRICAL_SURFACE('',#29501,4.925);
#6718=CYLINDRICAL_SURFACE('',#29502,4.925);
#6719=CYLINDRICAL_SURFACE('',#29503,4.925);
#6720=CYLINDRICAL_SURFACE('',#29504,4.925);
#6721=CYLINDRICAL_SURFACE('',#29505,4.925);
#6722=CYLINDRICAL_SURFACE('',#29506,4.925);
#6723=CYLINDRICAL_SURFACE('',#29507,4.925);
#6724=CYLINDRICAL_SURFACE('',#29508,4.925);
#6725=CYLINDRICAL_SURFACE('',#29509,4.925);
#6726=CYLINDRICAL_SURFACE('',#29510,4.925);
#6727=CYLINDRICAL_SURFACE('',#29511,4.925);
#6728=CYLINDRICAL_SURFACE('',#29512,4.925);
#6729=CYLINDRICAL_SURFACE('',#29513,4.925);
#6730=CYLINDRICAL_SURFACE('',#29514,4.925);
#6731=CYLINDRICAL_SURFACE('',#29515,4.925);
#6732=CYLINDRICAL_SURFACE('',#29516,4.925);
#6733=CYLINDRICAL_SURFACE('',#29517,4.925);
#6734=CYLINDRICAL_SURFACE('',#29518,4.0705);
#6735=CYLINDRICAL_SURFACE('',#29520,4.0705);
#6736=CYLINDRICAL_SURFACE('',#29522,4.0705);
#6737=CYLINDRICAL_SURFACE('',#29523,4.0705);
#6738=CYLINDRICAL_SURFACE('',#29524,4.0705);
#6739=CYLINDRICAL_SURFACE('',#29525,4.0705);
#6740=CYLINDRICAL_SURFACE('',#29526,4.0705);
#6741=CYLINDRICAL_SURFACE('',#29527,4.0705);
#6742=CYLINDRICAL_SURFACE('',#29528,4.0705);
#6743=CYLINDRICAL_SURFACE('',#29529,4.0705);
#6744=CYLINDRICAL_SURFACE('',#29530,4.0705);
#6745=CYLINDRICAL_SURFACE('',#29531,4.0705);
#6746=CYLINDRICAL_SURFACE('',#29532,4.0705);
#6747=CYLINDRICAL_SURFACE('',#29533,4.0705);
#6748=CYLINDRICAL_SURFACE('',#29534,4.0705);
#6749=CYLINDRICAL_SURFACE('',#29535,4.0705);
#6750=CYLINDRICAL_SURFACE('',#29536,4.0705);
#6751=CYLINDRICAL_SURFACE('',#29537,4.0705);
#6752=CYLINDRICAL_SURFACE('',#29538,4.0705);
#6753=CYLINDRICAL_SURFACE('',#29539,4.0705);
#6754=CYLINDRICAL_SURFACE('',#29544,4.0705);
#6755=CYLINDRICAL_SURFACE('',#29559,4.925);
#8056=FACE_OUTER_BOUND('',#9737,.T.);
#8057=FACE_OUTER_BOUND('',#9738,.T.);
#8058=FACE_OUTER_BOUND('',#9739,.T.);
#8059=FACE_OUTER_BOUND('',#9740,.T.);
#8060=FACE_OUTER_BOUND('',#9741,.T.);
#8061=FACE_OUTER_BOUND('',#9742,.T.);
#8062=FACE_OUTER_BOUND('',#9743,.T.);
#8063=FACE_OUTER_BOUND('',#9744,.T.);
#8064=FACE_OUTER_BOUND('',#9745,.T.);
#8065=FACE_OUTER_BOUND('',#9746,.T.);
#8066=FACE_OUTER_BOUND('',#9747,.T.);
#8067=FACE_OUTER_BOUND('',#9748,.T.);
#8068=FACE_OUTER_BOUND('',#9749,.T.);
#8069=FACE_OUTER_BOUND('',#9750,.T.);
#8070=FACE_OUTER_BOUND('',#9751,.T.);
#8071=FACE_OUTER_BOUND('',#9752,.T.);
#8072=FACE_OUTER_BOUND('',#9753,.T.);
#8073=FACE_OUTER_BOUND('',#9754,.T.);
#8074=FACE_OUTER_BOUND('',#9755,.T.);
#8075=FACE_OUTER_BOUND('',#9756,.T.);
#8076=FACE_OUTER_BOUND('',#9757,.T.);
#8077=FACE_OUTER_BOUND('',#9758,.T.);
#8078=FACE_OUTER_BOUND('',#9759,.T.);
#8079=FACE_OUTER_BOUND('',#9760,.T.);
#8080=FACE_OUTER_BOUND('',#9761,.T.);
#8081=FACE_OUTER_BOUND('',#9762,.T.);
#8082=FACE_OUTER_BOUND('',#9763,.T.);
#8083=FACE_OUTER_BOUND('',#9764,.T.);
#8084=FACE_OUTER_BOUND('',#9765,.T.);
#8085=FACE_OUTER_BOUND('',#9766,.T.);
#8086=FACE_OUTER_BOUND('',#9767,.T.);
#8087=FACE_OUTER_BOUND('',#9768,.T.);
#8088=FACE_OUTER_BOUND('',#9769,.T.);
#8089=FACE_OUTER_BOUND('',#9770,.T.);
#8090=FACE_OUTER_BOUND('',#9771,.T.);
#8091=FACE_OUTER_BOUND('',#9772,.T.);
#8092=FACE_OUTER_BOUND('',#9773,.T.);
#8093=FACE_OUTER_BOUND('',#9774,.T.);
#8094=FACE_OUTER_BOUND('',#9775,.T.);
#8095=FACE_OUTER_BOUND('',#9776,.T.);
#8096=FACE_OUTER_BOUND('',#9777,.T.);
#8097=FACE_OUTER_BOUND('',#9778,.T.);
#8098=FACE_OUTER_BOUND('',#9779,.T.);
#8099=FACE_OUTER_BOUND('',#9780,.T.);
#8100=FACE_OUTER_BOUND('',#9781,.T.);
#8101=FACE_OUTER_BOUND('',#9782,.T.);
#8102=FACE_OUTER_BOUND('',#9783,.T.);
#8103=FACE_OUTER_BOUND('',#9784,.T.);
#8104=FACE_OUTER_BOUND('',#9785,.T.);
#8105=FACE_OUTER_BOUND('',#9787,.T.);
#8106=FACE_OUTER_BOUND('',#9788,.T.);
#8107=FACE_OUTER_BOUND('',#9789,.T.);
#8108=FACE_OUTER_BOUND('',#9790,.T.);
#8109=FACE_OUTER_BOUND('',#9791,.T.);
#8110=FACE_OUTER_BOUND('',#9792,.T.);
#8111=FACE_OUTER_BOUND('',#9793,.T.);
#9737=EDGE_LOOP('',(#23910,#23911,#23912,#23913));
#9738=EDGE_LOOP('',(#23914,#23915,#23916,#23917));
#9739=EDGE_LOOP('',(#23918,#23919,#23920,#23921));
#9740=EDGE_LOOP('',(#23922,#23923,#23924,#23925));
#9741=EDGE_LOOP('',(#23926,#23927,#23928,#23929));
#9742=EDGE_LOOP('',(#23930,#23931,#23932,#23933));
#9743=EDGE_LOOP('',(#23934,#23935,#23936,#23937));
#9744=EDGE_LOOP('',(#23938,#23939,#23940,#23941));
#9745=EDGE_LOOP('',(#23942,#23943,#23944,#23945));
#9746=EDGE_LOOP('',(#23946,#23947,#23948,#23949));
#9747=EDGE_LOOP('',(#23950,#23951,#23952,#23953));
#9748=EDGE_LOOP('',(#23954,#23955,#23956,#23957));
#9749=EDGE_LOOP('',(#23958,#23959,#23960,#23961));
#9750=EDGE_LOOP('',(#23962,#23963,#23964,#23965));
#9751=EDGE_LOOP('',(#23966,#23967,#23968,#23969));
#9752=EDGE_LOOP('',(#23970,#23971,#23972,#23973));
#9753=EDGE_LOOP('',(#23974,#23975,#23976,#23977));
#9754=EDGE_LOOP('',(#23978,#23979,#23980,#23981));
#9755=EDGE_LOOP('',(#23982,#23983,#23984,#23985));
#9756=EDGE_LOOP('',(#23986,#23987,#23988,#23989));
#9757=EDGE_LOOP('',(#23990,#23991,#23992));
#9758=EDGE_LOOP('',(#23993,#23994,#23995,#23996,#23997));
#9759=EDGE_LOOP('',(#23998,#23999,#24000,#24001));
#9760=EDGE_LOOP('',(#24002,#24003,#24004,#24005));
#9761=EDGE_LOOP('',(#24006,#24007,#24008,#24009));
#9762=EDGE_LOOP('',(#24010,#24011,#24012,#24013));
#9763=EDGE_LOOP('',(#24014,#24015,#24016,#24017));
#9764=EDGE_LOOP('',(#24018,#24019,#24020,#24021));
#9765=EDGE_LOOP('',(#24022,#24023,#24024,#24025));
#9766=EDGE_LOOP('',(#24026,#24027,#24028,#24029));
#9767=EDGE_LOOP('',(#24030,#24031,#24032,#24033));
#9768=EDGE_LOOP('',(#24034,#24035,#24036,#24037));
#9769=EDGE_LOOP('',(#24038,#24039,#24040,#24041));
#9770=EDGE_LOOP('',(#24042,#24043,#24044,#24045));
#9771=EDGE_LOOP('',(#24046,#24047,#24048,#24049));
#9772=EDGE_LOOP('',(#24050,#24051,#24052,#24053));
#9773=EDGE_LOOP('',(#24054,#24055,#24056,#24057));
#9774=EDGE_LOOP('',(#24058,#24059,#24060,#24061));
#9775=EDGE_LOOP('',(#24062,#24063,#24064,#24065));
#9776=EDGE_LOOP('',(#24066,#24067,#24068,#24069));
#9777=EDGE_LOOP('',(#24070,#24071,#24072,#24073,#24074,#24075,#24076,#24077,
#24078,#24079,#24080,#24081,#24082,#24083,#24084,#24085,#24086,#24087,#24088,
#24089,#24090,#24091,#24092,#24093,#24094,#24095,#24096,#24097,#24098,#24099,
#24100,#24101,#24102,#24103,#24104,#24105,#24106,#24107,#24108,#24109,#24110,
#24111,#24112));
#9778=EDGE_LOOP('',(#24113,#24114,#24115,#24116,#24117));
#9779=EDGE_LOOP('',(#24118,#24119,#24120,#24121));
#9780=EDGE_LOOP('',(#24122,#24123,#24124,#24125,#24126,#24127,#24128,#24129,
#24130,#24131,#24132,#24133,#24134,#24135,#24136,#24137,#24138,#24139,#24140,
#24141,#24142,#24143,#24144,#24145,#24146,#24147,#24148,#24149,#24150,#24151,
#24152,#24153,#24154,#24155,#24156,#24157,#24158,#24159,#24160,#24161,#24162,
#24163,#24164,#24165));
#9781=EDGE_LOOP('',(#24166,#24167,#24168,#24169,#24170,#24171,#24172,#24173,
#24174,#24175));
#9782=EDGE_LOOP('',(#24176,#24177,#24178,#24179));
#9783=EDGE_LOOP('',(#24180,#24181,#24182,#24183));
#9784=EDGE_LOOP('',(#24184,#24185,#24186,#24187));
#9785=EDGE_LOOP('',(#24188,#24189,#24190,#24191,#24192,#24193));
#9786=EDGE_LOOP('',(#24194,#24195,#24196,#24197,#24198));
#9787=EDGE_LOOP('',(#24199,#24200,#24201,#24202));
#9788=EDGE_LOOP('',(#24203,#24204,#24205,#24206));
#9789=EDGE_LOOP('',(#24207,#24208,#24209,#24210,#24211));
#9790=EDGE_LOOP('',(#24212));
#9791=EDGE_LOOP('',(#24213));
#9792=EDGE_LOOP('',(#24214,#24215,#24216,#24217,#24218,#24219));
#9793=EDGE_LOOP('',(#24220,#24221,#24222,#24223));
#10872=CIRCLE('',#29498,4.925);
#10873=CIRCLE('',#29519,4.0705);
#10874=CIRCLE('',#29521,4.0705);
#10875=CIRCLE('',#29541,4.925);
#10876=CIRCLE('',#29542,4.925);
#10877=CIRCLE('',#29543,4.0705);
#10878=CIRCLE('',#29546,7.60300281800529);
#10879=CIRCLE('',#29551,4.925);
#10880=CIRCLE('',#29557,4.5);
#11225=B_SPLINE_CURVE_WITH_KNOTS('',3,(#46706,#46707,#46708,#46709,#46710,
#46711,#46712,#46713,#46714,#46715),.UNSPECIFIED.,.F.,.F.,(4,3,3,4),(-4.0932327200247,
-3.99841245657804,-2.99880934243353,-2.06652207565086),.UNSPECIFIED.);
#11226=B_SPLINE_CURVE_WITH_KNOTS('',3,(#46718,#46719,#46720,#46721,#46722,
#46723,#46724,#46725,#46726,#46727),.UNSPECIFIED.,.F.,.F.,(4,3,3,4),(0.,
0.499801557072245,0.999603114144509,1.11488200921585),.UNSPECIFIED.);
#11227=B_SPLINE_CURVE_WITH_KNOTS('',3,(#46732,#46733,#46734,#46735,#46736,
#46737,#46738,#46739,#46740,#46741,#46742,#46743,#46744,#46745,#46746,#46747,
#46748,#46749,#46750,#46751,#46752,#46753),.UNSPECIFIED.,.F.,.F.,(4,3,3,
3,3,3,3,4),(-10.3764180272043,-9.99603114144511,-8.9964280273006,-7.99682491315609,
-6.99722179901157,-5.99761868486707,-4.99801557072256,-4.0932327200247),
 .UNSPECIFIED.);
#11228=B_SPLINE_CURVE_WITH_KNOTS('',3,(#46754,#46755,#46756,#46757,#46758,
#46759,#46760,#46761,#46762,#46763,#46764,#46765,#46766,#46767,#46768,#46769,
#46770,#46771,#46772,#46773,#46774,#46775),.UNSPECIFIED.,.F.,.F.,(4,3,3,
3,3,3,3,4),(1.11488200921585,1.99920622828902,2.99880934243353,3.99841245657804,
4.99801557072255,5.99761868486706,6.99722179901157,7.39806731639545),
 .UNSPECIFIED.);
#11229=B_SPLINE_CURVE_WITH_KNOTS('',3,(#46780,#46781,#46782,#46783,#46784,
#46785,#46786,#46787,#46788,#46789,#46790,#46791,#46792,#46793,#46794,#46795,
#46796,#46797,#46798,#46799,#46800,#46801),.UNSPECIFIED.,.F.,.F.,(4,3,3,
3,3,3,3,4),(-16.6596033343839,-15.9936498263122,-14.9940467121677,-13.9944435980232,
-12.9948404838786,-11.9952373697341,-10.9956342555896,-10.3764180272043),
 .UNSPECIFIED.);
#11230=B_SPLINE_CURVE_WITH_KNOTS('',3,(#46802,#46803,#46804,#46805,#46806,
#46807,#46808,#46809,#46810,#46811,#46812,#46813,#46814,#46815,#46816,#46817,
#46818,#46819,#46820,#46821,#46822,#46823),.UNSPECIFIED.,.F.,.F.,(4,3,3,
3,3,3,3,4),(7.39806731639545,7.99682491315608,8.9964280273006,9.99603114144511,
10.9956342555896,11.9952373697341,12.9948404838786,13.681252623575),
 .UNSPECIFIED.);
#11231=B_SPLINE_CURVE_WITH_KNOTS('',3,(#46828,#46829,#46830,#46831,#46832,
#46833,#46834,#46835,#46836,#46837,#46838,#46839,#46840,#46841,#46842,#46843,
#46844,#46845,#46846,#46847,#46848,#46849),.UNSPECIFIED.,.F.,.F.,(4,3,3,
3,3,3,3,4),(-22.9427886415635,-21.9912685111792,-20.9916653970347,-19.9920622828902,
-18.9924591687457,-17.9928560546012,-16.9932529404567,-16.6596033343839),
 .UNSPECIFIED.);
#11232=B_SPLINE_CURVE_WITH_KNOTS('',3,(#46850,#46851,#46852,#46853,#46854,
#46855,#46856,#46857,#46858,#46859,#46860,#46861,#46862,#46863,#46864,#46865,
#46866,#46867,#46868,#46869,#46870,#46871),.UNSPECIFIED.,.F.,.F.,(4,3,3,
3,3,3,3,4),(13.681252623575,13.9944435980232,14.9940467121677,15.9936498263122,
16.9932529404567,17.9928560546012,18.9924591687457,19.9644379307546),
 .UNSPECIFIED.);
#11233=B_SPLINE_CURVE_WITH_KNOTS('',3,(#46876,#46877,#46878,#46879,#46880,
#46881,#46882,#46883,#46884,#46885,#46886,#46887,#46888,#46889,#46890,#46891,
#46892,#46893,#46894,#46895,#46896,#46897,#46898,#46899,#46900),
 .UNSPECIFIED.,.F.,.F.,(4,3,3,3,3,3,3,3,4),(-29.225973948743,-28.9884903101908,
-27.9888871960463,-26.9892840819018,-25.9896809677573,-24.9900778536128,
-23.9904747394683,-22.9908716253238,-22.9427886415635),.UNSPECIFIED.);
#11234=B_SPLINE_CURVE_WITH_KNOTS('',3,(#46901,#46902,#46903,#46904,#46905,
#46906,#46907,#46908,#46909,#46910,#46911,#46912,#46913,#46914,#46915,#46916,
#46917,#46918,#46919,#46920,#46921,#46922,#46923,#46924,#46925),
 .UNSPECIFIED.,.F.,.F.,(4,3,3,3,3,3,3,3,4),(19.9644379307546,19.9920622828902,
20.9916653970347,21.9912685111792,22.9908716253238,23.9904747394683,24.9900778536128,
25.9896809677573,26.2476232379342),.UNSPECIFIED.);
#11235=B_SPLINE_CURVE_WITH_KNOTS('',3,(#46930,#46931,#46932,#46933,#46934,
#46935,#46936,#46937,#46938,#46939,#46940,#46941,#46942,#46943,#46944,#46945,
#46946,#46947,#46948,#46949,#46950,#46951),.UNSPECIFIED.,.F.,.F.,(4,3,3,
3,3,3,3,4),(-35.5091592559226,-34.9861089950579,-33.9865058809134,-32.9869027667689,
-31.9872996526244,-30.9876965384798,-29.9880934243353,-29.225973948743),
 .UNSPECIFIED.);
#11236=B_SPLINE_CURVE_WITH_KNOTS('',3,(#46952,#46953,#46954,#46955,#46956,
#46957,#46958,#46959,#46960,#46961,#46962,#46963,#46964,#46965,#46966,#46967,
#46968,#46969,#46970,#46971,#46972,#46973),.UNSPECIFIED.,.F.,.F.,(4,3,3,
3,3,3,3,4),(26.2476232379342,26.9892840819018,27.9888871960463,28.9884903101908,
29.9880934243353,30.9876965384798,31.9872996526244,32.5308085451138),
 .UNSPECIFIED.);
#11237=B_SPLINE_CURVE_WITH_KNOTS('',3,(#46978,#46979,#46980,#46981,#46982,
#46983,#46984,#46985,#46986,#46987,#46988,#46989,#46990,#46991,#46992,#46993,
#46994,#46995,#46996,#46997,#46998,#46999),.UNSPECIFIED.,.F.,.F.,(4,3,3,
3,3,3,3,4),(-41.7923445631022,-40.9837276799249,-39.9841245657804,-38.9845214516359,
-37.9849183374914,-36.9853152233469,-35.9857121092024,-35.5091592559226),
 .UNSPECIFIED.);
#11238=B_SPLINE_CURVE_WITH_KNOTS('',3,(#47000,#47001,#47002,#47003,#47004,
#47005,#47006,#47007,#47008,#47009,#47010,#47011,#47012,#47013,#47014,#47015,
#47016,#47017,#47018,#47019,#47020,#47021),.UNSPECIFIED.,.F.,.F.,(4,3,3,
3,3,3,3,4),(32.5308085451138,32.9869027667689,33.9865058809134,34.9861089950579,
35.9857121092024,36.9853152233469,37.9849183374914,38.8139938522934),
 .UNSPECIFIED.);
#11239=B_SPLINE_CURVE_WITH_KNOTS('',3,(#47026,#47027,#47028,#47029,#47030,
#47031,#47032,#47033,#47034,#47035,#47036,#47037,#47038,#47039,#47040,#47041,
#47042,#47043,#47044,#47045,#47046,#47047,#47048,#47049,#47050),
 .UNSPECIFIED.,.F.,.F.,(4,3,3,3,3,3,3,3,4),(-48.0755298702818,-47.9809494789365,
-46.981346364792,-45.9817432506475,-44.982140136503,-43.9825370223585,-42.982933908214,
-41.9833307940695,-41.7923445631022),.UNSPECIFIED.);
#11240=B_SPLINE_CURVE_WITH_KNOTS('',3,(#47051,#47052,#47053,#47054,#47055,
#47056,#47057,#47058,#47059,#47060,#47061,#47062,#47063,#47064,#47065,#47066,
#47067,#47068,#47069,#47070,#47071,#47072,#47073,#47074,#47075),
 .UNSPECIFIED.,.F.,.F.,(4,3,3,3,3,3,3,3,4),(38.8139938522934,38.9845214516359,
39.9841245657804,40.983727679925,41.9833307940695,42.982933908214,43.9825370223585,
44.982140136503,45.097179159473),.UNSPECIFIED.);
#11241=B_SPLINE_CURVE_WITH_KNOTS('',3,(#47080,#47081,#47082,#47083,#47084,
#47085,#47086,#47087,#47088,#47089,#47090,#47091,#47092,#47093,#47094,#47095,
#47096,#47097,#47098,#47099,#47100,#47101),.UNSPECIFIED.,.F.,.F.,(4,3,3,
3,3,3,3,4),(-54.3587151774614,-53.9785681638036,-52.9789650496591,-51.9793619355146,
-50.9797588213701,-49.9801557072255,-48.980552593081,-48.0755298702818),
 .UNSPECIFIED.);
#11242=B_SPLINE_CURVE_WITH_KNOTS('',3,(#47102,#47103,#47104,#47105,#47106,
#47107,#47108,#47109,#47110,#47111,#47112,#47113,#47114,#47115,#47116,#47117,
#47118,#47119,#47120,#47121,#47122,#47123),.UNSPECIFIED.,.F.,.F.,(4,3,3,
3,3,3,3,4),(45.097179159473,45.9817432506475,46.981346364792,47.9809494789365,
48.980552593081,49.9801557072255,50.97975882137,51.3803644666526),
 .UNSPECIFIED.);
#11243=B_SPLINE_CURVE_WITH_KNOTS('',3,(#47128,#47129,#47130,#47131,#47132,
#47133,#47134,#47135,#47136,#47137,#47138,#47139,#47140,#47141,#47142,#47143,
#47144,#47145,#47146,#47147,#47148,#47149),.UNSPECIFIED.,.F.,.F.,(4,3,3,
3,3,3,3,4),(-60.641900484641,-59.9761868486707,-58.9765837345262,-57.9769806203817,
-56.9773775062371,-55.9777743920926,-54.9781712779481,-54.3587151774614),
 .UNSPECIFIED.);
#11244=B_SPLINE_CURVE_WITH_KNOTS('',3,(#47150,#47151,#47152,#47153,#47154,
#47155,#47156,#47157,#47158,#47159,#47160,#47161,#47162,#47163,#47164,#47165,
#47166,#47167,#47168,#47169,#47170,#47171),.UNSPECIFIED.,.F.,.F.,(4,3,3,
3,3,3,3,4),(51.3803644666526,51.9793619355146,52.9789650496591,53.9785681638036,
54.9781712779481,55.9777743920926,56.9773775062371,57.6635497738322),
 .UNSPECIFIED.);
#11245=B_SPLINE_CURVE_WITH_KNOTS('',3,(#47176,#47177,#47178,#47179,#47180,
#47181,#47182,#47183,#47184,#47185,#47186,#47187,#47188,#47189,#47190,#47191,
#47192,#47193,#47194,#47195,#47196,#47197),.UNSPECIFIED.,.F.,.F.,(4,3,3,
3,3,3,3,4),(-66.9250857918206,-65.9738055335377,-64.9742024193932,-63.9745993052487,
-62.9749961911042,-61.9753930769597,-60.9757899628152,-60.641900484641),
 .UNSPECIFIED.);
#11246=B_SPLINE_CURVE_WITH_KNOTS('',3,(#47198,#47199,#47200,#47201,#47202,
#47203,#47204,#47205,#47206,#47207,#47208,#47209,#47210,#47211,#47212,#47213,
#47214,#47215,#47216,#47217,#47218,#47219),.UNSPECIFIED.,.F.,.F.,(4,3,3,
3,3,3,3,4),(57.6635497738322,57.9769806203816,58.9765837345261,59.9761868486707,
60.9757899628152,61.9753930769597,62.9749961911042,63.9467350810118),
 .UNSPECIFIED.);
#11247=B_SPLINE_CURVE_WITH_KNOTS('',3,(#47224,#47225,#47226,#47227,#47228,
#47229,#47230,#47231,#47232,#47233,#47234,#47235,#47236,#47237,#47238,#47239,
#47240,#47241,#47242,#47243,#47244,#47245,#47246,#47247,#47248),
 .UNSPECIFIED.,.F.,.F.,(4,3,3,3,3,3,3,3,4),(-73.2082710990002,-72.9710273325493,
-71.9714242184048,-70.9718211042603,-69.9722179901158,-68.9726148759713,
-67.9730117618268,-66.9734086476822,-66.9250857918206),.UNSPECIFIED.);
#11248=B_SPLINE_CURVE_WITH_KNOTS('',3,(#47249,#47250,#47251,#47252,#47253,
#47254,#47255,#47256,#47257,#47258,#47259,#47260,#47261,#47262,#47263,#47264,
#47265,#47266,#47267,#47268,#47269,#47270,#47271,#47272,#47273),
 .UNSPECIFIED.,.F.,.F.,(4,3,3,3,3,3,3,3,4),(63.9467350810118,63.9745993052487,
64.9742024193932,65.9738055335377,66.9734086476822,67.9730117618267,68.9726148759712,
69.9722179901158,70.2299203881913),.UNSPECIFIED.);
#11249=B_SPLINE_CURVE_WITH_KNOTS('',3,(#47278,#47279,#47280,#47281,#47282,
#47283,#47284,#47285,#47286,#47287,#47288,#47289,#47290,#47291,#47292,#47293,
#47294,#47295,#47296,#47297,#47298,#47299),.UNSPECIFIED.,.F.,.F.,(4,3,3,
3,3,3,3,4),(-79.4914564061798,-78.9686460174164,-77.9690429032719,-76.9694397891273,
-75.9698366749828,-74.9702335608383,-73.9706304466938,-73.2082710990002),
 .UNSPECIFIED.);
#11250=B_SPLINE_CURVE_WITH_KNOTS('',3,(#47300,#47301,#47302,#47303,#47304,
#47305,#47306,#47307,#47308,#47309,#47310,#47311,#47312,#47313,#47314,#47315,
#47316,#47317,#47318,#47319,#47320,#47321),.UNSPECIFIED.,.F.,.F.,(4,3,3,
3,3,3,3,4),(70.2299203881913,70.9718211042603,71.9714242184048,72.9710273325493,
73.9706304466938,74.9702335608383,75.9698366749828,76.5131056953709),
 .UNSPECIFIED.);
#11251=B_SPLINE_CURVE_WITH_KNOTS('',3,(#47326,#47327,#47328,#47329,#47330,
#47331,#47332,#47333,#47334,#47335,#47336,#47337,#47338,#47339,#47340,#47341,
#47342,#47343,#47344,#47345,#47346,#47347),.UNSPECIFIED.,.F.,.F.,(4,3,3,
3,3,3,3,4),(-85.7746417133594,-84.9662647022835,-83.9666615881389,-82.9670584739944,
-81.9674553598499,-80.9678522457054,-79.9682491315609,-79.4914564061798),
 .UNSPECIFIED.);
#11252=B_SPLINE_CURVE_WITH_KNOTS('',3,(#47348,#47349,#47350,#47351,#47352,
#47353,#47354,#47355,#47356,#47357,#47358,#47359,#47360,#47361,#47362,#47363,
#47364,#47365,#47366,#47367,#47368,#47369),.UNSPECIFIED.,.F.,.F.,(4,3,3,
3,3,3,3,4),(76.5131056953709,76.9694397891273,77.9690429032718,78.9686460174164,
79.9682491315609,80.9678522457054,81.9674553598499,82.7962910025505),
 .UNSPECIFIED.);
#11253=B_SPLINE_CURVE_WITH_KNOTS('',3,(#47374,#47375,#47376,#47377,#47378,
#47379,#47380,#47381,#47382,#47383,#47384,#47385,#47386,#47387,#47388,#47389,
#47390,#47391,#47392,#47393,#47394,#47395,#47396,#47397,#47398),
 .UNSPECIFIED.,.F.,.F.,(4,3,3,3,3,3,3,3,4),(-92.057827020539,-91.963486501295,
-90.9638833871505,-89.964280273006,-88.9646771588615,-87.965074044717,-86.9654709305725,
-85.965867816428,-85.7746417133594),.UNSPECIFIED.);
#11254=B_SPLINE_CURVE_WITH_KNOTS('',3,(#47399,#47400,#47401,#47402,#47403,
#47404,#47405,#47406,#47407,#47408,#47409,#47410,#47411,#47412,#47413,#47414,
#47415,#47416,#47417,#47418,#47419,#47420,#47421,#47422,#47423),
 .UNSPECIFIED.,.F.,.F.,(4,3,3,3,3,3,3,3,4),(82.7962910025505,82.9670584739944,
83.9666615881389,84.9662647022834,85.9658678164279,86.9654709305725,87.965074044717,
88.9646771588615,89.0794763097301),.UNSPECIFIED.);
#11255=B_SPLINE_CURVE_WITH_KNOTS('',3,(#47428,#47429,#47430,#47431,#47432,
#47433,#47434,#47435,#47436,#47437,#47438,#47439,#47440,#47441,#47442,#47443,
#47444,#47445,#47446,#47447,#47448,#47449),.UNSPECIFIED.,.F.,.F.,(4,3,3,
3,3,3,3,4),(-98.3410123277186,-97.9611051861621,-96.9615020720176,-95.961898957873,
-94.9622958437285,-93.962692729584,-92.9630896154395,-92.057827020539),
 .UNSPECIFIED.);
#11256=B_SPLINE_CURVE_WITH_KNOTS('',3,(#47450,#47451,#47452,#47453,#47454,
#47455,#47456,#47457,#47458,#47459,#47460,#47461,#47462,#47463,#47464,#47465,
#47466,#47467,#47468,#47469,#47470,#47471),.UNSPECIFIED.,.F.,.F.,(4,3,3,
3,3,3,3,4),(89.0794763097301,89.964280273006,90.9638833871505,91.963486501295,
92.9630896154395,93.962692729584,94.9622958437285,95.3626616169097),
 .UNSPECIFIED.);
#11257=B_SPLINE_CURVE_WITH_KNOTS('',3,(#47476,#47477,#47478,#47479,#47480,
#47481,#47482,#47483,#47484,#47485,#47486,#47487,#47488,#47489,#47490,#47491,
#47492,#47493,#47494,#47495,#47496,#47497),.UNSPECIFIED.,.F.,.F.,(4,3,3,
3,3,3,3,4),(-104.624197634898,-103.958723871029,-102.959120756885,-101.95951764274,
-100.959914528596,-99.9603114144511,-98.9607083003066,-98.3410123277186),
 .UNSPECIFIED.);
#11258=B_SPLINE_CURVE_WITH_KNOTS('',3,(#47498,#47499,#47500,#47501,#47502,
#47503,#47504,#47505,#47506,#47507,#47508,#47509,#47510,#47511,#47512,#47513,
#47514,#47515,#47516,#47517,#47518,#47519),.UNSPECIFIED.,.F.,.F.,(4,3,3,
3,3,3,3,4),(95.3626616169097,95.961898957873,96.9615020720176,97.9611051861621,
98.9607083003066,99.9603114144511,100.959914528596,101.645846924089),
 .UNSPECIFIED.);
#11259=B_SPLINE_CURVE_WITH_KNOTS('',3,(#47524,#47525,#47526,#47527,#47528,
#47529,#47530,#47531,#47532,#47533,#47534,#47535,#47536,#47537,#47538,#47539,
#47540,#47541,#47542,#47543,#47544,#47545),.UNSPECIFIED.,.F.,.F.,(4,3,3,
3,3,3,3,4),(-110.907382942078,-109.956342555896,-108.956739441752,-107.957136327607,
-106.957533213463,-105.957930099318,-104.958326985174,-104.624197634898),
 .UNSPECIFIED.);
#11260=B_SPLINE_CURVE_WITH_KNOTS('',3,(#47546,#47547,#47548,#47549,#47550,
#47551,#47552,#47553,#47554,#47555,#47556,#47557,#47558,#47559,#47560,#47561,
#47562,#47563,#47564,#47565,#47566,#47567),.UNSPECIFIED.,.F.,.F.,(4,3,3,
3,3,3,3,4),(101.645846924089,101.95951764274,102.959120756885,103.958723871029,
104.958326985174,105.957930099318,106.957533213463,107.929032231269),
 .UNSPECIFIED.);
#11261=B_SPLINE_CURVE_WITH_KNOTS('',3,(#47572,#47573,#47574,#47575,#47576,
#47577,#47578,#47579,#47580,#47581,#47582,#47583,#47584,#47585,#47586,#47587,
#47588,#47589,#47590,#47591,#47592,#47593,#47594,#47595,#47596),
 .UNSPECIFIED.,.F.,.F.,(4,3,3,3,3,3,3,3,4),(-117.190568249257,-116.953564354908,
-115.953961240763,-114.954358126619,-113.954755012474,-112.95515189833,
-111.955548784185,-110.955945670041,-110.907382942078),.UNSPECIFIED.);
#11262=B_SPLINE_CURVE_WITH_KNOTS('',3,(#47597,#47598,#47599,#47600,#47601,
#47602,#47603,#47604,#47605,#47606,#47607,#47608,#47609,#47610,#47611,#47612,
#47613,#47614,#47615,#47616,#47617,#47618,#47619,#47620,#47621),
 .UNSPECIFIED.,.F.,.F.,(4,3,3,3,3,3,3,3,4),(107.929032231269,107.957136327607,
108.956739441752,109.956342555896,110.955945670041,111.955548784185,112.95515189833,
113.954755012474,114.212217538448),.UNSPECIFIED.);
#11263=B_SPLINE_CURVE_WITH_KNOTS('',3,(#47626,#47627,#47628,#47629,#47630,
#47631,#47632,#47633,#47634,#47635,#47636,#47637,#47638,#47639,#47640,#47641,
#47642,#47643,#47644,#47645,#47646,#47647),.UNSPECIFIED.,.F.,.F.,(4,3,3,
3,3,3,3,4),(-123.473753556437,-122.951183039775,-121.95157992563,-120.951976811486,
-119.952373697341,-118.952770583197,-117.953167469052,-117.190568249257),
 .UNSPECIFIED.);
#11264=B_SPLINE_CURVE_WITH_KNOTS('',3,(#47648,#47649,#47650,#47651,#47652,
#47653,#47654,#47655,#47656,#47657,#47658,#47659,#47660,#47661,#47662,#47663,
#47664,#47665,#47666,#47667,#47668,#47669),.UNSPECIFIED.,.F.,.F.,(4,3,3,
3,3,3,3,4),(114.212217538448,114.954358126619,115.953961240763,116.953564354908,
117.953167469052,118.952770583197,119.952373697341,120.495402845628),
 .UNSPECIFIED.);
#11265=B_SPLINE_CURVE_WITH_KNOTS('',3,(#47675,#47676,#47677,#47678),
 .UNSPECIFIED.,.F.,.F.,(4,4),(135.088484104361,135.498200854482),
 .UNSPECIFIED.);
#11266=B_SPLINE_CURVE_WITH_KNOTS('',3,(#47684,#47685,#47686,#47687,#47688,
#47689,#47690,#47691,#47692,#47693),.UNSPECIFIED.,.F.,.F.,(4,1,1,1,1,1,
1,4),(128.805298797182,129.567898016976,130.567501131121,131.567104245265,
132.56670735941,133.566310473554,134.565913587699,135.088484104361),
 .UNSPECIFIED.);
#11267=B_SPLINE_CURVE_WITH_KNOTS('',3,(#47696,#47697,#47698,#47699,#47700,
#47701,#47702,#47703,#47704,#47705),.UNSPECIFIED.,.F.,.F.,(4,1,1,1,1,1,
1,4),(128.805298797182,129.261872763039,130.261475877184,131.261078991328,
132.260682105473,133.260285219617,133.760086776689,134.259888333762),
 .UNSPECIFIED.);
#11268=B_SPLINE_CURVE_WITH_KNOTS('',3,(#47710,#47711,#47712,#47713,#47714,
#47715,#47716,#47717,#47718,#47719,#47720),.UNSPECIFIED.,.F.,.F.,(4,1,1,
1,1,1,1,1,4),(122.522113490002,122.570676217965,123.570279332109,124.569882446254,
125.569485560398,126.569088674543,127.568691788687,128.568294902832,128.805298797182),
 .UNSPECIFIED.);
#11269=B_SPLINE_CURVE_WITH_KNOTS('',3,(#47721,#47722,#47723,#47724,#47725,
#47726,#47727,#47728,#47729,#47730),.UNSPECIFIED.,.F.,.F.,(4,1,1,1,1,1,
1,4),(122.522113490002,123.264254078172,124.263857192317,125.263460306461,
126.263063420606,127.26266653475,128.262269648895,128.805298797182),
 .UNSPECIFIED.);
#11270=B_SPLINE_CURVE_WITH_KNOTS('',3,(#47735,#47736,#47737,#47738,#47739,
#47740,#47741,#47742,#47743,#47744),.UNSPECIFIED.,.F.,.F.,(4,1,1,1,1,1,
1,4),(116.238928182822,116.573057533098,117.572660647242,118.572263761387,
119.571866875531,120.571469989676,121.57107310382,122.522113490002),
 .UNSPECIFIED.);
#11271=B_SPLINE_CURVE_WITH_KNOTS('',3,(#47745,#47746,#47747,#47748,#47749,
#47750,#47751,#47752,#47753,#47754,#47755),.UNSPECIFIED.,.F.,.F.,(4,1,1,
1,1,1,1,1,4),(116.238928182822,116.26703227916,117.266635393305,118.26623850745,
119.265841621594,120.265444735739,121.265047849883,122.264650964028,122.522113490002),
 .UNSPECIFIED.);
#11272=B_SPLINE_CURVE_WITH_KNOTS('',3,(#47760,#47761,#47762,#47763,#47764,
#47765,#47766,#47767,#47768,#47769),.UNSPECIFIED.,.F.,.F.,(4,1,1,1,1,1,
1,4),(109.955742875643,110.575438848231,111.575041962375,112.57464507652,
113.574248190664,114.573851304809,115.573454418953,116.238928182822),
 .UNSPECIFIED.);
#11273=B_SPLINE_CURVE_WITH_KNOTS('',3,(#47770,#47771,#47772,#47773,#47774,
#47775,#47776,#47777,#47778,#47779),.UNSPECIFIED.,.F.,.F.,(4,1,1,1,1,1,
1,4),(109.955742875643,110.269413594293,111.269016708438,112.268619822582,
113.268222936727,114.267826050871,115.267429165016,116.238928182822),
 .UNSPECIFIED.);
#11274=B_SPLINE_CURVE_WITH_KNOTS('',3,(#47784,#47785,#47786,#47787,#47788,
#47789,#47790,#47791,#47792,#47793),.UNSPECIFIED.,.F.,.F.,(4,1,1,1,1,1,
1,4),(103.672557568463,104.577820163364,105.577423277508,106.577026391653,
107.576629505797,108.576232619942,109.575835734086,109.955742875643),
 .UNSPECIFIED.);
#11275=B_SPLINE_CURVE_WITH_KNOTS('',3,(#47794,#47795,#47796,#47797,#47798,
#47799,#47800,#47801,#47802,#47803),.UNSPECIFIED.,.F.,.F.,(4,1,1,1,1,1,
1,4),(103.672557568463,104.271794909426,105.271398023571,106.271001137715,
107.27060425186,108.270207366004,109.269810480149,109.955742875643),
 .UNSPECIFIED.);
#11276=B_SPLINE_CURVE_WITH_KNOTS('',3,(#47808,#47809,#47810,#47811,#47812,
#47813,#47814,#47815,#47816,#47817,#47818),.UNSPECIFIED.,.F.,.F.,(4,1,1,
1,1,1,1,1,4),(97.3893722612836,97.5805983643521,98.5802014784966,99.5798045926411,
100.579407706786,101.57901082093,102.578613935075,103.578217049219,103.672557568463),
 .UNSPECIFIED.);
#11277=B_SPLINE_CURVE_WITH_KNOTS('',3,(#47819,#47820,#47821,#47822,#47823,
#47824,#47825,#47826,#47827,#47828),.UNSPECIFIED.,.F.,.F.,(4,1,1,1,1,1,
1,4),(97.3893722612836,98.2741762245593,99.2737793387038,100.273382452848,
101.272985566993,102.272588681137,103.272191795282,103.672557568463),
 .UNSPECIFIED.);
#11278=B_SPLINE_CURVE_WITH_KNOTS('',3,(#47833,#47834,#47835,#47836,#47837,
#47838,#47839,#47840,#47841,#47842),.UNSPECIFIED.,.F.,.F.,(4,1,1,1,1,1,
1,4),(91.106186954104,91.582979679485,92.5825827936296,93.5821859077741,
94.5817890219186,95.5813921360631,96.5809952502076,97.3893722612836),
 .UNSPECIFIED.);
#11279=B_SPLINE_CURVE_WITH_KNOTS('',3,(#47843,#47844,#47845,#47846,#47847,
#47848,#47849,#47850,#47851,#47852,#47853),.UNSPECIFIED.,.F.,.F.,(4,1,1,
1,1,1,1,1,4),(91.106186954104,91.2769544255477,92.2765575396922,93.2761606538367,
94.2757637679812,95.2753668821258,96.2749699962703,97.2745731104148,97.3893722612836),
 .UNSPECIFIED.);
#11280=B_SPLINE_CURVE_WITH_KNOTS('',3,(#47858,#47859,#47860,#47861,#47862,
#47863,#47864,#47865,#47866,#47867),.UNSPECIFIED.,.F.,.F.,(4,1,1,1,1,1,
1,4),(84.8230016469244,85.585360994618,86.5849641087625,87.584567222907,
88.5841703370515,89.583773451196,90.5833765653405,91.106186954104),
 .UNSPECIFIED.);
#11281=B_SPLINE_CURVE_WITH_KNOTS('',3,(#47868,#47869,#47870,#47871,#47872,
#47873,#47874,#47875,#47876,#47877),.UNSPECIFIED.,.F.,.F.,(4,1,1,1,1,1,
1,4),(84.8230016469244,85.2793357406806,86.2789388548251,87.2785419689697,
88.2781450831142,89.2777481972587,90.2773513114032,91.106186954104),
 .UNSPECIFIED.);
#11282=B_SPLINE_CURVE_WITH_KNOTS('',3,(#47882,#47883,#47884,#47885,#47886,
#47887,#47888,#47889,#47890,#47891,#47892),.UNSPECIFIED.,.F.,.F.,(4,1,1,
1,1,1,1,1,4),(78.5398163397448,78.5881391956064,79.5877423097509,80.5873454238954,
81.5869485380399,82.5865516521845,83.586154766329,84.5857578804735,84.8230016469244),
 .UNSPECIFIED.);
#11283=B_SPLINE_CURVE_WITH_KNOTS('',3,(#47893,#47894,#47895,#47896,#47897,
#47898,#47899,#47900,#47901,#47902),.UNSPECIFIED.,.F.,.F.,(4,1,1,1,1,1,
1,4),(78.5398163397448,79.2817170558136,80.2813201699581,81.2809232841026,
82.2805263982471,83.2801295123916,84.2797326265361,84.8230016469244),
 .UNSPECIFIED.);
#11284=B_SPLINE_CURVE_WITH_KNOTS('',3,(#47907,#47908,#47909,#47910,#47911,
#47912,#47913,#47914,#47915,#47916),.UNSPECIFIED.,.F.,.F.,(4,1,1,1,1,1,
1,4),(72.2566310325652,72.5905205107393,73.5901236248838,74.5897267390284,
75.5893298531729,76.5889329673174,77.5885360814619,78.5398163397448),
 .UNSPECIFIED.);
#11285=B_SPLINE_CURVE_WITH_KNOTS('',3,(#47917,#47918,#47919,#47920,#47921,
#47922,#47923,#47924,#47925,#47926,#47927),.UNSPECIFIED.,.F.,.F.,(4,1,1,
1,1,1,1,1,4),(72.2566310325652,72.284495256802,73.2840983709465,74.283701485091,
75.2833045992355,76.28290771338,77.2825108275245,78.2821139416691,78.5398163397448),
 .UNSPECIFIED.);
#11286=B_SPLINE_CURVE_WITH_KNOTS('',3,(#47932,#47933,#47934,#47935,#47936,
#47937,#47938,#47939,#47940,#47941),.UNSPECIFIED.,.F.,.F.,(4,1,1,1,1,1,
1,4),(65.9734457253856,66.5929018258723,67.5925049400168,68.5921080541613,
69.5917111683058,70.5913142824503,71.5909173965948,72.2566310325652),
 .UNSPECIFIED.);
#11287=B_SPLINE_CURVE_WITH_KNOTS('',3,(#47942,#47943,#47944,#47945,#47946,
#47947,#47948,#47949,#47950,#47951),.UNSPECIFIED.,.F.,.F.,(4,1,1,1,1,1,
1,4),(65.9734457253856,66.2868765719349,67.2864796860794,68.286082800224,
69.2856859143685,70.285289028513,71.2848921426575,72.2566310325652),
 .UNSPECIFIED.);
#11288=B_SPLINE_CURVE_WITH_KNOTS('',3,(#47956,#47957,#47958,#47959,#47960,
#47961,#47962,#47963,#47964,#47965),.UNSPECIFIED.,.F.,.F.,(4,1,1,1,1,1,
1,4),(59.690260418206,60.5952831410052,61.5948862551497,62.5944893692942,
63.5940924834387,64.5936955975832,65.5932987117278,65.9734457253856),
 .UNSPECIFIED.);
#11289=B_SPLINE_CURVE_WITH_KNOTS('',3,(#47966,#47967,#47968,#47969,#47970,
#47971,#47972,#47973,#47974,#47975),.UNSPECIFIED.,.F.,.F.,(4,1,1,1,1,1,
1,4),(59.690260418206,60.2892578870679,61.2888610012124,62.2884641153569,
63.2880672295014,64.2876703436459,65.2872734577904,65.9734457253856),
 .UNSPECIFIED.);
#11290=B_SPLINE_CURVE_WITH_KNOTS('',3,(#47980,#47981,#47982,#47983,#47984,
#47985,#47986,#47987,#47988,#47989,#47990),.UNSPECIFIED.,.F.,.F.,(4,1,1,
1,1,1,1,1,4),(53.4070751110264,53.5980613419936,54.5976644561381,55.5972675702826,
56.5968706844272,57.5964737985717,58.5960769127162,59.5956800268607,59.690260418206),
 .UNSPECIFIED.);
#11291=B_SPLINE_CURVE_WITH_KNOTS('',3,(#47991,#47992,#47993,#47994,#47995,
#47996,#47997,#47998,#47999,#48000),.UNSPECIFIED.,.F.,.F.,(4,1,1,1,1,1,
1,4),(53.4070751110264,54.2916392022008,55.2912423163453,56.2908454304898,
57.2904485446343,58.2900516587789,59.2896547729234,59.690260418206),
 .UNSPECIFIED.);
#11292=B_SPLINE_CURVE_WITH_KNOTS('',3,(#48005,#48006,#48007,#48008,#48009,
#48010,#48011,#48012,#48013,#48014),.UNSPECIFIED.,.F.,.F.,(4,1,1,1,1,1,
1,4),(47.1238898038469,47.6004426571266,48.6000457712711,49.5996488854156,
50.5992519995601,51.5988551137046,52.5984582278491,53.4070751110264),
 .UNSPECIFIED.);
#11293=B_SPLINE_CURVE_WITH_KNOTS('',3,(#48015,#48016,#48017,#48018,#48019,
#48020,#48021,#48022,#48023,#48024,#48025),.UNSPECIFIED.,.F.,.F.,(4,1,1,
1,1,1,1,1,4),(47.1238898038468,47.2944174031892,48.2940205173337,49.2936236314783,
50.2932267456228,51.2928298597673,52.2924329739118,53.2920360880563,53.4070751110264),
 .UNSPECIFIED.);
#11294=B_SPLINE_CURVE_WITH_KNOTS('',3,(#48030,#48031,#48032,#48033,#48034,
#48035,#48036,#48037,#48038,#48039),.UNSPECIFIED.,.F.,.F.,(4,1,1,1,1,1,
1,4),(40.8407044966673,41.6028239722595,42.602427086404,43.6020302005485,
44.601633314693,45.6012364288375,46.600839542982,47.1238898038469),
 .UNSPECIFIED.);
#11295=B_SPLINE_CURVE_WITH_KNOTS('',3,(#48040,#48041,#48042,#48043,#48044,
#48045,#48046,#48047,#48048,#48049),.UNSPECIFIED.,.F.,.F.,(4,1,1,1,1,1,
1,4),(40.8407044966672,41.2967987183222,42.2964018324667,43.2960049466112,
44.2956080607557,45.2952111749002,46.2948142890447,47.1238898038468),
 .UNSPECIFIED.);
#11296=B_SPLINE_CURVE_WITH_KNOTS('',3,(#48054,#48055,#48056,#48057,#48058,
#48059,#48060,#48061,#48062,#48063,#48064),.UNSPECIFIED.,.F.,.F.,(4,1,1,
1,1,1,1,1,4),(34.5575191894877,34.6056021732479,35.6052052873924,36.6048084015369,
37.6044115156814,38.604014629826,39.6036177439705,40.603220858115,40.8407044966673),
 .UNSPECIFIED.);
#11297=B_SPLINE_CURVE_WITH_KNOTS('',3,(#48065,#48066,#48067,#48068,#48069,
#48070,#48071,#48072,#48073,#48074),.UNSPECIFIED.,.F.,.F.,(4,1,1,1,1,1,
1,4),(34.5575191894876,35.2991800334551,36.2987831475996,37.2983862617441,
38.2979893758886,39.2975924900331,40.2971956041777,40.8407044966672),
 .UNSPECIFIED.);
#11298=B_SPLINE_CURVE_WITH_KNOTS('',3,(#48079,#48080,#48081,#48082,#48083,
#48084,#48085,#48086,#48087,#48088),.UNSPECIFIED.,.F.,.F.,(4,1,1,1,1,1,
1,4),(28.2743338823081,28.6079834883808,29.6075866025254,30.6071897166699,
31.6067928308144,32.6063959449589,33.6059990591034,34.5575191894877),
 .UNSPECIFIED.);
#11299=B_SPLINE_CURVE_WITH_KNOTS('',3,(#48089,#48090,#48091,#48092,#48093,
#48094,#48095,#48096,#48097,#48098,#48099),.UNSPECIFIED.,.F.,.F.,(4,1,1,
1,1,1,1,1,4),(28.274333882308,28.3019582344435,29.301561348588,30.3011644627325,
31.3007675768771,32.3003706910216,33.2999738051661,34.2995769193106,34.5575191894876),
 .UNSPECIFIED.);
#11300=B_SPLINE_CURVE_WITH_KNOTS('',3,(#48104,#48105,#48106,#48107,#48108,
#48109,#48110,#48111,#48112,#48113),.UNSPECIFIED.,.F.,.F.,(4,1,1,1,1,1,
1,4),(21.9911485751285,22.6103648035138,23.6099679176583,24.6095710318028,
25.6091741459473,26.6087772600918,27.6083803742363,28.2743338823081),
 .UNSPECIFIED.);
#11301=B_SPLINE_CURVE_WITH_KNOTS('',3,(#48114,#48115,#48116,#48117,#48118,
#48119,#48120,#48121,#48122,#48123),.UNSPECIFIED.,.F.,.F.,(4,1,1,1,1,1,
1,4),(21.9911485751285,22.3043395495765,23.303942663721,24.3035457778655,
25.30314889201,26.3027520061545,27.302355120299,28.274333882308),
 .UNSPECIFIED.);
#11302=B_SPLINE_CURVE_WITH_KNOTS('',3,(#48128,#48129,#48130,#48131,#48132,
#48133,#48134,#48135,#48136,#48137),.UNSPECIFIED.,.F.,.F.,(4,1,1,1,1,1,
1,4),(15.7079632679489,16.6127461186467,17.6123492327912,18.6119523469357,
19.6115554610803,20.6111585752248,21.6107616893693,21.9911485751285),
 .UNSPECIFIED.);
#11303=B_SPLINE_CURVE_WITH_KNOTS('',3,(#48138,#48139,#48140,#48141,#48142,
#48143,#48144,#48145,#48146,#48147),.UNSPECIFIED.,.F.,.F.,(4,1,1,1,1,1,
1,4),(15.7079632679489,16.3067208647094,17.3063239788539,18.3059270929984,
19.3055302071429,20.3051333212874,21.3047364354319,21.9911485751285),
 .UNSPECIFIED.);
#11304=B_SPLINE_CURVE_WITH_KNOTS('',3,(#48673,#48674,#48675,#48676,#48677,
#48678,#48679,#48680,#48681,#48682,#48683,#48684,#48685,#48686,#48687,#48688,
#48689,#48690,#48691,#48692,#48693,#48694,#48695,#48696,#48697,#48698,#48699,
#48700,#48701,#48702,#48703,#48704,#48705,#48706,#48707,#48708,#48709,#48710,
#48711,#48712,#48713,#48714,#48715,#48716,#48717,#48718,#48719,#48720,#48721,
#48722,#48723,#48724,#48725,#48726,#48727,#48728,#48729,#48730,#48731,#48732,
#48733,#48734,#48735,#48736,#48737,#48738,#48739,#48740,#48741,#48742,#48743,
#48744,#48745,#48746,#48747,#48748,#48749,#48750,#48751,#48752,#48753,#48754,
#48755,#48756,#48757,#48758,#48759,#48760,#48761,#48762,#48763,#48764,#48765,
#48766,#48767,#48768,#48769,#48770,#48771,#48772,#48773,#48774,#48775),
 .UNSPECIFIED.,.F.,.F.,(4,3,3,3,3,3,3,3,3,3,3,3,3,3,3,3,3,3,3,3,3,3,3,3,
3,3,3,3,3,3,3,3,3,3,4),(-0.933975894023114,-0.900886022956469,-0.857613677956334,
-0.830917467558831,-0.811990732117496,-0.805266958984206,-0.762537705919167,
-0.721029781628806,-0.68471034787474,-0.677426067872528,-0.635390348422708,
-0.593572252555102,-0.552797767315397,-0.522216903385619,-0.510030154625355,
-0.502729037187648,-0.496839898567668,-0.456766765593561,-0.430474311596282,
-0.389892426332242,-0.34937929636466,-0.329910151917754,-0.324685557329147,
-0.285203392664255,-0.245885205074442,-0.210138932487817,-0.18387156592684,
-0.169358115925774,-0.161848011397128,-0.156162121436153,-0.117121591077115,
-0.0788937454479904,-0.0394468727239952,-0.00242854395559244,0.),
 .UNSPECIFIED.);
#11305=B_SPLINE_CURVE_WITH_KNOTS('',3,(#48776,#48777,#48778,#48779,#48780,
#48781,#48782,#48783,#48784,#48785,#48786,#48787,#48788),.UNSPECIFIED.,
 .F.,.F.,(4,3,3,3,4),(120.495402845628,120.951976811486,121.95157992563,
122.951183039775,123.883470306557),.UNSPECIFIED.);
#11306=B_SPLINE_CURVE_WITH_KNOTS('',3,(#48790,#48791,#48792,#48793,#48794,
#48795,#48796,#48797,#48798,#48799,#48800,#48801,#48802,#48803,#48804,#48805,
#48806,#48807,#48808,#48809,#48810,#48811,#48812,#48813,#48814,#48815,#48816,
#48817,#48818,#48819,#48820,#48821,#48822,#48823,#48824,#48825,#48826,#48827,
#48828,#48829,#48830,#48831,#48832,#48833,#48834,#48835,#48836,#48837,#48838,
#48839,#48840,#48841,#48842,#48843,#48844,#48845,#48846,#48847,#48848,#48849,
#48850,#48851,#48852,#48853,#48854,#48855,#48856,#48857,#48858,#48859,#48860,
#48861,#48862,#48863,#48864,#48865,#48866,#48867,#48868,#48869,#48870,#48871,
#48872,#48873,#48874,#48875,#48876,#48877,#48878,#48879,#48880,#48881,#48882,
#48883,#48884,#48885,#48886,#48887,#48888,#48889,#48890,#48891,#48892),
 .UNSPECIFIED.,.F.,.F.,(4,3,3,3,3,3,3,3,3,3,3,3,3,3,3,3,3,3,3,3,3,3,3,3,
3,3,3,3,3,3,3,3,3,3,4),(-0.937740963081769,-0.909984679133564,-0.872833882725954,
-0.847996397065448,-0.833928218367593,-0.824785785263065,-0.78663373762343,
-0.747733784440234,-0.730715054922586,-0.721961762671648,-0.713934774220468,
-0.674204019543976,-0.633909683375831,-0.593656192357265,-0.564100672307414,
-0.551648204867746,-0.54396197545851,-0.502501117350991,-0.475434112157862,
-0.435310758308129,-0.394542023824858,-0.374961735244211,-0.367483120962523,
-0.326359080771091,-0.284254421333978,-0.242709754795601,-0.212371035446151,
-0.198407867967393,-0.190923667635028,-0.185034664212022,-0.142232442426345,
-0.0988549974710058,-0.0555174255396185,-0.0127493435743661,0.),
 .UNSPECIFIED.);
#11307=B_SPLINE_CURVE_WITH_KNOTS('',3,(#48893,#48894,#48895,#48896,#48897,
#48898,#48899,#48900,#48901),.UNSPECIFIED.,.F.,.F.,(4,1,1,1,1,1,4),(10.3764180272042,
11.3087052939868,12.3083084081313,13.3079115222759,14.3075146364204,15.3071177505649,
15.7079632679489),.UNSPECIFIED.);
#11308=B_SPLINE_CURVE_WITH_KNOTS('',3,(#48907,#48908,#48909,#48910,#48911,
#48912,#48913,#48914,#48915,#48916,#48917,#48918,#48919,#48920,#48921,#48922,
#48923,#48924,#48925,#48926,#48927,#48928,#48929,#48930,#48931,#48932,#48933,
#48934,#48935,#48936,#48937,#48938,#48939,#48940,#48941,#48942,#48943,#48944,
#48945,#48946,#48947,#48948,#48949,#48950,#48951,#48952,#48953,#48954,#48955,
#48956,#48957,#48958,#48959,#48960,#48961,#48962,#48963,#48964,#48965,#48966,
#48967,#48968,#48969,#48970,#48971,#48972,#48973,#48974,#48975,#48976,#48977,
#48978,#48979,#48980,#48981,#48982,#48983,#48984,#48985,#48986,#48987,#48988,
#48989,#48990,#48991,#48992,#48993,#48994,#48995,#48996,#48997,#48998,#48999,
#49000,#49001,#49002,#49003,#49004,#49005,#49006,#49007,#49008,#49009),
 .UNSPECIFIED.,.F.,.F.,(4,3,3,3,3,3,3,3,3,3,3,3,3,3,3,3,3,3,3,3,3,3,3,3,
3,3,3,3,3,3,3,3,3,3,4),(-0.933975894023115,-0.90088602295648,-0.857613686561679,
-0.830917475626341,-0.811990735770248,-0.805266957540168,-0.762537700650808,
-0.72102977701899,-0.684710343841149,-0.67742606502949,-0.635390295376529,
-0.593572109506116,-0.552797660028653,-0.522216822920556,-0.510030127654026,
-0.502728981266388,-0.496839893719554,-0.456766643291822,-0.430474311596264,
-0.389892498153584,-0.349379548247307,-0.329910675083222,-0.324686090829592,
-0.285204009769594,-0.24588601906745,-0.210138932487834,-0.183871565926854,
-0.169358141411446,-0.161848180179082,-0.156162148451424,-0.117121611338568,
-0.0788936961114827,-0.0394468480557413,-0.00242847333026767,0.),
 .UNSPECIFIED.);
#11309=B_SPLINE_CURVE_WITH_KNOTS('',3,(#49012,#49013,#49014,#49015,#49016,
#49017,#49018,#49019,#49020),.UNSPECIFIED.,.F.,.F.,(4,1,1,1,1,1,4),(11.6147305479242,
12.1145321049964,12.6143336620687,13.6139367762132,14.6135398903577,15.6131430045022,
15.7079632679489),.UNSPECIFIED.);
#11310=B_SPLINE_CURVE_WITH_KNOTS('',3,(#49546,#49547,#49548,#49549,#49550,
#49551,#49552,#49553,#49554,#49555,#49556,#49557,#49558,#49559,#49560,#49561,
#49562,#49563,#49564,#49565,#49566,#49567,#49568,#49569,#49570,#49571,#49572,
#49573,#49574,#49575,#49576,#49577,#49578,#49579,#49580,#49581,#49582,#49583,
#49584,#49585,#49586,#49587,#49588,#49589,#49590,#49591,#49592,#49593,#49594,
#49595,#49596,#49597,#49598,#49599,#49600,#49601,#49602,#49603,#49604,#49605,
#49606,#49607,#49608,#49609,#49610,#49611,#49612,#49613,#49614,#49615,#49616,
#49617,#49618,#49619,#49620,#49621,#49622,#49623,#49624,#49625,#49626,#49627,
#49628,#49629,#49630,#49631,#49632,#49633,#49634,#49635,#49636,#49637,#49638,
#49639,#49640,#49641,#49642,#49643,#49644,#49645,#49646,#49647,#49648),
 .UNSPECIFIED.,.F.,.F.,(4,3,3,3,3,3,3,3,3,3,3,3,3,3,3,3,3,3,3,3,3,3,3,3,
3,3,3,3,3,3,3,3,3,3,4),(-0.93774096308164,-0.909984679133421,-0.872833901724178,
-0.847996414876281,-0.833928216062254,-0.824785782258315,-0.786633754260955,
-0.747733798998064,-0.730715068570549,-0.721961765812645,-0.713934771789967,
-0.674204030030189,-0.633909683853084,-0.593656117964,-0.564100616512456,
-0.551648127597297,-0.543961983767159,-0.502501076596855,-0.475434112157824,
-0.43531058957835,-0.394541812627602,-0.374961344140611,-0.367483133322358,
-0.326358922649391,-0.284254298812646,-0.24270975479558,-0.212371035446133,
-0.198407868112275,-0.190923678285126,-0.185034666341196,-0.142232895600103,
-0.0988556198980695,-0.0555180472647553,-0.0127497906429885,0.),
 .UNSPECIFIED.);
#11311=B_SPLINE_CURVE_WITH_KNOTS('',3,(#49649,#49650,#49651,#49652,#49653,
#49654,#49655,#49656,#49657,#49658,#49659,#49660,#49661),.UNSPECIFIED.,
 .F.,.F.,(4,3,3,3,4),(-125.949992382208,-125.450190825136,-124.950389268064,
-123.950786153919,-123.473753556437),.UNSPECIFIED.);
#13354=VERTEX_POINT('',#46702);
#13355=VERTEX_POINT('',#46703);
#13356=VERTEX_POINT('',#46705);
#13357=VERTEX_POINT('',#46716);
#13358=VERTEX_POINT('',#46729);
#13359=VERTEX_POINT('',#46730);
#13360=VERTEX_POINT('',#46777);
#13361=VERTEX_POINT('',#46778);
#13362=VERTEX_POINT('',#46825);
#13363=VERTEX_POINT('',#46826);
#13364=VERTEX_POINT('',#46873);
#13365=VERTEX_POINT('',#46874);
#13366=VERTEX_POINT('',#46927);
#13367=VERTEX_POINT('',#46928);
#13368=VERTEX_POINT('',#46975);
#13369=VERTEX_POINT('',#46976);
#13370=VERTEX_POINT('',#47023);
#13371=VERTEX_POINT('',#47024);
#13372=VERTEX_POINT('',#47077);
#13373=VERTEX_POINT('',#47078);
#13374=VERTEX_POINT('',#47125);
#13375=VERTEX_POINT('',#47126);
#13376=VERTEX_POINT('',#47173);
#13377=VERTEX_POINT('',#47174);
#13378=VERTEX_POINT('',#47221);
#13379=VERTEX_POINT('',#47222);
#13380=VERTEX_POINT('',#47275);
#13381=VERTEX_POINT('',#47276);
#13382=VERTEX_POINT('',#47323);
#13383=VERTEX_POINT('',#47324);
#13384=VERTEX_POINT('',#47371);
#13385=VERTEX_POINT('',#47372);
#13386=VERTEX_POINT('',#47425);
#13387=VERTEX_POINT('',#47426);
#13388=VERTEX_POINT('',#47473);
#13389=VERTEX_POINT('',#47474);
#13390=VERTEX_POINT('',#47521);
#13391=VERTEX_POINT('',#47522);
#13392=VERTEX_POINT('',#47569);
#13393=VERTEX_POINT('',#47570);
#13394=VERTEX_POINT('',#47623);
#13395=VERTEX_POINT('',#47624);
#13396=VERTEX_POINT('',#47671);
#13397=VERTEX_POINT('',#47672);
#13398=VERTEX_POINT('',#47674);
#13399=VERTEX_POINT('',#47681);
#13400=VERTEX_POINT('',#47682);
#13401=VERTEX_POINT('',#47694);
#13402=VERTEX_POINT('',#47707);
#13403=VERTEX_POINT('',#47708);
#13404=VERTEX_POINT('',#47732);
#13405=VERTEX_POINT('',#47733);
#13406=VERTEX_POINT('',#47757);
#13407=VERTEX_POINT('',#47758);
#13408=VERTEX_POINT('',#47781);
#13409=VERTEX_POINT('',#47782);
#13410=VERTEX_POINT('',#47805);
#13411=VERTEX_POINT('',#47806);
#13412=VERTEX_POINT('',#47830);
#13413=VERTEX_POINT('',#47831);
#13414=VERTEX_POINT('',#47855);
#13415=VERTEX_POINT('',#47856);
#13416=VERTEX_POINT('',#47879);
#13417=VERTEX_POINT('',#47880);
#13418=VERTEX_POINT('',#47904);
#13419=VERTEX_POINT('',#47905);
#13420=VERTEX_POINT('',#47929);
#13421=VERTEX_POINT('',#47930);
#13422=VERTEX_POINT('',#47953);
#13423=VERTEX_POINT('',#47954);
#13424=VERTEX_POINT('',#47977);
#13425=VERTEX_POINT('',#47978);
#13426=VERTEX_POINT('',#48002);
#13427=VERTEX_POINT('',#48003);
#13428=VERTEX_POINT('',#48027);
#13429=VERTEX_POINT('',#48028);
#13430=VERTEX_POINT('',#48051);
#13431=VERTEX_POINT('',#48052);
#13432=VERTEX_POINT('',#48076);
#13433=VERTEX_POINT('',#48077);
#13434=VERTEX_POINT('',#48101);
#13435=VERTEX_POINT('',#48102);
#13436=VERTEX_POINT('',#48125);
#13437=VERTEX_POINT('',#48126);
#13438=VERTEX_POINT('',#48672);
#13439=VERTEX_POINT('',#48789);
#13440=VERTEX_POINT('',#48903);
#13441=VERTEX_POINT('',#48906);
#13442=VERTEX_POINT('',#49545);
#13443=VERTEX_POINT('',#49663);
#13444=VERTEX_POINT('',#49664);
#13445=VERTEX_POINT('',#49668);
#13446=VERTEX_POINT('',#49672);
#13447=VERTEX_POINT('',#49676);
#13448=VERTEX_POINT('',#49680);
#13449=VERTEX_POINT('',#49684);
#13450=VERTEX_POINT('',#49687);
#13451=VERTEX_POINT('',#49695);
#13452=VERTEX_POINT('',#49697);
#13453=VERTEX_POINT('',#49701);
#13454=VERTEX_POINT('',#49705);
#13455=VERTEX_POINT('',#49709);
#13456=VERTEX_POINT('',#49711);
#13457=VERTEX_POINT('',#49722);
#16959=EDGE_CURVE('',#13354,#13355,#3637,.T.);
#16960=EDGE_CURVE('',#13354,#13356,#11225,.T.);
#16961=EDGE_CURVE('',#13356,#13357,#10872,.T.);
#16962=EDGE_CURVE('',#13357,#13355,#11226,.T.);
#16963=EDGE_CURVE('',#13358,#13359,#3638,.T.);
#16964=EDGE_CURVE('',#13358,#13354,#11227,.T.);
#16965=EDGE_CURVE('',#13355,#13359,#11228,.T.);
#16966=EDGE_CURVE('',#13360,#13361,#3639,.T.);
#16967=EDGE_CURVE('',#13360,#13358,#11229,.T.);
#16968=EDGE_CURVE('',#13359,#13361,#11230,.T.);
#16969=EDGE_CURVE('',#13362,#13363,#3640,.T.);
#16970=EDGE_CURVE('',#13362,#13360,#11231,.T.);
#16971=EDGE_CURVE('',#13361,#13363,#11232,.T.);
#16972=EDGE_CURVE('',#13364,#13365,#3641,.T.);
#16973=EDGE_CURVE('',#13364,#13362,#11233,.T.);
#16974=EDGE_CURVE('',#13363,#13365,#11234,.T.);
#16975=EDGE_CURVE('',#13366,#13367,#3642,.T.);
#16976=EDGE_CURVE('',#13366,#13364,#11235,.T.);
#16977=EDGE_CURVE('',#13365,#13367,#11236,.T.);
#16978=EDGE_CURVE('',#13368,#13369,#3643,.T.);
#16979=EDGE_CURVE('',#13368,#13366,#11237,.T.);
#16980=EDGE_CURVE('',#13367,#13369,#11238,.T.);
#16981=EDGE_CURVE('',#13370,#13371,#3644,.T.);
#16982=EDGE_CURVE('',#13370,#13368,#11239,.T.);
#16983=EDGE_CURVE('',#13369,#13371,#11240,.T.);
#16984=EDGE_CURVE('',#13372,#13373,#3645,.T.);
#16985=EDGE_CURVE('',#13372,#13370,#11241,.T.);
#16986=EDGE_CURVE('',#13371,#13373,#11242,.T.);
#16987=EDGE_CURVE('',#13374,#13375,#3646,.T.);
#16988=EDGE_CURVE('',#13374,#13372,#11243,.T.);
#16989=EDGE_CURVE('',#13373,#13375,#11244,.T.);
#16990=EDGE_CURVE('',#13376,#13377,#3647,.T.);
#16991=EDGE_CURVE('',#13376,#13374,#11245,.T.);
#16992=EDGE_CURVE('',#13375,#13377,#11246,.T.);
#16993=EDGE_CURVE('',#13378,#13379,#3648,.T.);
#16994=EDGE_CURVE('',#13378,#13376,#11247,.T.);
#16995=EDGE_CURVE('',#13377,#13379,#11248,.T.);
#16996=EDGE_CURVE('',#13380,#13381,#3649,.T.);
#16997=EDGE_CURVE('',#13380,#13378,#11249,.T.);
#16998=EDGE_CURVE('',#13379,#13381,#11250,.T.);
#16999=EDGE_CURVE('',#13382,#13383,#3650,.T.);
#17000=EDGE_CURVE('',#13382,#13380,#11251,.T.);
#17001=EDGE_CURVE('',#13381,#13383,#11252,.T.);
#17002=EDGE_CURVE('',#13384,#13385,#3651,.T.);
#17003=EDGE_CURVE('',#13384,#13382,#11253,.T.);
#17004=EDGE_CURVE('',#13383,#13385,#11254,.T.);
#17005=EDGE_CURVE('',#13386,#13387,#3652,.T.);
#17006=EDGE_CURVE('',#13386,#13384,#11255,.T.);
#17007=EDGE_CURVE('',#13385,#13387,#11256,.T.);
#17008=EDGE_CURVE('',#13388,#13389,#3653,.T.);
#17009=EDGE_CURVE('',#13388,#13386,#11257,.T.);
#17010=EDGE_CURVE('',#13387,#13389,#11258,.T.);
#17011=EDGE_CURVE('',#13390,#13391,#3654,.T.);
#17012=EDGE_CURVE('',#13390,#13388,#11259,.T.);
#17013=EDGE_CURVE('',#13389,#13391,#11260,.T.);
#17014=EDGE_CURVE('',#13392,#13393,#3655,.T.);
#17015=EDGE_CURVE('',#13392,#13390,#11261,.T.);
#17016=EDGE_CURVE('',#13391,#13393,#11262,.T.);
#17017=EDGE_CURVE('',#13394,#13395,#3656,.T.);
#17018=EDGE_CURVE('',#13394,#13392,#11263,.T.);
#17019=EDGE_CURVE('',#13393,#13395,#11264,.T.);
#17020=EDGE_CURVE('',#13396,#13397,#3657,.T.);
#17021=EDGE_CURVE('',#13396,#13398,#11265,.T.);
#17022=EDGE_CURVE('',#13397,#13398,#10873,.T.);
#17023=EDGE_CURVE('',#13399,#13400,#3658,.T.);
#17024=EDGE_CURVE('',#13399,#13396,#11266,.T.);
#17025=EDGE_CURVE('',#13401,#13397,#10874,.T.);
#17026=EDGE_CURVE('',#13400,#13401,#11267,.T.);
#17027=EDGE_CURVE('',#13402,#13403,#3659,.T.);
#17028=EDGE_CURVE('',#13402,#13399,#11268,.T.);
#17029=EDGE_CURVE('',#13403,#13400,#11269,.T.);
#17030=EDGE_CURVE('',#13404,#13405,#3660,.T.);
#17031=EDGE_CURVE('',#13404,#13402,#11270,.T.);
#17032=EDGE_CURVE('',#13405,#13403,#11271,.T.);
#17033=EDGE_CURVE('',#13406,#13407,#3661,.T.);
#17034=EDGE_CURVE('',#13406,#13404,#11272,.T.);
#17035=EDGE_CURVE('',#13407,#13405,#11273,.T.);
#17036=EDGE_CURVE('',#13408,#13409,#3662,.T.);
#17037=EDGE_CURVE('',#13408,#13406,#11274,.T.);
#17038=EDGE_CURVE('',#13409,#13407,#11275,.T.);
#17039=EDGE_CURVE('',#13410,#13411,#3663,.T.);
#17040=EDGE_CURVE('',#13410,#13408,#11276,.T.);
#17041=EDGE_CURVE('',#13411,#13409,#11277,.T.);
#17042=EDGE_CURVE('',#13412,#13413,#3664,.T.);
#17043=EDGE_CURVE('',#13412,#13410,#11278,.T.);
#17044=EDGE_CURVE('',#13413,#13411,#11279,.T.);
#17045=EDGE_CURVE('',#13414,#13415,#3665,.T.);
#17046=EDGE_CURVE('',#13414,#13412,#11280,.T.);
#17047=EDGE_CURVE('',#13415,#13413,#11281,.T.);
#17048=EDGE_CURVE('',#13416,#13417,#3666,.T.);
#17049=EDGE_CURVE('',#13416,#13414,#11282,.T.);
#17050=EDGE_CURVE('',#13417,#13415,#11283,.T.);
#17051=EDGE_CURVE('',#13418,#13419,#3667,.T.);
#17052=EDGE_CURVE('',#13418,#13416,#11284,.T.);
#17053=EDGE_CURVE('',#13419,#13417,#11285,.T.);
#17054=EDGE_CURVE('',#13420,#13421,#3668,.T.);
#17055=EDGE_CURVE('',#13420,#13418,#11286,.T.);
#17056=EDGE_CURVE('',#13421,#13419,#11287,.T.);
#17057=EDGE_CURVE('',#13422,#13423,#3669,.T.);
#17058=EDGE_CURVE('',#13422,#13420,#11288,.T.);
#17059=EDGE_CURVE('',#13423,#13421,#11289,.T.);
#17060=EDGE_CURVE('',#13424,#13425,#3670,.T.);
#17061=EDGE_CURVE('',#13424,#13422,#11290,.T.);
#17062=EDGE_CURVE('',#13425,#13423,#11291,.T.);
#17063=EDGE_CURVE('',#13426,#13427,#3671,.T.);
#17064=EDGE_CURVE('',#13426,#13424,#11292,.T.);
#17065=EDGE_CURVE('',#13427,#13425,#11293,.T.);
#17066=EDGE_CURVE('',#13428,#13429,#3672,.T.);
#17067=EDGE_CURVE('',#13428,#13426,#11294,.T.);
#17068=EDGE_CURVE('',#13429,#13427,#11295,.T.);
#17069=EDGE_CURVE('',#13430,#13431,#3673,.T.);
#17070=EDGE_CURVE('',#13430,#13428,#11296,.T.);
#17071=EDGE_CURVE('',#13431,#13429,#11297,.T.);
#17072=EDGE_CURVE('',#13432,#13433,#3674,.T.);
#17073=EDGE_CURVE('',#13432,#13430,#11298,.T.);
#17074=EDGE_CURVE('',#13433,#13431,#11299,.T.);
#17075=EDGE_CURVE('',#13434,#13435,#3675,.T.);
#17076=EDGE_CURVE('',#13434,#13432,#11300,.T.);
#17077=EDGE_CURVE('',#13435,#13433,#11301,.T.);
#17078=EDGE_CURVE('',#13436,#13437,#3676,.T.);
#17079=EDGE_CURVE('',#13436,#13434,#11302,.T.);
#17080=EDGE_CURVE('',#13437,#13435,#11303,.T.);
#17081=EDGE_CURVE('',#13438,#13401,#11304,.T.);
#17082=EDGE_CURVE('',#13395,#13438,#11305,.T.);
#17083=EDGE_CURVE('',#13439,#13357,#11306,.T.);
#17084=EDGE_CURVE('',#13439,#13437,#11307,.T.);
#17085=EDGE_CURVE('',#13357,#13440,#10875,.T.);
#17086=EDGE_CURVE('',#13440,#13356,#10876,.T.);
#17087=EDGE_CURVE('',#13356,#13441,#11308,.T.);
#17088=EDGE_CURVE('',#13441,#13439,#10877,.T.);
#17089=EDGE_CURVE('',#13441,#13436,#11309,.T.);
#17090=EDGE_CURVE('',#13398,#13442,#11310,.T.);
#17091=EDGE_CURVE('',#13442,#13394,#11311,.T.);
#17092=EDGE_CURVE('',#13443,#13444,#189,.T.);
#17093=EDGE_CURVE('',#13445,#13443,#190,.T.);
#17094=EDGE_CURVE('',#13446,#13445,#191,.T.);
#17095=EDGE_CURVE('',#13447,#13446,#192,.T.);
#17096=EDGE_CURVE('',#13448,#13447,#193,.T.);
#17097=EDGE_CURVE('',#13448,#13449,#3677,.T.);
#17098=EDGE_CURVE('',#13449,#13449,#10878,.T.);
#17099=EDGE_CURVE('',#13450,#13448,#194,.T.);
#17100=EDGE_CURVE('',#13444,#13450,#195,.T.);
#17101=EDGE_CURVE('',#13451,#13446,#3678,.T.);
#17102=EDGE_CURVE('',#13451,#13452,#3679,.T.);
#17103=EDGE_CURVE('',#13452,#13447,#3680,.T.);
#17104=EDGE_CURVE('',#13453,#13445,#3681,.T.);
#17105=EDGE_CURVE('',#13453,#13451,#3682,.T.);
#17106=EDGE_CURVE('',#13454,#13443,#3683,.T.);
#17107=EDGE_CURVE('',#13454,#13453,#3684,.T.);
#17108=EDGE_CURVE('',#13455,#13454,#3685,.T.);
#17109=EDGE_CURVE('',#13456,#13455,#3686,.T.);
#17110=EDGE_CURVE('',#13452,#13456,#3687,.T.);
#17111=EDGE_CURVE('',#13442,#13438,#10879,.F.);
#17112=EDGE_CURVE('',#13455,#13444,#3688,.T.);
#17113=EDGE_CURVE('',#13456,#13450,#3689,.T.);
#17114=EDGE_CURVE('',#13457,#13457,#10880,.T.);
#17115=EDGE_CURVE('',#13440,#13457,#3690,.T.);
#23910=ORIENTED_EDGE('',*,*,#16959,.F.);
#23911=ORIENTED_EDGE('',*,*,#16960,.T.);
#23912=ORIENTED_EDGE('',*,*,#16961,.T.);
#23913=ORIENTED_EDGE('',*,*,#16962,.T.);
#23914=ORIENTED_EDGE('',*,*,#16963,.F.);
#23915=ORIENTED_EDGE('',*,*,#16964,.T.);
#23916=ORIENTED_EDGE('',*,*,#16959,.T.);
#23917=ORIENTED_EDGE('',*,*,#16965,.T.);
#23918=ORIENTED_EDGE('',*,*,#16966,.F.);
#23919=ORIENTED_EDGE('',*,*,#16967,.T.);
#23920=ORIENTED_EDGE('',*,*,#16963,.T.);
#23921=ORIENTED_EDGE('',*,*,#16968,.T.);
#23922=ORIENTED_EDGE('',*,*,#16969,.F.);
#23923=ORIENTED_EDGE('',*,*,#16970,.T.);
#23924=ORIENTED_EDGE('',*,*,#16966,.T.);
#23925=ORIENTED_EDGE('',*,*,#16971,.T.);
#23926=ORIENTED_EDGE('',*,*,#16972,.F.);
#23927=ORIENTED_EDGE('',*,*,#16973,.T.);
#23928=ORIENTED_EDGE('',*,*,#16969,.T.);
#23929=ORIENTED_EDGE('',*,*,#16974,.T.);
#23930=ORIENTED_EDGE('',*,*,#16975,.F.);
#23931=ORIENTED_EDGE('',*,*,#16976,.T.);
#23932=ORIENTED_EDGE('',*,*,#16972,.T.);
#23933=ORIENTED_EDGE('',*,*,#16977,.T.);
#23934=ORIENTED_EDGE('',*,*,#16978,.F.);
#23935=ORIENTED_EDGE('',*,*,#16979,.T.);
#23936=ORIENTED_EDGE('',*,*,#16975,.T.);
#23937=ORIENTED_EDGE('',*,*,#16980,.T.);
#23938=ORIENTED_EDGE('',*,*,#16981,.F.);
#23939=ORIENTED_EDGE('',*,*,#16982,.T.);
#23940=ORIENTED_EDGE('',*,*,#16978,.T.);
#23941=ORIENTED_EDGE('',*,*,#16983,.T.);
#23942=ORIENTED_EDGE('',*,*,#16984,.F.);
#23943=ORIENTED_EDGE('',*,*,#16985,.T.);
#23944=ORIENTED_EDGE('',*,*,#16981,.T.);
#23945=ORIENTED_EDGE('',*,*,#16986,.T.);
#23946=ORIENTED_EDGE('',*,*,#16987,.F.);
#23947=ORIENTED_EDGE('',*,*,#16988,.T.);
#23948=ORIENTED_EDGE('',*,*,#16984,.T.);
#23949=ORIENTED_EDGE('',*,*,#16989,.T.);
#23950=ORIENTED_EDGE('',*,*,#16990,.F.);
#23951=ORIENTED_EDGE('',*,*,#16991,.T.);
#23952=ORIENTED_EDGE('',*,*,#16987,.T.);
#23953=ORIENTED_EDGE('',*,*,#16992,.T.);
#23954=ORIENTED_EDGE('',*,*,#16993,.F.);
#23955=ORIENTED_EDGE('',*,*,#16994,.T.);
#23956=ORIENTED_EDGE('',*,*,#16990,.T.);
#23957=ORIENTED_EDGE('',*,*,#16995,.T.);
#23958=ORIENTED_EDGE('',*,*,#16996,.F.);
#23959=ORIENTED_EDGE('',*,*,#16997,.T.);
#23960=ORIENTED_EDGE('',*,*,#16993,.T.);
#23961=ORIENTED_EDGE('',*,*,#16998,.T.);
#23962=ORIENTED_EDGE('',*,*,#16999,.F.);
#23963=ORIENTED_EDGE('',*,*,#17000,.T.);
#23964=ORIENTED_EDGE('',*,*,#16996,.T.);
#23965=ORIENTED_EDGE('',*,*,#17001,.T.);
#23966=ORIENTED_EDGE('',*,*,#17002,.F.);
#23967=ORIENTED_EDGE('',*,*,#17003,.T.);
#23968=ORIENTED_EDGE('',*,*,#16999,.T.);
#23969=ORIENTED_EDGE('',*,*,#17004,.T.);
#23970=ORIENTED_EDGE('',*,*,#17005,.F.);
#23971=ORIENTED_EDGE('',*,*,#17006,.T.);
#23972=ORIENTED_EDGE('',*,*,#17002,.T.);
#23973=ORIENTED_EDGE('',*,*,#17007,.T.);
#23974=ORIENTED_EDGE('',*,*,#17008,.F.);
#23975=ORIENTED_EDGE('',*,*,#17009,.T.);
#23976=ORIENTED_EDGE('',*,*,#17005,.T.);
#23977=ORIENTED_EDGE('',*,*,#17010,.T.);
#23978=ORIENTED_EDGE('',*,*,#17011,.F.);
#23979=ORIENTED_EDGE('',*,*,#17012,.T.);
#23980=ORIENTED_EDGE('',*,*,#17008,.T.);
#23981=ORIENTED_EDGE('',*,*,#17013,.T.);
#23982=ORIENTED_EDGE('',*,*,#17014,.F.);
#23983=ORIENTED_EDGE('',*,*,#17015,.T.);
#23984=ORIENTED_EDGE('',*,*,#17011,.T.);
#23985=ORIENTED_EDGE('',*,*,#17016,.T.);
#23986=ORIENTED_EDGE('',*,*,#17017,.F.);
#23987=ORIENTED_EDGE('',*,*,#17018,.T.);
#23988=ORIENTED_EDGE('',*,*,#17014,.T.);
#23989=ORIENTED_EDGE('',*,*,#17019,.T.);
#23990=ORIENTED_EDGE('',*,*,#17020,.F.);
#23991=ORIENTED_EDGE('',*,*,#17021,.T.);
#23992=ORIENTED_EDGE('',*,*,#17022,.F.);
#23993=ORIENTED_EDGE('',*,*,#17023,.F.);
#23994=ORIENTED_EDGE('',*,*,#17024,.T.);
#23995=ORIENTED_EDGE('',*,*,#17020,.T.);
#23996=ORIENTED_EDGE('',*,*,#17025,.F.);
#23997=ORIENTED_EDGE('',*,*,#17026,.F.);
#23998=ORIENTED_EDGE('',*,*,#17027,.F.);
#23999=ORIENTED_EDGE('',*,*,#17028,.T.);
#24000=ORIENTED_EDGE('',*,*,#17023,.T.);
#24001=ORIENTED_EDGE('',*,*,#17029,.F.);
#24002=ORIENTED_EDGE('',*,*,#17030,.F.);
#24003=ORIENTED_EDGE('',*,*,#17031,.T.);
#24004=ORIENTED_EDGE('',*,*,#17027,.T.);
#24005=ORIENTED_EDGE('',*,*,#17032,.F.);
#24006=ORIENTED_EDGE('',*,*,#17033,.F.);
#24007=ORIENTED_EDGE('',*,*,#17034,.T.);
#24008=ORIENTED_EDGE('',*,*,#17030,.T.);
#24009=ORIENTED_EDGE('',*,*,#17035,.F.);
#24010=ORIENTED_EDGE('',*,*,#17036,.F.);
#24011=ORIENTED_EDGE('',*,*,#17037,.T.);
#24012=ORIENTED_EDGE('',*,*,#17033,.T.);
#24013=ORIENTED_EDGE('',*,*,#17038,.F.);
#24014=ORIENTED_EDGE('',*,*,#17039,.F.);
#24015=ORIENTED_EDGE('',*,*,#17040,.T.);
#24016=ORIENTED_EDGE('',*,*,#17036,.T.);
#24017=ORIENTED_EDGE('',*,*,#17041,.F.);
#24018=ORIENTED_EDGE('',*,*,#17042,.F.);
#24019=ORIENTED_EDGE('',*,*,#17043,.T.);
#24020=ORIENTED_EDGE('',*,*,#17039,.T.);
#24021=ORIENTED_EDGE('',*,*,#17044,.F.);
#24022=ORIENTED_EDGE('',*,*,#17045,.F.);
#24023=ORIENTED_EDGE('',*,*,#17046,.T.);
#24024=ORIENTED_EDGE('',*,*,#17042,.T.);
#24025=ORIENTED_EDGE('',*,*,#17047,.F.);
#24026=ORIENTED_EDGE('',*,*,#17048,.F.);
#24027=ORIENTED_EDGE('',*,*,#17049,.T.);
#24028=ORIENTED_EDGE('',*,*,#17045,.T.);
#24029=ORIENTED_EDGE('',*,*,#17050,.F.);
#24030=ORIENTED_EDGE('',*,*,#17051,.F.);
#24031=ORIENTED_EDGE('',*,*,#17052,.T.);
#24032=ORIENTED_EDGE('',*,*,#17048,.T.);
#24033=ORIENTED_EDGE('',*,*,#17053,.F.);
#24034=ORIENTED_EDGE('',*,*,#17054,.F.);
#24035=ORIENTED_EDGE('',*,*,#17055,.T.);
#24036=ORIENTED_EDGE('',*,*,#17051,.T.);
#24037=ORIENTED_EDGE('',*,*,#17056,.F.);
#24038=ORIENTED_EDGE('',*,*,#17057,.F.);
#24039=ORIENTED_EDGE('',*,*,#17058,.T.);
#24040=ORIENTED_EDGE('',*,*,#17054,.T.);
#24041=ORIENTED_EDGE('',*,*,#17059,.F.);
#24042=ORIENTED_EDGE('',*,*,#17060,.F.);
#24043=ORIENTED_EDGE('',*,*,#17061,.T.);
#24044=ORIENTED_EDGE('',*,*,#17057,.T.);
#24045=ORIENTED_EDGE('',*,*,#17062,.F.);
#24046=ORIENTED_EDGE('',*,*,#17063,.F.);
#24047=ORIENTED_EDGE('',*,*,#17064,.T.);
#24048=ORIENTED_EDGE('',*,*,#17060,.T.);
#24049=ORIENTED_EDGE('',*,*,#17065,.F.);
#24050=ORIENTED_EDGE('',*,*,#17066,.F.);
#24051=ORIENTED_EDGE('',*,*,#17067,.T.);
#24052=ORIENTED_EDGE('',*,*,#17063,.T.);
#24053=ORIENTED_EDGE('',*,*,#17068,.F.);
#24054=ORIENTED_EDGE('',*,*,#17069,.F.);
#24055=ORIENTED_EDGE('',*,*,#17070,.T.);
#24056=ORIENTED_EDGE('',*,*,#17066,.T.);
#24057=ORIENTED_EDGE('',*,*,#17071,.F.);
#24058=ORIENTED_EDGE('',*,*,#17072,.F.);
#24059=ORIENTED_EDGE('',*,*,#17073,.T.);
#24060=ORIENTED_EDGE('',*,*,#17069,.T.);
#24061=ORIENTED_EDGE('',*,*,#17074,.F.);
#24062=ORIENTED_EDGE('',*,*,#17075,.F.);
#24063=ORIENTED_EDGE('',*,*,#17076,.T.);
#24064=ORIENTED_EDGE('',*,*,#17072,.T.);
#24065=ORIENTED_EDGE('',*,*,#17077,.F.);
#24066=ORIENTED_EDGE('',*,*,#17078,.F.);
#24067=ORIENTED_EDGE('',*,*,#17079,.T.);
#24068=ORIENTED_EDGE('',*,*,#17075,.T.);
#24069=ORIENTED_EDGE('',*,*,#17080,.F.);
#24070=ORIENTED_EDGE('',*,*,#17081,.F.);
#24071=ORIENTED_EDGE('',*,*,#17082,.F.);
#24072=ORIENTED_EDGE('',*,*,#17019,.F.);
#24073=ORIENTED_EDGE('',*,*,#17016,.F.);
#24074=ORIENTED_EDGE('',*,*,#17013,.F.);
#24075=ORIENTED_EDGE('',*,*,#17010,.F.);
#24076=ORIENTED_EDGE('',*,*,#17007,.F.);
#24077=ORIENTED_EDGE('',*,*,#17004,.F.);
#24078=ORIENTED_EDGE('',*,*,#17001,.F.);
#24079=ORIENTED_EDGE('',*,*,#16998,.F.);
#24080=ORIENTED_EDGE('',*,*,#16995,.F.);
#24081=ORIENTED_EDGE('',*,*,#16992,.F.);
#24082=ORIENTED_EDGE('',*,*,#16989,.F.);
#24083=ORIENTED_EDGE('',*,*,#16986,.F.);
#24084=ORIENTED_EDGE('',*,*,#16983,.F.);
#24085=ORIENTED_EDGE('',*,*,#16980,.F.);
#24086=ORIENTED_EDGE('',*,*,#16977,.F.);
#24087=ORIENTED_EDGE('',*,*,#16974,.F.);
#24088=ORIENTED_EDGE('',*,*,#16971,.F.);
#24089=ORIENTED_EDGE('',*,*,#16968,.F.);
#24090=ORIENTED_EDGE('',*,*,#16965,.F.);
#24091=ORIENTED_EDGE('',*,*,#16962,.F.);
#24092=ORIENTED_EDGE('',*,*,#17083,.F.);
#24093=ORIENTED_EDGE('',*,*,#17084,.T.);
#24094=ORIENTED_EDGE('',*,*,#17080,.T.);
#24095=ORIENTED_EDGE('',*,*,#17077,.T.);
#24096=ORIENTED_EDGE('',*,*,#17074,.T.);
#24097=ORIENTED_EDGE('',*,*,#17071,.T.);
#24098=ORIENTED_EDGE('',*,*,#17068,.T.);
#24099=ORIENTED_EDGE('',*,*,#17065,.T.);
#24100=ORIENTED_EDGE('',*,*,#17062,.T.);
#24101=ORIENTED_EDGE('',*,*,#17059,.T.);
#24102=ORIENTED_EDGE('',*,*,#17056,.T.);
#24103=ORIENTED_EDGE('',*,*,#17053,.T.);
#24104=ORIENTED_EDGE('',*,*,#17050,.T.);
#24105=ORIENTED_EDGE('',*,*,#17047,.T.);
#24106=ORIENTED_EDGE('',*,*,#17044,.T.);
#24107=ORIENTED_EDGE('',*,*,#17041,.T.);
#24108=ORIENTED_EDGE('',*,*,#17038,.T.);
#24109=ORIENTED_EDGE('',*,*,#17035,.T.);
#24110=ORIENTED_EDGE('',*,*,#17032,.T.);
#24111=ORIENTED_EDGE('',*,*,#17029,.T.);
#24112=ORIENTED_EDGE('',*,*,#17026,.T.);
#24113=ORIENTED_EDGE('',*,*,#17085,.T.);
#24114=ORIENTED_EDGE('',*,*,#17086,.T.);
#24115=ORIENTED_EDGE('',*,*,#17087,.T.);
#24116=ORIENTED_EDGE('',*,*,#17088,.T.);
#24117=ORIENTED_EDGE('',*,*,#17083,.T.);
#24118=ORIENTED_EDGE('',*,*,#17078,.T.);
#24119=ORIENTED_EDGE('',*,*,#17084,.F.);
#24120=ORIENTED_EDGE('',*,*,#17088,.F.);
#24121=ORIENTED_EDGE('',*,*,#17089,.T.);
#24122=ORIENTED_EDGE('',*,*,#17090,.F.);
#24123=ORIENTED_EDGE('',*,*,#17021,.F.);
#24124=ORIENTED_EDGE('',*,*,#17024,.F.);
#24125=ORIENTED_EDGE('',*,*,#17028,.F.);
#24126=ORIENTED_EDGE('',*,*,#17031,.F.);
#24127=ORIENTED_EDGE('',*,*,#17034,.F.);
#24128=ORIENTED_EDGE('',*,*,#17037,.F.);
#24129=ORIENTED_EDGE('',*,*,#17040,.F.);
#24130=ORIENTED_EDGE('',*,*,#17043,.F.);
#24131=ORIENTED_EDGE('',*,*,#17046,.F.);
#24132=ORIENTED_EDGE('',*,*,#17049,.F.);
#24133=ORIENTED_EDGE('',*,*,#17052,.F.);
#24134=ORIENTED_EDGE('',*,*,#17055,.F.);
#24135=ORIENTED_EDGE('',*,*,#17058,.F.);
#24136=ORIENTED_EDGE('',*,*,#17061,.F.);
#24137=ORIENTED_EDGE('',*,*,#17064,.F.);
#24138=ORIENTED_EDGE('',*,*,#17067,.F.);
#24139=ORIENTED_EDGE('',*,*,#17070,.F.);
#24140=ORIENTED_EDGE('',*,*,#17073,.F.);
#24141=ORIENTED_EDGE('',*,*,#17076,.F.);
#24142=ORIENTED_EDGE('',*,*,#17079,.F.);
#24143=ORIENTED_EDGE('',*,*,#17089,.F.);
#24144=ORIENTED_EDGE('',*,*,#17087,.F.);
#24145=ORIENTED_EDGE('',*,*,#16960,.F.);
#24146=ORIENTED_EDGE('',*,*,#16964,.F.);
#24147=ORIENTED_EDGE('',*,*,#16967,.F.);
#24148=ORIENTED_EDGE('',*,*,#16970,.F.);
#24149=ORIENTED_EDGE('',*,*,#16973,.F.);
#24150=ORIENTED_EDGE('',*,*,#16976,.F.);
#24151=ORIENTED_EDGE('',*,*,#16979,.F.);
#24152=ORIENTED_EDGE('',*,*,#16982,.F.);
#24153=ORIENTED_EDGE('',*,*,#16985,.F.);
#24154=ORIENTED_EDGE('',*,*,#16988,.F.);
#24155=ORIENTED_EDGE('',*,*,#16991,.F.);
#24156=ORIENTED_EDGE('',*,*,#16994,.F.);
#24157=ORIENTED_EDGE('',*,*,#16997,.F.);
#24158=ORIENTED_EDGE('',*,*,#17000,.F.);
#24159=ORIENTED_EDGE('',*,*,#17003,.F.);
#24160=ORIENTED_EDGE('',*,*,#17006,.F.);
#24161=ORIENTED_EDGE('',*,*,#17009,.F.);
#24162=ORIENTED_EDGE('',*,*,#17012,.F.);
#24163=ORIENTED_EDGE('',*,*,#17015,.F.);
#24164=ORIENTED_EDGE('',*,*,#17018,.F.);
#24165=ORIENTED_EDGE('',*,*,#17091,.F.);
#24166=ORIENTED_EDGE('',*,*,#17092,.F.);
#24167=ORIENTED_EDGE('',*,*,#17093,.F.);
#24168=ORIENTED_EDGE('',*,*,#17094,.F.);
#24169=ORIENTED_EDGE('',*,*,#17095,.F.);
#24170=ORIENTED_EDGE('',*,*,#17096,.F.);
#24171=ORIENTED_EDGE('',*,*,#17097,.T.);
#24172=ORIENTED_EDGE('',*,*,#17098,.F.);
#24173=ORIENTED_EDGE('',*,*,#17097,.F.);
#24174=ORIENTED_EDGE('',*,*,#17099,.F.);
#24175=ORIENTED_EDGE('',*,*,#17100,.F.);
#24176=ORIENTED_EDGE('',*,*,#17095,.T.);
#24177=ORIENTED_EDGE('',*,*,#17101,.F.);
#24178=ORIENTED_EDGE('',*,*,#17102,.T.);
#24179=ORIENTED_EDGE('',*,*,#17103,.T.);
#24180=ORIENTED_EDGE('',*,*,#17094,.T.);
#24181=ORIENTED_EDGE('',*,*,#17104,.F.);
#24182=ORIENTED_EDGE('',*,*,#17105,.T.);
#24183=ORIENTED_EDGE('',*,*,#17101,.T.);
#24184=ORIENTED_EDGE('',*,*,#17093,.T.);
#24185=ORIENTED_EDGE('',*,*,#17106,.F.);
#24186=ORIENTED_EDGE('',*,*,#17107,.T.);
#24187=ORIENTED_EDGE('',*,*,#17104,.T.);
#24188=ORIENTED_EDGE('',*,*,#17107,.F.);
#24189=ORIENTED_EDGE('',*,*,#17108,.F.);
#24190=ORIENTED_EDGE('',*,*,#17109,.F.);
#24191=ORIENTED_EDGE('',*,*,#17110,.F.);
#24192=ORIENTED_EDGE('',*,*,#17102,.F.);
#24193=ORIENTED_EDGE('',*,*,#17105,.F.);
#24194=ORIENTED_EDGE('',*,*,#17111,.T.);
#24195=ORIENTED_EDGE('',*,*,#17081,.T.);
#24196=ORIENTED_EDGE('',*,*,#17025,.T.);
#24197=ORIENTED_EDGE('',*,*,#17022,.T.);
#24198=ORIENTED_EDGE('',*,*,#17090,.T.);
#24199=ORIENTED_EDGE('',*,*,#17092,.T.);
#24200=ORIENTED_EDGE('',*,*,#17112,.F.);
#24201=ORIENTED_EDGE('',*,*,#17108,.T.);
#24202=ORIENTED_EDGE('',*,*,#17106,.T.);
#24203=ORIENTED_EDGE('',*,*,#17100,.T.);
#24204=ORIENTED_EDGE('',*,*,#17113,.F.);
#24205=ORIENTED_EDGE('',*,*,#17109,.T.);
#24206=ORIENTED_EDGE('',*,*,#17112,.T.);
#24207=ORIENTED_EDGE('',*,*,#17099,.T.);
#24208=ORIENTED_EDGE('',*,*,#17096,.T.);
#24209=ORIENTED_EDGE('',*,*,#17103,.F.);
#24210=ORIENTED_EDGE('',*,*,#17110,.T.);
#24211=ORIENTED_EDGE('',*,*,#17113,.T.);
#24212=ORIENTED_EDGE('',*,*,#17098,.T.);
#24213=ORIENTED_EDGE('',*,*,#17114,.F.);
#24214=ORIENTED_EDGE('',*,*,#17085,.F.);
#24215=ORIENTED_EDGE('',*,*,#16961,.F.);
#24216=ORIENTED_EDGE('',*,*,#17086,.F.);
#24217=ORIENTED_EDGE('',*,*,#17115,.T.);
#24218=ORIENTED_EDGE('',*,*,#17114,.T.);
#24219=ORIENTED_EDGE('',*,*,#17115,.F.);
#24220=ORIENTED_EDGE('',*,*,#17017,.T.);
#24221=ORIENTED_EDGE('',*,*,#17082,.T.);
#24222=ORIENTED_EDGE('',*,*,#17111,.F.);
#24223=ORIENTED_EDGE('',*,*,#17091,.T.);
#26880=ADVANCED_FACE('',(#8056),#6714,.T.);
#26881=ADVANCED_FACE('',(#8057),#6715,.T.);
#26882=ADVANCED_FACE('',(#8058),#6716,.T.);
#26883=ADVANCED_FACE('',(#8059),#6717,.T.);
#26884=ADVANCED_FACE('',(#8060),#6718,.T.);
#26885=ADVANCED_FACE('',(#8061),#6719,.T.);
#26886=ADVANCED_FACE('',(#8062),#6720,.T.);
#26887=ADVANCED_FACE('',(#8063),#6721,.T.);
#26888=ADVANCED_FACE('',(#8064),#6722,.T.);
#26889=ADVANCED_FACE('',(#8065),#6723,.T.);
#26890=ADVANCED_FACE('',(#8066),#6724,.T.);
#26891=ADVANCED_FACE('',(#8067),#6725,.T.);
#26892=ADVANCED_FACE('',(#8068),#6726,.T.);
#26893=ADVANCED_FACE('',(#8069),#6727,.T.);
#26894=ADVANCED_FACE('',(#8070),#6728,.T.);
#26895=ADVANCED_FACE('',(#8071),#6729,.T.);
#26896=ADVANCED_FACE('',(#8072),#6730,.T.);
#26897=ADVANCED_FACE('',(#8073),#6731,.T.);
#26898=ADVANCED_FACE('',(#8074),#6732,.T.);
#26899=ADVANCED_FACE('',(#8075),#6733,.T.);
#26900=ADVANCED_FACE('',(#8076),#6734,.T.);
#26901=ADVANCED_FACE('',(#8077),#6735,.T.);
#26902=ADVANCED_FACE('',(#8078),#6736,.T.);
#26903=ADVANCED_FACE('',(#8079),#6737,.T.);
#26904=ADVANCED_FACE('',(#8080),#6738,.T.);
#26905=ADVANCED_FACE('',(#8081),#6739,.T.);
#26906=ADVANCED_FACE('',(#8082),#6740,.T.);
#26907=ADVANCED_FACE('',(#8083),#6741,.T.);
#26908=ADVANCED_FACE('',(#8084),#6742,.T.);
#26909=ADVANCED_FACE('',(#8085),#6743,.T.);
#26910=ADVANCED_FACE('',(#8086),#6744,.T.);
#26911=ADVANCED_FACE('',(#8087),#6745,.T.);
#26912=ADVANCED_FACE('',(#8088),#6746,.T.);
#26913=ADVANCED_FACE('',(#8089),#6747,.T.);
#26914=ADVANCED_FACE('',(#8090),#6748,.T.);
#26915=ADVANCED_FACE('',(#8091),#6749,.T.);
#26916=ADVANCED_FACE('',(#8092),#6750,.T.);
#26917=ADVANCED_FACE('',(#8093),#6751,.T.);
#26918=ADVANCED_FACE('',(#8094),#6752,.T.);
#26919=ADVANCED_FACE('',(#8095),#6753,.T.);
#26920=ADVANCED_FACE('',(#8096),#578,.F.);
#26921=ADVANCED_FACE('',(#8097),#1543,.T.);
#26922=ADVANCED_FACE('',(#8098),#6754,.T.);
#26923=ADVANCED_FACE('',(#8099),#579,.F.);
#26924=ADVANCED_FACE('',(#8100),#406,.T.);
#26925=ADVANCED_FACE('',(#8101),#1544,.T.);
#26926=ADVANCED_FACE('',(#8102),#1545,.T.);
#26927=ADVANCED_FACE('',(#8103),#1546,.T.);
#26928=ADVANCED_FACE('',(#8104,#716),#1547,.F.);
#26929=ADVANCED_FACE('',(#8105),#1548,.T.);
#26930=ADVANCED_FACE('',(#8106),#1549,.T.);
#26931=ADVANCED_FACE('',(#8107),#1550,.T.);
#26932=ADVANCED_FACE('',(#8108),#1551,.T.);
#26933=ADVANCED_FACE('',(#8109),#1552,.T.);
#26934=ADVANCED_FACE('',(#8110),#407,.T.);
#26935=ADVANCED_FACE('',(#8111),#6755,.T.);
#27237=CLOSED_SHELL('',(#26880,#26881,#26882,#26883,#26884,#26885,#26886,
#26887,#26888,#26889,#26890,#26891,#26892,#26893,#26894,#26895,#26896,#26897,
#26898,#26899,#26900,#26901,#26902,#26903,#26904,#26905,#26906,#26907,#26908,
#26909,#26910,#26911,#26912,#26913,#26914,#26915,#26916,#26917,#26918,#26919,
#26920,#26921,#26922,#26923,#26924,#26925,#26926,#26927,#26928,#26929,#26930,
#26931,#26932,#26933,#26934,#26935));
#29496=AXIS2_PLACEMENT_3D('',#46700,#35923,#35924);
#29497=AXIS2_PLACEMENT_3D('',#46701,#35925,#35926);
#29498=AXIS2_PLACEMENT_3D('',#46717,#35928,#35929);
#29499=AXIS2_PLACEMENT_3D('',#46728,#35930,#35931);
#29500=AXIS2_PLACEMENT_3D('',#46776,#35933,#35934);
#29501=AXIS2_PLACEMENT_3D('',#46824,#35936,#35937);
#29502=AXIS2_PLACEMENT_3D('',#46872,#35939,#35940);
#29503=AXIS2_PLACEMENT_3D('',#46926,#35942,#35943);
#29504=AXIS2_PLACEMENT_3D('',#46974,#35945,#35946);
#29505=AXIS2_PLACEMENT_3D('',#47022,#35948,#35949);
#29506=AXIS2_PLACEMENT_3D('',#47076,#35951,#35952);
#29507=AXIS2_PLACEMENT_3D('',#47124,#35954,#35955);
#29508=AXIS2_PLACEMENT_3D('',#47172,#35957,#35958);
#29509=AXIS2_PLACEMENT_3D('',#47220,#35960,#35961);
#29510=AXIS2_PLACEMENT_3D('',#47274,#35963,#35964);
#29511=AXIS2_PLACEMENT_3D('',#47322,#35966,#35967);
#29512=AXIS2_PLACEMENT_3D('',#47370,#35969,#35970);
#29513=AXIS2_PLACEMENT_3D('',#47424,#35972,#35973);
#29514=AXIS2_PLACEMENT_3D('',#47472,#35975,#35976);
#29515=AXIS2_PLACEMENT_3D('',#47520,#35978,#35979);
#29516=AXIS2_PLACEMENT_3D('',#47568,#35981,#35982);
#29517=AXIS2_PLACEMENT_3D('',#47622,#35984,#35985);
#29518=AXIS2_PLACEMENT_3D('',#47670,#35987,#35988);
#29519=AXIS2_PLACEMENT_3D('',#47679,#35990,#35991);
#29520=AXIS2_PLACEMENT_3D('',#47680,#35992,#35993);
#29521=AXIS2_PLACEMENT_3D('',#47695,#35995,#35996);
#29522=AXIS2_PLACEMENT_3D('',#47706,#35997,#35998);
#29523=AXIS2_PLACEMENT_3D('',#47731,#36000,#36001);
#29524=AXIS2_PLACEMENT_3D('',#47756,#36003,#36004);
#29525=AXIS2_PLACEMENT_3D('',#47780,#36006,#36007);
#29526=AXIS2_PLACEMENT_3D('',#47804,#36009,#36010);
#29527=AXIS2_PLACEMENT_3D('',#47829,#36012,#36013);
#29528=AXIS2_PLACEMENT_3D('',#47854,#36015,#36016);
#29529=AXIS2_PLACEMENT_3D('',#47878,#36018,#36019);
#29530=AXIS2_PLACEMENT_3D('',#47903,#36021,#36022);
#29531=AXIS2_PLACEMENT_3D('',#47928,#36024,#36025);
#29532=AXIS2_PLACEMENT_3D('',#47952,#36027,#36028);
#29533=AXIS2_PLACEMENT_3D('',#47976,#36030,#36031);
#29534=AXIS2_PLACEMENT_3D('',#48001,#36033,#36034);
#29535=AXIS2_PLACEMENT_3D('',#48026,#36036,#36037);
#29536=AXIS2_PLACEMENT_3D('',#48050,#36039,#36040);
#29537=AXIS2_PLACEMENT_3D('',#48075,#36042,#36043);
#29538=AXIS2_PLACEMENT_3D('',#48100,#36045,#36046);
#29539=AXIS2_PLACEMENT_3D('',#48124,#36048,#36049);
#29540=AXIS2_PLACEMENT_3D('',#48902,#36051,#36052);
#29541=AXIS2_PLACEMENT_3D('',#48904,#36053,#36054);
#29542=AXIS2_PLACEMENT_3D('',#48905,#36055,#36056);
#29543=AXIS2_PLACEMENT_3D('',#49010,#36057,#36058);
#29544=AXIS2_PLACEMENT_3D('',#49011,#36059,#36060);
#29545=AXIS2_PLACEMENT_3D('',#49662,#36061,#36062);
#29546=AXIS2_PLACEMENT_3D('',#49686,#36064,#36065);
#29547=AXIS2_PLACEMENT_3D('',#49694,#36066,#36067);
#29548=AXIS2_PLACEMENT_3D('',#49700,#36071,#36072);
#29549=AXIS2_PLACEMENT_3D('',#49704,#36075,#36076);
#29550=AXIS2_PLACEMENT_3D('',#49708,#36079,#36080);
#29551=AXIS2_PLACEMENT_3D('',#49714,#36084,#36085);
#29552=AXIS2_PLACEMENT_3D('',#49715,#36086,#36087);
#29553=AXIS2_PLACEMENT_3D('',#49717,#36089,#36090);
#29554=AXIS2_PLACEMENT_3D('',#49719,#36092,#36093);
#29555=AXIS2_PLACEMENT_3D('',#49720,#36094,#36095);
#29556=AXIS2_PLACEMENT_3D('',#49721,#36096,#36097);
#29557=AXIS2_PLACEMENT_3D('',#49723,#36098,#36099);
#29558=AXIS2_PLACEMENT_3D('',#49724,#36100,#36101);
#29559=AXIS2_PLACEMENT_3D('',#49726,#36103,#36104);
#35923=DIRECTION('axis',(0.,0.,1.));
#35924=DIRECTION('refdir',(1.,0.,0.));
#35925=DIRECTION('center_axis',(1.,0.,0.));
#35926=DIRECTION('ref_axis',(0.,1.,0.));
#35927=DIRECTION('',(-1.,0.,0.));
#35928=DIRECTION('center_axis',(1.,0.,0.));
#35929=DIRECTION('ref_axis',(0.,1.,0.));
#35930=DIRECTION('center_axis',(1.,0.,0.));
#35931=DIRECTION('ref_axis',(0.,1.,0.));
#35932=DIRECTION('',(-1.,0.,0.));
#35933=DIRECTION('center_axis',(1.,0.,0.));
#35934=DIRECTION('ref_axis',(0.,1.,0.));
#35935=DIRECTION('',(-1.,0.,0.));
#35936=DIRECTION('center_axis',(1.,0.,0.));
#35937=DIRECTION('ref_axis',(0.,1.,0.));
#35938=DIRECTION('',(-1.,0.,0.));
#35939=DIRECTION('center_axis',(1.,0.,0.));
#35940=DIRECTION('ref_axis',(0.,1.,0.));
#35941=DIRECTION('',(-1.,0.,0.));
#35942=DIRECTION('center_axis',(1.,0.,0.));
#35943=DIRECTION('ref_axis',(0.,1.,0.));
#35944=DIRECTION('',(-1.,0.,0.));
#35945=DIRECTION('center_axis',(1.,0.,0.));
#35946=DIRECTION('ref_axis',(0.,1.,0.));
#35947=DIRECTION('',(-1.,0.,0.));
#35948=DIRECTION('center_axis',(1.,0.,0.));
#35949=DIRECTION('ref_axis',(0.,1.,0.));
#35950=DIRECTION('',(-1.,0.,0.));
#35951=DIRECTION('center_axis',(1.,0.,0.));
#35952=DIRECTION('ref_axis',(0.,1.,0.));
#35953=DIRECTION('',(-1.,0.,0.));
#35954=DIRECTION('center_axis',(1.,0.,0.));
#35955=DIRECTION('ref_axis',(0.,1.,0.));
#35956=DIRECTION('',(-1.,0.,0.));
#35957=DIRECTION('center_axis',(1.,0.,0.));
#35958=DIRECTION('ref_axis',(0.,1.,0.));
#35959=DIRECTION('',(-1.,0.,0.));
#35960=DIRECTION('center_axis',(1.,0.,0.));
#35961=DIRECTION('ref_axis',(0.,1.,0.));
#35962=DIRECTION('',(-1.,0.,0.));
#35963=DIRECTION('center_axis',(1.,0.,0.));
#35964=DIRECTION('ref_axis',(0.,1.,0.));
#35965=DIRECTION('',(-1.,0.,0.));
#35966=DIRECTION('center_axis',(1.,0.,0.));
#35967=DIRECTION('ref_axis',(0.,1.,0.));
#35968=DIRECTION('',(-1.,0.,0.));
#35969=DIRECTION('center_axis',(1.,0.,0.));
#35970=DIRECTION('ref_axis',(0.,1.,0.));
#35971=DIRECTION('',(-1.,0.,0.));
#35972=DIRECTION('center_axis',(1.,0.,0.));
#35973=DIRECTION('ref_axis',(0.,1.,0.));
#35974=DIRECTION('',(-1.,0.,0.));
#35975=DIRECTION('center_axis',(1.,0.,0.));
#35976=DIRECTION('ref_axis',(0.,1.,0.));
#35977=DIRECTION('',(-1.,0.,0.));
#35978=DIRECTION('center_axis',(1.,0.,0.));
#35979=DIRECTION('ref_axis',(0.,1.,0.));
#35980=DIRECTION('',(-1.,0.,0.));
#35981=DIRECTION('center_axis',(1.,0.,0.));
#35982=DIRECTION('ref_axis',(0.,1.,0.));
#35983=DIRECTION('',(-1.,0.,0.));
#35984=DIRECTION('center_axis',(1.,0.,0.));
#35985=DIRECTION('ref_axis',(0.,1.,0.));
#35986=DIRECTION('',(-1.,0.,0.));
#35987=DIRECTION('center_axis',(1.,0.,0.));
#35988=DIRECTION('ref_axis',(0.,1.,1.18505573263654E-13));
#35989=DIRECTION('',(1.,0.,0.));
#35990=DIRECTION('center_axis',(1.,0.,0.));
#35991=DIRECTION('ref_axis',(0.,1.,1.18505573263654E-13));
#35992=DIRECTION('center_axis',(1.,0.,0.));
#35993=DIRECTION('ref_axis',(0.,1.,1.18505573263654E-13));
#35994=DIRECTION('',(1.,0.,0.));
#35995=DIRECTION('center_axis',(1.,0.,0.));
#35996=DIRECTION('ref_axis',(0.,1.,1.18505573263654E-13));
#35997=DIRECTION('center_axis',(1.,0.,0.));
#35998=DIRECTION('ref_axis',(0.,1.,1.18505573263654E-13));
#35999=DIRECTION('',(1.,0.,0.));
#36000=DIRECTION('center_axis',(1.,0.,0.));
#36001=DIRECTION('ref_axis',(0.,1.,1.18505573263654E-13));
#36002=DIRECTION('',(1.,0.,0.));
#36003=DIRECTION('center_axis',(1.,0.,0.));
#36004=DIRECTION('ref_axis',(0.,1.,1.18505573263654E-13));
#36005=DIRECTION('',(1.,0.,0.));
#36006=DIRECTION('center_axis',(1.,0.,0.));
#36007=DIRECTION('ref_axis',(0.,1.,1.18505573263654E-13));
#36008=DIRECTION('',(1.,0.,0.));
#36009=DIRECTION('center_axis',(1.,0.,0.));
#36010=DIRECTION('ref_axis',(0.,1.,1.18505573263654E-13));
#36011=DIRECTION('',(1.,0.,0.));
#36012=DIRECTION('center_axis',(1.,0.,0.));
#36013=DIRECTION('ref_axis',(0.,1.,1.18505573263654E-13));
#36014=DIRECTION('',(1.,0.,0.));
#36015=DIRECTION('center_axis',(1.,0.,0.));
#36016=DIRECTION('ref_axis',(0.,1.,1.18505573263654E-13));
#36017=DIRECTION('',(1.,0.,0.));
#36018=DIRECTION('center_axis',(1.,0.,0.));
#36019=DIRECTION('ref_axis',(0.,1.,1.18505573263654E-13));
#36020=DIRECTION('',(1.,0.,0.));
#36021=DIRECTION('center_axis',(1.,0.,0.));
#36022=DIRECTION('ref_axis',(0.,1.,1.18505573263654E-13));
#36023=DIRECTION('',(1.,0.,0.));
#36024=DIRECTION('center_axis',(1.,0.,0.));
#36025=DIRECTION('ref_axis',(0.,1.,1.18505573263654E-13));
#36026=DIRECTION('',(1.,0.,0.));
#36027=DIRECTION('center_axis',(1.,0.,0.));
#36028=DIRECTION('ref_axis',(0.,1.,1.18505573263654E-13));
#36029=DIRECTION('',(1.,0.,0.));
#36030=DIRECTION('center_axis',(1.,0.,0.));
#36031=DIRECTION('ref_axis',(0.,1.,1.18505573263654E-13));
#36032=DIRECTION('',(1.,0.,0.));
#36033=DIRECTION('center_axis',(1.,0.,0.));
#36034=DIRECTION('ref_axis',(0.,1.,1.18505573263654E-13));
#36035=DIRECTION('',(1.,0.,0.));
#36036=DIRECTION('center_axis',(1.,0.,0.));
#36037=DIRECTION('ref_axis',(0.,1.,1.18505573263654E-13));
#36038=DIRECTION('',(1.,0.,0.));
#36039=DIRECTION('center_axis',(1.,0.,0.));
#36040=DIRECTION('ref_axis',(0.,1.,1.18505573263654E-13));
#36041=DIRECTION('',(1.,0.,0.));
#36042=DIRECTION('center_axis',(1.,0.,0.));
#36043=DIRECTION('ref_axis',(0.,1.,1.18505573263654E-13));
#36044=DIRECTION('',(1.,0.,0.));
#36045=DIRECTION('center_axis',(1.,0.,0.));
#36046=DIRECTION('ref_axis',(0.,1.,1.18505573263654E-13));
#36047=DIRECTION('',(1.,0.,0.));
#36048=DIRECTION('center_axis',(1.,0.,0.));
#36049=DIRECTION('ref_axis',(0.,1.,1.18505573263654E-13));
#36050=DIRECTION('',(1.,0.,0.));
#36051=DIRECTION('center_axis',(1.,0.,0.));
#36052=DIRECTION('ref_axis',(0.,0.,-1.));
#36053=DIRECTION('center_axis',(1.,0.,0.));
#36054=DIRECTION('ref_axis',(0.,1.,0.));
#36055=DIRECTION('center_axis',(1.,0.,0.));
#36056=DIRECTION('ref_axis',(0.,1.,0.));
#36057=DIRECTION('center_axis',(-1.,0.,0.));
#36058=DIRECTION('ref_axis',(0.,1.,1.18505573263654E-13));
#36059=DIRECTION('center_axis',(1.,0.,0.));
#36060=DIRECTION('ref_axis',(0.,1.,1.18505573263654E-13));
#36061=DIRECTION('center_axis',(-1.,0.,0.));
#36062=DIRECTION('ref_axis',(0.,1.,0.));
#36063=DIRECTION('',(0.500438231481872,0.865772242839476,1.06026520598399E-16));
#36064=DIRECTION('center_axis',(1.,0.,0.));
#36065=DIRECTION('ref_axis',(0.,1.,0.));
#36066=DIRECTION('center_axis',(0.,-0.5,0.866025403784439));
#36067=DIRECTION('ref_axis',(0.,-0.866025403784439,-0.5));
#36068=DIRECTION('',(1.,0.,0.));
#36069=DIRECTION('',(0.,-0.866025403784439,-0.5));
#36070=DIRECTION('',(1.,0.,0.));
#36071=DIRECTION('center_axis',(0.,0.5,0.866025403784439));
#36072=DIRECTION('ref_axis',(0.,-0.866025403784439,0.5));
#36073=DIRECTION('',(1.,0.,0.));
#36074=DIRECTION('',(0.,-0.866025403784439,0.5));
#36075=DIRECTION('center_axis',(0.,1.,-3.60555503696918E-16));
#36076=DIRECTION('ref_axis',(0.,3.60555503696918E-16,1.));
#36077=DIRECTION('',(1.,0.,0.));
#36078=DIRECTION('',(0.,3.60555503696918E-16,1.));
#36079=DIRECTION('center_axis',(1.,0.,0.));
#36080=DIRECTION('ref_axis',(0.,0.,-1.));
#36081=DIRECTION('',(0.,0.866025403784439,0.5));
#36082=DIRECTION('',(0.,0.866025403784439,-0.5));
#36083=DIRECTION('',(0.,1.20185167898973E-16,-1.));
#36084=DIRECTION('center_axis',(-1.,0.,0.));
#36085=DIRECTION('ref_axis',(0.,1.,0.));
#36086=DIRECTION('center_axis',(0.,0.5,-0.866025403784439));
#36087=DIRECTION('ref_axis',(0.,0.866025403784439,0.5));
#36088=DIRECTION('',(1.,0.,0.));
#36089=DIRECTION('center_axis',(0.,-0.5,-0.866025403784439));
#36090=DIRECTION('ref_axis',(0.,0.866025403784439,-0.5));
#36091=DIRECTION('',(1.,0.,0.));
#36092=DIRECTION('center_axis',(0.,-1.,-1.20185167898973E-16));
#36093=DIRECTION('ref_axis',(0.,1.20185167898973E-16,-1.));
#36094=DIRECTION('center_axis',(1.,0.,0.));
#36095=DIRECTION('ref_axis',(0.,0.,-1.));
#36096=DIRECTION('center_axis',(-1.,0.,0.));
#36097=DIRECTION('ref_axis',(0.,0.,1.));
#36098=DIRECTION('center_axis',(1.,0.,0.));
#36099=DIRECTION('ref_axis',(0.,0.,-1.));
#36100=DIRECTION('center_axis',(1.,0.,0.));
#36101=DIRECTION('ref_axis',(0.,1.,0.));
#36102=DIRECTION('',(-0.707106781186546,0.707106781186549,8.65956056235495E-17));
#36103=DIRECTION('center_axis',(1.,0.,0.));
#36104=DIRECTION('ref_axis',(0.,1.,0.));
#46700=CARTESIAN_POINT('',(0.,0.,0.));
#46701=CARTESIAN_POINT('Origin',(-14.75,0.,0.));
#46702=CARTESIAN_POINT('',(-29.0911584740964,-4.93085069296601,0.00239406595250471));
#46703=CARTESIAN_POINT('',(-29.3088415259036,-4.92746336814012,0.00144215323830204));
#46704=CARTESIAN_POINT('',(-14.75,-4.925,-6.03138548580071E-16));
#46705=CARTESIAN_POINT('',(-29.575,2.17167188636589,4.42425492889053));
#46706=CARTESIAN_POINT('Ctrl Pts',(-29.0911584740964,-4.93085069296601,
0.00239406595250471));
#46707=CARTESIAN_POINT('Ctrl Pts',(-29.0987040309128,-4.93188800524103,
0.15750466532186));
#46708=CARTESIAN_POINT('Ctrl Pts',(-29.1062495877292,-4.92523207312776,
0.312531807375031));
#46709=CARTESIAN_POINT('Ctrl Pts',(-29.1137951445456,-4.91059689710246,
0.466805765893802));
#46710=CARTESIAN_POINT('Ctrl Pts',(-29.1933410329187,-4.75631165258633,
2.09317468495417));
#46711=CARTESIAN_POINT('Ctrl Pts',(-29.2728869212918,-3.71524898717827,
3.63583816030893));
#46712=CARTESIAN_POINT('Ctrl Pts',(-29.3524328096649,-2.26290809811278,
4.38440317990658));
#46713=CARTESIAN_POINT('Ctrl Pts',(-29.4266218731099,-0.908371583825934,
5.08255790377123));
#46714=CARTESIAN_POINT('Ctrl Pts',(-29.5008109365549,0.803915241080997,
5.08996618673832));
#46715=CARTESIAN_POINT('Ctrl Pts',(-29.575,2.17494790042119,4.42655504786424));
#46716=CARTESIAN_POINT('',(-29.575,-2.1683958723106,4.4219548099168));
#46717=CARTESIAN_POINT('Origin',(-29.575,0.,0.));
#46718=CARTESIAN_POINT('Ctrl Pts',(-29.575,-2.16839587231058,4.42195480991681));
#46719=CARTESIAN_POINT('Ctrl Pts',(-29.5352270558135,-2.90509583874374,
4.0606989321402));
#46720=CARTESIAN_POINT('Ctrl Pts',(-29.4954541116269,-3.54417075123437,
3.51185369356184));
#46721=CARTESIAN_POINT('Ctrl Pts',(-29.4556811674404,-4.01940836209596,
2.8419582808667));
#46722=CARTESIAN_POINT('Ctrl Pts',(-29.4159082232539,-4.49464597295758,
2.17206286817154));
#46723=CARTESIAN_POINT('Ctrl Pts',(-29.3761352790673,-4.80604628219013,
1.38111728135961));
#46724=CARTESIAN_POINT('Ctrl Pts',(-29.3363623348808,-4.89820932110733,
0.567147712221922));
#46725=CARTESIAN_POINT('Ctrl Pts',(-29.3271887318884,-4.91946666443181,
0.379406175157601));
#46726=CARTESIAN_POINT('Ctrl Pts',(-29.318015128896,-4.929060779183,0.190439782628943));
#46727=CARTESIAN_POINT('Ctrl Pts',(-29.3088415259036,-4.92746336814012,
0.00144215323830204));
#46728=CARTESIAN_POINT('Origin',(-14.75,0.,0.));
#46729=CARTESIAN_POINT('',(-27.5911584740964,-4.91871916148224,0.00298870709768639));
#46730=CARTESIAN_POINT('',(-27.8088415259036,-4.91810465358294,0.00250400581179228));
#46731=CARTESIAN_POINT('',(-14.75,-4.925,-6.03138548580071E-16));
#46732=CARTESIAN_POINT('Ctrl Pts',(-27.5911584740964,-4.91871916148224,
0.00298870709768639));
#46733=CARTESIAN_POINT('Ctrl Pts',(-27.6214287006744,-4.92217786568793,
0.629288456904983));
#46734=CARTESIAN_POINT('Ctrl Pts',(-27.6516989272523,-4.81132058056506,
1.2544097760338));
#46735=CARTESIAN_POINT('Ctrl Pts',(-27.6819691538303,-4.58053680634953,
1.83157791678433));
#46736=CARTESIAN_POINT('Ctrl Pts',(-27.7615150422034,-3.97406958038444,
3.34829442957306));
#46737=CARTESIAN_POINT('Ctrl Pts',(-27.8410609305764,-2.53943282222183,
4.53386340685575));
#46738=CARTESIAN_POINT('Ctrl Pts',(-27.9206068189495,-0.935593024822473,
4.84364324705812));
#46739=CARTESIAN_POINT('Ctrl Pts',(-28.0001527073226,0.668246772576907,
5.1534230872605));
#46740=CARTESIAN_POINT('Ctrl Pts',(-28.0796985956957,2.44128960921305,4.58741379038254));
#46741=CARTESIAN_POINT('Ctrl Pts',(-28.1592444840688,3.56896084480546,3.40568511210877));
#46742=CARTESIAN_POINT('Ctrl Pts',(-28.2387903724418,4.69663208039786,2.22395643383501));
#46743=CARTESIAN_POINT('Ctrl Pts',(-28.3183362608148,5.17893171494654,0.426508374165463));
#46744=CARTESIAN_POINT('Ctrl Pts',(-28.3978821491879,4.79450650284291,-1.16110247139908));
#46745=CARTESIAN_POINT('Ctrl Pts',(-28.477428037561,4.41008129073928,-2.74871331696362));
#46746=CARTESIAN_POINT('Ctrl Pts',(-28.5569739259341,3.15893123198334,-4.12648694842314));
#46747=CARTESIAN_POINT('Ctrl Pts',(-28.6365198143072,1.61540970892298,-4.66128231395555));
#46748=CARTESIAN_POINT('Ctrl Pts',(-28.7160657026803,0.0718881858626222,
-5.19607767948796));
#46749=CARTESIAN_POINT('Ctrl Pts',(-28.7956115910533,-1.76400480150215,
-4.88789477909325));
#46750=CARTESIAN_POINT('Ctrl Pts',(-28.8751574794264,-3.04819738337245,
-3.87876614751291));
#46751=CARTESIAN_POINT('Ctrl Pts',(-28.9471578109831,-4.21057413933529,
-2.96536135006638));
#46752=CARTESIAN_POINT('Ctrl Pts',(-29.0191581425397,-4.92095257284757,
-1.4776841912631));
#46753=CARTESIAN_POINT('Ctrl Pts',(-29.0911584740964,-4.93085069296601,
0.00239406595250471));
#46754=CARTESIAN_POINT('Ctrl Pts',(-29.3088415259036,-4.92746336814012,
0.00144215323830204));
#46755=CARTESIAN_POINT('Ctrl Pts',(-29.2384692405229,-4.91520935345547,
-1.44839114811431));
#46756=CARTESIAN_POINT('Ctrl Pts',(-29.1680969551423,-4.24436898433528,
-2.90006264127696));
#46757=CARTESIAN_POINT('Ctrl Pts',(-29.0977246697616,-3.12788046011008,
-3.81474362504512));
#46758=CARTESIAN_POINT('Ctrl Pts',(-29.0181787813885,-1.86584852470544,
-4.8486607564584));
#46759=CARTESIAN_POINT('Ctrl Pts',(-28.9386328930154,-0.0344076573231608,
-5.19645995170656));
#46760=CARTESIAN_POINT('Ctrl Pts',(-28.8590870046423,1.52027960945058,-4.69387792027941));
#46761=CARTESIAN_POINT('Ctrl Pts',(-28.7795411162692,3.07496687622432,-4.19129588885225));
#46762=CARTESIAN_POINT('Ctrl Pts',(-28.6999952278962,4.35290054238952,-2.83833263074978));
#46763=CARTESIAN_POINT('Ctrl Pts',(-28.6204493395231,4.76944898889192,-1.25865959225591));
#46764=CARTESIAN_POINT('Ctrl Pts',(-28.54090345115,5.18599743539432,0.321013446237961));
#46765=CARTESIAN_POINT('Ctrl Pts',(-28.4613575627769,4.74116066223391,2.12739626512323));
#46766=CARTESIAN_POINT('Ctrl Pts',(-28.3818116744039,3.63804206657526,3.33181334358779));
#46767=CARTESIAN_POINT('Ctrl Pts',(-28.3022657860308,2.53492347091661,4.53623042205235));
#46768=CARTESIAN_POINT('Ctrl Pts',(-28.2227198976577,0.773523052759708,
5.13868176009622));
#46769=CARTESIAN_POINT('Ctrl Pts',(-28.1431740092847,-0.836391940911384,
4.8618460820682));
#46770=CARTESIAN_POINT('Ctrl Pts',(-28.0636281209116,-2.44630693458247,
4.58501040404019));
#46771=CARTESIAN_POINT('Ctrl Pts',(-27.9840822325385,-3.90473650376776,
3.42888770994031));
#46772=CARTESIAN_POINT('Ctrl Pts',(-27.9045363441654,-4.54206616433802,
1.92485926408358));
#46773=CARTESIAN_POINT('Ctrl Pts',(-27.8726380714115,-4.79763833485293,
1.32173683278195));
#46774=CARTESIAN_POINT('Ctrl Pts',(-27.8407397986575,-4.92117374333981,
0.662669505529257));
#46775=CARTESIAN_POINT('Ctrl Pts',(-27.8088415259036,-4.91810465358294,
0.00250400581179228));
#46776=CARTESIAN_POINT('Origin',(-14.75,0.,0.));
#46777=CARTESIAN_POINT('',(-26.0911584740964,-4.92036739665688,-0.00383377046079936));
#46778=CARTESIAN_POINT('',(-26.3088415259036,-4.92121007081632,-0.00410983607026229));
#46779=CARTESIAN_POINT('',(-14.75,-4.925,-6.03138548580071E-16));
#46780=CARTESIAN_POINT('Ctrl Pts',(-26.0911584740964,-4.92036739665688,
-0.00383377046079936));
#46781=CARTESIAN_POINT('Ctrl Pts',(-26.1441533704359,-4.91244432033151,
1.09173065983813));
#46782=CARTESIAN_POINT('Ctrl Pts',(-26.1971482667754,-4.55141276587038,
2.19203324705585));
#46783=CARTESIAN_POINT('Ctrl Pts',(-26.2501431631149,-3.87908362999679,
3.04775276608836));
#46784=CARTESIAN_POINT('Ctrl Pts',(-26.329689051488,-2.86991063247732,4.33219662844735));
#46785=CARTESIAN_POINT('Ctrl Pts',(-26.4092349398611,-1.15937419217738,
5.06558698769252));
#46786=CARTESIAN_POINT('Ctrl Pts',(-26.4887808282342,0.466768297211532,
4.91103020168458));
#46787=CARTESIAN_POINT('Ctrl Pts',(-26.5683267166072,2.09291078660044,4.75647341567663));
#46788=CARTESIAN_POINT('Ctrl Pts',(-26.6478726049803,3.63465932507832,3.71396948441558));
#46789=CARTESIAN_POINT('Ctrl Pts',(-26.7274184933534,4.38378843538607,2.26240825335668));
#46790=CARTESIAN_POINT('Ctrl Pts',(-26.8069643817264,5.13291754569381,0.810847022297775));
#46791=CARTESIAN_POINT('Ctrl Pts',(-26.8865102700995,5.08942722783144,-1.04977150855898));
#46792=CARTESIAN_POINT('Ctrl Pts',(-26.9660561584726,4.27329930907013,-2.46474911465105));
#46793=CARTESIAN_POINT('Ctrl Pts',(-27.0456020468457,3.45717139030882,-3.87972672074312));
#46794=CARTESIAN_POINT('Ctrl Pts',(-27.1251479352187,1.86840587064857,-4.84906340207051));
#46795=CARTESIAN_POINT('Ctrl Pts',(-27.2046938235918,0.236816482345431,
-4.92747617760022));
#46796=CARTESIAN_POINT('Ctrl Pts',(-27.2842397119649,-1.39477290595772,
-5.00588895312993));
#46797=CARTESIAN_POINT('Ctrl Pts',(-27.363785600338,-3.06918616290375,-4.19337782286196));
#46798=CARTESIAN_POINT('Ctrl Pts',(-27.4433314887111,-4.01724394449298,
-2.86319023358059));
#46799=CARTESIAN_POINT('Ctrl Pts',(-27.4926071505062,-4.60452979374673,
-2.03918945724775));
#46800=CARTESIAN_POINT('Ctrl Pts',(-27.5418828123013,-4.91308887859519,
-1.01653899859688));
#46801=CARTESIAN_POINT('Ctrl Pts',(-27.5911584740964,-4.91871916148224,
0.00298870709768639));
#46802=CARTESIAN_POINT('Ctrl Pts',(-27.8088415259036,-4.91810465358294,
0.00250400581179228));
#46803=CARTESIAN_POINT('Ctrl Pts',(-27.7611939102845,-4.91352024206437,
-0.983609324467926));
#46804=CARTESIAN_POINT('Ctrl Pts',(-27.7135462946653,-4.62644968879859,
-1.97217295080227));
#46805=CARTESIAN_POINT('Ctrl Pts',(-27.6658986790462,-4.07499817460332,
-2.78038834104901));
#46806=CARTESIAN_POINT('Ctrl Pts',(-27.5863527906731,-3.15437077234312,
-4.12967330271128));
#46807=CARTESIAN_POINT('Ctrl Pts',(-27.5068069023,-1.49688621586748,-4.97630902842222));
#46808=CARTESIAN_POINT('Ctrl Pts',(-27.427261013927,0.135976152639213,-4.93130021039854));
#46809=CARTESIAN_POINT('Ctrl Pts',(-27.3477151255539,1.7688385211459,-4.88629139237487));
#46810=CARTESIAN_POINT('Ctrl Pts',(-27.2681692371808,3.37707870168364,-3.9496380306166));
#46811=CARTESIAN_POINT('Ctrl Pts',(-27.1886233488077,4.22197683163389,-2.55164722242325));
#46812=CARTESIAN_POINT('Ctrl Pts',(-27.1090774604347,5.06687496158415,-1.1536564142299));
#46813=CARTESIAN_POINT('Ctrl Pts',(-27.0295315720616,5.14843104094691,0.705671840398515));
#46814=CARTESIAN_POINT('Ctrl Pts',(-26.9499856836885,4.42915646105591,2.17225163970649));
#46815=CARTESIAN_POINT('Ctrl Pts',(-26.8704397953154,3.7098818811649,3.63883143901446));
#46816=CARTESIAN_POINT('Ctrl Pts',(-26.7908939069423,2.18977664202013,4.71266278300198));
#46817=CARTESIAN_POINT('Ctrl Pts',(-26.7113480185693,0.567134884896936,
4.90045492678425));
#46818=CARTESIAN_POINT('Ctrl Pts',(-26.6318021301962,-1.05550687222627,
5.08824707056651));
#46819=CARTESIAN_POINT('Ctrl Pts',(-26.5522562418232,-2.7806851473279,4.39000001414349));
#46820=CARTESIAN_POINT('Ctrl Pts',(-26.4727103534501,-3.81592225162572,
3.12646916519825));
#46821=CARTESIAN_POINT('Ctrl Pts',(-26.4180874109346,-4.52680370627415,
2.25882189467213));
#46822=CARTESIAN_POINT('Ctrl Pts',(-26.3634644684191,-4.91235316928586,
1.12462305447093));
#46823=CARTESIAN_POINT('Ctrl Pts',(-26.3088415259036,-4.92121007081632,
-0.00410983607026228));
#46824=CARTESIAN_POINT('Origin',(-14.75,0.,0.));
#46825=CARTESIAN_POINT('',(-24.5911584740964,-4.93264761214373,-0.00145024765580815));
#46826=CARTESIAN_POINT('',(-24.8088415259036,-4.93298564037245,-0.000844910194652536));
#46827=CARTESIAN_POINT('',(-14.75,-4.925,-6.03138548580071E-16));
#46828=CARTESIAN_POINT('Ctrl Pts',(-24.5911584740964,-4.93264761214373,
-0.00145024765580815));
#46829=CARTESIAN_POINT('Ctrl Pts',(-24.6668780401975,-4.9266177416151,1.55388178409041));
#46830=CARTESIAN_POINT('Ctrl Pts',(-24.7425976062985,-4.12958481778531,
3.11453421006534));
#46831=CARTESIAN_POINT('Ctrl Pts',(-24.8183171723996,-2.86343383037207,
4.01706799645064));
#46832=CARTESIAN_POINT('Ctrl Pts',(-24.8978630607726,-1.53330067860747,
4.96520934909558));
#46833=CARTESIAN_POINT('Ctrl Pts',(-24.9774089491457,0.314560165826125,
5.18703834835445));
#46834=CARTESIAN_POINT('Ctrl Pts',(-25.0569548375188,1.83130840270388,4.58065477546433));
#46835=CARTESIAN_POINT('Ctrl Pts',(-25.1365007258919,3.34805663958163,3.9742712025742));
#46836=CARTESIAN_POINT('Ctrl Pts',(-25.2160466142649,4.53369226890353,2.5396750575351));
#46837=CARTESIAN_POINT('Ctrl Pts',(-25.295592502638,4.84357719847932,0.935867858373788));
#46838=CARTESIAN_POINT('Ctrl Pts',(-25.3751383910111,5.15346212805511,-0.667939340787529));
#46839=CARTESIAN_POINT('Ctrl Pts',(-25.4546842793842,4.58759635788477,-2.44095759407106));
#46840=CARTESIAN_POINT('Ctrl Pts',(-25.5342301677572,3.40591819971526,-3.56872660483793));
#46841=CARTESIAN_POINT('Ctrl Pts',(-25.6137760561303,2.22424004154574,-4.69649561560481));
#46842=CARTESIAN_POINT('Ctrl Pts',(-25.6933219445034,0.426749495377071,
-5.17901538385504));
#46843=CARTESIAN_POINT('Ctrl Pts',(-25.7728678328765,-1.16085155874105,
-4.79463371383198));
#46844=CARTESIAN_POINT('Ctrl Pts',(-25.8524137212495,-2.74845261285917,
-4.41025204380892));
#46845=CARTESIAN_POINT('Ctrl Pts',(-25.9319596096226,-4.12616417492674,
-3.15896893551255));
#46846=CARTESIAN_POINT('Ctrl Pts',(-26.0115054979957,-4.661115178591,-1.61557869862796));
#46847=CARTESIAN_POINT('Ctrl Pts',(-26.0380564900293,-4.83967223700271,
-1.10042269594398));
#46848=CARTESIAN_POINT('Ctrl Pts',(-26.0646074820628,-4.92433693997005,
-0.552722898855101));
#46849=CARTESIAN_POINT('Ctrl Pts',(-26.0911584740964,-4.92036739665688,
-0.00383377046079936));
#46850=CARTESIAN_POINT('Ctrl Pts',(-26.3088415259036,-4.92121007081632,
-0.00410983607026228));
#46851=CARTESIAN_POINT('Ctrl Pts',(-26.283918580046,-4.92525123130941,-0.519119599791246));
#46852=CARTESIAN_POINT('Ctrl Pts',(-26.2589956341884,-4.85087080801869,
-1.03299143706225));
#46853=CARTESIAN_POINT('Ctrl Pts',(-26.2340726883308,-4.69319011704004,
-1.5198867036229));
#46854=CARTESIAN_POINT('Ctrl Pts',(-26.1545267999577,-4.18992494466251,
-3.07389708203135));
#46855=CARTESIAN_POINT('Ctrl Pts',(-26.0749809115847,-2.83809866641343,
-4.35310319738077));
#46856=CARTESIAN_POINT('Ctrl Pts',(-25.9954350232116,-1.25869311650182,
-4.76988247643117));
#46857=CARTESIAN_POINT('Ctrl Pts',(-25.9158891348386,0.320712433409791,
-5.18666175548156));
#46858=CARTESIAN_POINT('Ctrl Pts',(-25.8363432464654,2.12769725498392,-4.74101419823293));
#46859=CARTESIAN_POINT('Ctrl Pts',(-25.7567973580924,3.33219893892002,-3.63765499595275));
#46860=CARTESIAN_POINT('Ctrl Pts',(-25.6772514697193,4.53670062285612,-2.53429579367258));
#46861=CARTESIAN_POINT('Ctrl Pts',(-25.5977055813462,5.13871916915418,-0.773224946360884));
#46862=CARTESIAN_POINT('Ctrl Pts',(-25.5181596929732,4.86170857536212,0.836585847286859));
#46863=CARTESIAN_POINT('Ctrl Pts',(-25.4386138046001,4.58469798157006,2.44639664093459));
#46864=CARTESIAN_POINT('Ctrl Pts',(-25.359067916227,3.4286582476879,3.90494738091836));
#46865=CARTESIAN_POINT('Ctrl Pts',(-25.2795220278539,1.92463240018136,4.54223247168555));
#46866=CARTESIAN_POINT('Ctrl Pts',(-25.1999761394808,0.420606552674816,
5.17951756245273));
#46867=CARTESIAN_POINT('Ctrl Pts',(-25.1204302511078,-1.43140540845612,
4.99553700400332));
#46868=CARTESIAN_POINT('Ctrl Pts',(-25.0408843627347,-2.78065642310143,
4.07480491924754));
#46869=CARTESIAN_POINT('Ctrl Pts',(-24.9635367504577,-4.09262045392238,
3.17951756047544));
#46870=CARTESIAN_POINT('Ctrl Pts',(-24.8861891381806,-4.92922749371504,
1.58763673888852));
#46871=CARTESIAN_POINT('Ctrl Pts',(-24.8088415259036,-4.93298564037245,
-0.000844910194652536));
#46872=CARTESIAN_POINT('Origin',(-14.75,0.,0.));
#46873=CARTESIAN_POINT('',(-23.0911584740964,-4.92477578693879,0.00455121266192807));
#46874=CARTESIAN_POINT('',(-23.3088415259036,-4.92376359828451,0.00452755087589233));
#46875=CARTESIAN_POINT('',(-14.75,-4.925,-6.03138548580071E-16));
#46876=CARTESIAN_POINT('Ctrl Pts',(-23.0911584740964,-4.92477578693879,
0.00455121266192807));
#46877=CARTESIAN_POINT('Ctrl Pts',(-23.1100568215859,-4.92836778419939,
0.39435127717714));
#46878=CARTESIAN_POINT('Ctrl Pts',(-23.1289551690754,-4.88600126774917,
0.783379637951124));
#46879=CARTESIAN_POINT('Ctrl Pts',(-23.147853516565,-4.7947032911263,1.1605640760821));
#46880=CARTESIAN_POINT('Ctrl Pts',(-23.227399404938,-4.41041685226391,2.74818813835895));
#46881=CARTESIAN_POINT('Ctrl Pts',(-23.3069452933111,-3.15921646993337,
4.12597456962399));
#46882=CARTESIAN_POINT('Ctrl Pts',(-23.3864911816842,-1.6158582674624,4.66101820240316));
#46883=CARTESIAN_POINT('Ctrl Pts',(-23.4660370700573,-0.0725000649914348,
5.19606183518233));
#46884=CARTESIAN_POINT('Ctrl Pts',(-23.5455829584304,1.76301595761996,4.88836266947564));
#46885=CARTESIAN_POINT('Ctrl Pts',(-23.6251288468034,3.04752024302872,3.87926655341467));
#46886=CARTESIAN_POINT('Ctrl Pts',(-23.7046747351765,4.33202452843749,2.87017043735369));
#46887=CARTESIAN_POINT('Ctrl Pts',(-23.7842206235496,5.06551707664363,1.1596773709384));
#46888=CARTESIAN_POINT('Ctrl Pts',(-23.8637665119226,4.91105798552202,-0.46647410387683));
#46889=CARTESIAN_POINT('Ctrl Pts',(-23.9433124002957,4.75659889440041,-2.09262557869207));
#46890=CARTESIAN_POINT('Ctrl Pts',(-24.0228582886688,3.71418816395107,-3.63443546190725));
#46891=CARTESIAN_POINT('Ctrl Pts',(-24.1024041770419,2.26267151748941,-4.38365215585762));
#46892=CARTESIAN_POINT('Ctrl Pts',(-24.181950065415,0.811154871027751,-5.132868849808));
#46893=CARTESIAN_POINT('Ctrl Pts',(-24.261495953788,-1.04946769144621,-5.08949235449356));
#46894=CARTESIAN_POINT('Ctrl Pts',(-24.3410418421611,-2.4644935804178,-4.2734482583492));
#46895=CARTESIAN_POINT('Ctrl Pts',(-24.4205877305342,-3.87951946938938,
-3.45740416220484));
#46896=CARTESIAN_POINT('Ctrl Pts',(-24.5001336189073,-4.84894868485859,
-1.86869246523057));
#46897=CARTESIAN_POINT('Ctrl Pts',(-24.5796795072803,-4.92746056304542,
-0.237109763727941));
#46898=CARTESIAN_POINT('Ctrl Pts',(-24.5835058295524,-4.93123714728213,
-0.158627250588653));
#46899=CARTESIAN_POINT('Ctrl Pts',(-24.5873321518244,-4.93295231843154,
-0.0800455421075516));
#46900=CARTESIAN_POINT('Ctrl Pts',(-24.5911584740964,-4.93264761214373,
-0.00145024765580815));
#46901=CARTESIAN_POINT('Ctrl Pts',(-24.8088415259036,-4.93298564037245,
-0.000844910194652536));
#46902=CARTESIAN_POINT('Ctrl Pts',(-24.8066432498076,-4.93309244966778,
-0.0459907283445572));
#46903=CARTESIAN_POINT('Ctrl Pts',(-24.8044449737115,-4.93252653505162,
-0.0911338008527958));
#46904=CARTESIAN_POINT('Ctrl Pts',(-24.8022466976155,-4.93127968975541,
-0.136258058327248));
#46905=CARTESIAN_POINT('Ctrl Pts',(-24.7227008092424,-4.88616187360439,
-1.76910534008413));
#46906=CARTESIAN_POINT('Ctrl Pts',(-24.6431549208693,-3.94943617314267,
-3.37731629253574));
#46907=CARTESIAN_POINT('Ctrl Pts',(-24.5636090324963,-2.55140047284839,
-4.22213703896742));
#46908=CARTESIAN_POINT('Ctrl Pts',(-24.4840631441232,-1.15336477255412,
-5.06695778539909));
#46909=CARTESIAN_POINT('Ctrl Pts',(-24.4045172557501,0.705980927572705,
-5.14838832581082));
#46910=CARTESIAN_POINT('Ctrl Pts',(-24.324971367377,2.17252059826335,-4.42902243726831));
#46911=CARTESIAN_POINT('Ctrl Pts',(-24.2454254790039,3.63906026895399,-3.70965654872581));
#46912=CARTESIAN_POINT('Ctrl Pts',(-24.1658795906309,4.71279391020846,-2.18949423122905));
#46913=CARTESIAN_POINT('Ctrl Pts',(-24.0863337022578,4.90048718004666,-0.566842967216153));
#46914=CARTESIAN_POINT('Ctrl Pts',(-24.0067878138847,5.08818044988486,1.05580829679675));
#46915=CARTESIAN_POINT('Ctrl Pts',(-23.9272419255116,4.3898333483068,2.78094850732579));
#46916=CARTESIAN_POINT('Ctrl Pts',(-23.8476960371386,3.12624123694881,3.81611075100284));
#46917=CARTESIAN_POINT('Ctrl Pts',(-23.7681501487655,1.86264912559084,4.85127299467987));
#46918=CARTESIAN_POINT('Ctrl Pts',(-23.6886042603924,0.0338120044529563,
5.19645727150491));
#46919=CARTESIAN_POINT('Ctrl Pts',(-23.6090583720193,-1.52016861672953,
4.69309843356272));
#46920=CARTESIAN_POINT('Ctrl Pts',(-23.5295124836463,-3.07414923791204,
4.18973959562053));
#46921=CARTESIAN_POINT('Ctrl Pts',(-23.4499665952732,-4.35327335913915,
2.83783764291109));
#46922=CARTESIAN_POINT('Ctrl Pts',(-23.3704207069001,-4.76995770197036,
1.25840735017577));
#46923=CARTESIAN_POINT('Ctrl Pts',(-23.3498943132346,-4.8774808817366,0.850843758656771));
#46924=CARTESIAN_POINT('Ctrl Pts',(-23.3293679195691,-4.92757673294028,
0.428129724095519));
#46925=CARTESIAN_POINT('Ctrl Pts',(-23.3088415259036,-4.92376359828451,
0.00452755087589233));
#46926=CARTESIAN_POINT('Origin',(-14.75,0.,0.));
#46927=CARTESIAN_POINT('',(-21.5911584740964,-4.91693164693359,-0.000632398697534842));
#46928=CARTESIAN_POINT('',(-21.8088415259036,-4.91711569616659,-0.00117946379282014));
#46929=CARTESIAN_POINT('',(-14.75,-4.925,-6.03138548580071E-16));
#46930=CARTESIAN_POINT('Ctrl Pts',(-21.5911584740964,-4.91693164693359,
-0.000632398697534842));
#46931=CARTESIAN_POINT('Ctrl Pts',(-21.6327814913475,-4.91594750340395,
0.861347871439622));
#46932=CARTESIAN_POINT('Ctrl Pts',(-21.6744045085985,-4.70055318639053,
1.72378817794021));
#46933=CARTESIAN_POINT('Ctrl Pts',(-21.7160275258496,-4.27359604091789,
2.46423730661521));
#46934=CARTESIAN_POINT('Ctrl Pts',(-21.7955734142227,-3.4576368030521,3.87931212880427));
#46935=CARTESIAN_POINT('Ctrl Pts',(-21.8751193025958,-1.86898324578976,
4.84883661113057));
#46936=CARTESIAN_POINT('Ctrl Pts',(-21.9546651909688,-0.237405254457672,
4.92744633348781));
#46937=CARTESIAN_POINT('Ctrl Pts',(-22.0342110793419,1.39417273687441,5.00605605584506));
#46938=CARTESIAN_POINT('Ctrl Pts',(-22.113756967715,3.06867516227623,4.19375101823326));
#46939=CARTESIAN_POINT('Ctrl Pts',(-22.1933028560881,4.01689627682146,2.86367472410927));
#46940=CARTESIAN_POINT('Ctrl Pts',(-22.2728487444611,4.9651173913667,1.53359842998527));
#46941=CARTESIAN_POINT('Ctrl Pts',(-22.3523946328342,5.18705719505533,-0.314249120650923));
#46942=CARTESIAN_POINT('Ctrl Pts',(-22.4319405212073,4.58076458321006,-1.83103371282965));
#46943=CARTESIAN_POINT('Ctrl Pts',(-22.5114864095804,3.97447197136479,-3.34781830500836));
#46944=CARTESIAN_POINT('Ctrl Pts',(-22.5910322979534,2.53994694398564,-4.5335399387296));
#46945=CARTESIAN_POINT('Ctrl Pts',(-22.6705781863265,0.936158324065459,
-4.84352105564377));
#46946=CARTESIAN_POINT('Ctrl Pts',(-22.7501240746996,-0.667630295854733,
-5.15350217255794));
#46947=CARTESIAN_POINT('Ctrl Pts',(-22.8296699630727,-2.44068250831595,
-4.58774277266501));
#46948=CARTESIAN_POINT('Ctrl Pts',(-22.9092158514458,-3.56852236684944,
-3.40613222607422));
#46949=CARTESIAN_POINT('Ctrl Pts',(-22.9698633923293,-4.42841236656523,
-2.50524626705758));
#46950=CARTESIAN_POINT('Ctrl Pts',(-23.0305109332129,-4.9132485462191,-1.24637378817277));
#46951=CARTESIAN_POINT('Ctrl Pts',(-23.0911584740964,-4.92477578693879,
0.00455121266192807));
#46952=CARTESIAN_POINT('Ctrl Pts',(-23.3088415259036,-4.92376359828451,
0.00452755087589233));
#46953=CARTESIAN_POINT('Ctrl Pts',(-23.249822031196,-4.9127997005681,-1.2134548491438));
#46954=CARTESIAN_POINT('Ctrl Pts',(-23.1908025364885,-4.4561520233695,-2.43877979118426));
#46955=CARTESIAN_POINT('Ctrl Pts',(-23.1317830417809,-3.63745529283231,
-3.33241721991151));
#46956=CARTESIAN_POINT('Ctrl Pts',(-23.0522371534078,-2.53402397642775,
-4.53685286450225));
#46957=CARTESIAN_POINT('Ctrl Pts',(-22.9726912650347,-0.77291677918332,
-5.13876552092253));
#46958=CARTESIAN_POINT('Ctrl Pts',(-22.8931453766617,0.83687745995922,-4.86165832319329));
#46959=CARTESIAN_POINT('Ctrl Pts',(-22.8135994882886,2.44667169910178,-4.58455112546405));
#46960=CARTESIAN_POINT('Ctrl Pts',(-22.7340535999155,3.90515298014245,-3.42842407358526));
#46961=CARTESIAN_POINT('Ctrl Pts',(-22.6545077115424,4.5423478449547,-1.92436004709929));
#46962=CARTESIAN_POINT('Ctrl Pts',(-22.5749618231694,5.17954270976695,-0.42029602061334));
#46963=CARTESIAN_POINT('Ctrl Pts',(-22.4954159347963,4.9954511583508,1.43170498047977));
#46964=CARTESIAN_POINT('Ctrl Pts',(-22.4158700464232,4.07463817966522,2.78090079647325));
#46965=CARTESIAN_POINT('Ctrl Pts',(-22.3363241580501,3.15382520097963,4.13009661246674));
#46966=CARTESIAN_POINT('Ctrl Pts',(-22.2567782696771,1.4962907950246,4.97648724336059));
#46967=CARTESIAN_POINT('Ctrl Pts',(-22.177232381304,-0.136553786680188,
4.93127149915006));
#46968=CARTESIAN_POINT('Ctrl Pts',(-22.0976864929309,-1.76939836838497,
4.88605575493953));
#46969=CARTESIAN_POINT('Ctrl Pts',(-22.0181406045578,-3.37755312583951,
3.94923363562461));
#46970=CARTESIAN_POINT('Ctrl Pts',(-21.9385947161848,-4.22229002887781,
2.55114728056903));
#46971=CARTESIAN_POINT('Ctrl Pts',(-21.8953436527577,-4.68159433887712,
1.79097321179257));
#46972=CARTESIAN_POINT('Ctrl Pts',(-21.8520925893307,-4.91520443767987,
0.894432581458181));
#46973=CARTESIAN_POINT('Ctrl Pts',(-21.8088415259036,-4.91711569616659,
-0.00117946379282014));
#46974=CARTESIAN_POINT('Origin',(-14.75,0.,0.));
#46975=CARTESIAN_POINT('',(-20.0911584740964,-4.92710437571252,-0.00432825790191715));
#46976=CARTESIAN_POINT('',(-20.3088415259036,-4.92810468982102,-0.00410855472338207));
#46977=CARTESIAN_POINT('',(-14.75,-4.925,-6.03138548580071E-16));
#46978=CARTESIAN_POINT('Ctrl Pts',(-20.0911584740964,-4.92710437571252,
-0.00432825790191715));
#46979=CARTESIAN_POINT('Ctrl Pts',(-20.155506161109,-4.91490963574447,1.32130828947872));
#46980=CARTESIAN_POINT('Ctrl Pts',(-20.2198538481216,-4.36214110397647,
2.65590833175386));
#46981=CARTESIAN_POINT('Ctrl Pts',(-20.2842015351343,-3.40634621717809,
3.56831810142706));
#46982=CARTESIAN_POINT('Ctrl Pts',(-20.3637474235073,-2.22480330705116,
4.69622881676794));
#46983=CARTESIAN_POINT('Ctrl Pts',(-20.4432933118804,-0.427370559254853,
5.1789641106682));
#46984=CARTESIAN_POINT('Ctrl Pts',(-20.5228392002535,1.16027654508549,4.79477287920708));
#46985=CARTESIAN_POINT('Ctrl Pts',(-20.6023850886266,2.74792364942585,4.41058164774596));
#46986=CARTESIAN_POINT('Ctrl Pts',(-20.6819309769996,4.12578511031025,3.15946389092347));
#46987=CARTESIAN_POINT('Ctrl Pts',(-20.7614768653727,4.66092129423408,1.61613777667943));
#46988=CARTESIAN_POINT('Ctrl Pts',(-20.8410227537458,5.19605747815791,0.0728116624353919));
#46989=CARTESIAN_POINT('Ctrl Pts',(-20.9205686421189,4.88846838512118,-1.76272280923018));
#46990=CARTESIAN_POINT('Ctrl Pts',(-21.0001145304919,3.87944930013121,-3.04728760571889));
#46991=CARTESIAN_POINT('Ctrl Pts',(-21.079660418865,2.87043021514126,-4.33185240220757));
#46992=CARTESIAN_POINT('Ctrl Pts',(-21.1592063072381,1.1599811381981,-5.06544752351941));
#46993=CARTESIAN_POINT('Ctrl Pts',(-21.2387521956112,-0.466179596436317,
-4.91108594998304));
#46994=CARTESIAN_POINT('Ctrl Pts',(-21.3182980839842,-2.09234033107078,
-4.75672437644668));
#46995=CARTESIAN_POINT('Ctrl Pts',(-21.3978439723573,-3.6342127233965,-3.71440610806206));
#46996=CARTESIAN_POINT('Ctrl Pts',(-21.4773898607304,-4.38351646032473,
-2.26293439284383));
#46997=CARTESIAN_POINT('Ctrl Pts',(-21.5153127318524,-4.74074107152647,
-1.57095676937065));
#46998=CARTESIAN_POINT('Ctrl Pts',(-21.5532356029744,-4.9178283034161,-0.785985524275935));
#46999=CARTESIAN_POINT('Ctrl Pts',(-21.5911584740964,-4.91693164693359,
-0.000632398697534842));
#47000=CARTESIAN_POINT('Ctrl Pts',(-21.8088415259036,-4.91711569616659,
-0.00117946379282014));
#47001=CARTESIAN_POINT('Ctrl Pts',(-21.7725467009576,-4.91871955944082,
-0.752746704602252));
#47002=CARTESIAN_POINT('Ctrl Pts',(-21.7362518760116,-4.75716117024752,
-1.50366003608004));
#47003=CARTESIAN_POINT('Ctrl Pts',(-21.6999570510655,-4.42889215011132,
-2.17278619696736));
#47004=CARTESIAN_POINT('Ctrl Pts',(-21.6204111626925,-3.70943831968447,
-3.63928272865185));
#47005=CARTESIAN_POINT('Ctrl Pts',(-21.5408652743194,-2.18921161020874,
-4.71292520122458));
#47006=CARTESIAN_POINT('Ctrl Pts',(-21.4613193859463,-0.566549092315044,
-4.90052116218762));
#47007=CARTESIAN_POINT('Ctrl Pts',(-21.3817734975732,1.05611342557867,-5.08811712315067));
#47008=CARTESIAN_POINT('Ctrl Pts',(-21.3022276092002,2.78121175189034,-4.38966657250399));
#47009=CARTESIAN_POINT('Ctrl Pts',(-21.2226817208271,3.81629821795521,-3.12601238748351));
#47010=CARTESIAN_POINT('Ctrl Pts',(-21.143135832454,4.85138468402006,-1.86235820246306));
#47011=CARTESIAN_POINT('Ctrl Pts',(-21.0635899440809,5.19645928983812,-0.0335003830688158));
#47012=CARTESIAN_POINT('Ctrl Pts',(-20.9840440557079,4.69300726397856,1.52045005024925));
#47013=CARTESIAN_POINT('Ctrl Pts',(-20.9044981673348,4.189555238119,3.07440048356732));
#47014=CARTESIAN_POINT('Ctrl Pts',(-20.8249522789617,2.83757658058181,4.35344353080922));
#47015=CARTESIAN_POINT('Ctrl Pts',(-20.7454063905886,1.25812130277897,4.77003315738511));
#47016=CARTESIAN_POINT('Ctrl Pts',(-20.6658605022155,-0.321333975023885,
5.186622783961));
#47017=CARTESIAN_POINT('Ctrl Pts',(-20.5863146138425,-2.1282658730924,4.74075898987086));
#47018=CARTESIAN_POINT('Ctrl Pts',(-20.5067687254694,-3.33263534483166,
3.63725544792229));
#47019=CARTESIAN_POINT('Ctrl Pts',(-20.4407929922808,-4.33154503775366,
2.72200443061253));
#47020=CARTESIAN_POINT('Ctrl Pts',(-20.3748172590922,-4.91594471882842,
1.3543550430017));
#47021=CARTESIAN_POINT('Ctrl Pts',(-20.3088415259036,-4.92810468982102,
-0.00410855472338207));
#47022=CARTESIAN_POINT('Origin',(-14.75,0.,0.));
#47023=CARTESIAN_POINT('',(-18.5911584740964,-4.93133925263252,0.00269369058761092));
#47024=CARTESIAN_POINT('',(-18.8088415259036,-4.93057297854711,0.00316028518611533));
#47025=CARTESIAN_POINT('',(-14.75,-4.925,-6.03138548580071E-16));
#47026=CARTESIAN_POINT('Ctrl Pts',(-18.5911584740964,-4.93133925263252,
0.00269369058761092));
#47027=CARTESIAN_POINT('Ctrl Pts',(-18.5986849424975,-4.93235666587827,
0.157401246761113));
#47028=CARTESIAN_POINT('Ctrl Pts',(-18.6062114108986,-4.92571004477723,
0.312020226781154));
#47029=CARTESIAN_POINT('Ctrl Pts',(-18.6137378792997,-4.91111389702246,
0.465885087471429));
#47030=CARTESIAN_POINT('Ctrl Pts',(-18.6932837676727,-4.75684984141161,
2.0920550759408));
#47031=CARTESIAN_POINT('Ctrl Pts',(-18.7728296560458,-3.7146240379434,3.63398997126305));
#47032=CARTESIAN_POINT('Ctrl Pts',(-18.8523755444189,-2.26319725960073,
4.3833807487362));
#47033=CARTESIAN_POINT('Ctrl Pts',(-18.931921432792,-0.811770481258054,
5.13277152620935));
#47034=CARTESIAN_POINT('Ctrl Pts',(-19.0114673211651,1.04885727195908,5.08961818583339));
#47035=CARTESIAN_POINT('Ctrl Pts',(-19.0910132095381,2.46398102306833,4.27374380867811));
#47036=CARTESIAN_POINT('Ctrl Pts',(-19.1705590979112,3.87910477417757,3.45786943152285));
#47037=CARTESIAN_POINT('Ctrl Pts',(-19.2501049862843,4.84872452317893,1.86927401758828));
#47038=CARTESIAN_POINT('Ctrl Pts',(-19.3296508746573,4.92743208790438,0.237700743258566));
#47039=CARTESIAN_POINT('Ctrl Pts',(-19.4091967630304,5.00613965262983,-1.39387253107114));
#47040=CARTESIAN_POINT('Ctrl Pts',(-19.4887426514035,4.19393503307937,-3.068423665796));
#47041=CARTESIAN_POINT('Ctrl Pts',(-19.5682885397766,2.86391560429619,-4.01672454068289));
#47042=CARTESIAN_POINT('Ctrl Pts',(-19.6478344281497,1.53389617551299,-4.9650254155698));
#47043=CARTESIAN_POINT('Ctrl Pts',(-19.7273803165227,-0.313938062502946,
-5.18707603061872));
#47044=CARTESIAN_POINT('Ctrl Pts',(-19.8069262048958,-1.8307590101278,-4.58087437844472));
#47045=CARTESIAN_POINT('Ctrl Pts',(-19.8864720932689,-3.34757995775264,
-3.97467272627071));
#47046=CARTESIAN_POINT('Ctrl Pts',(-19.9660179816419,-4.5333876149864,-2.54021880687379));
#47047=CARTESIAN_POINT('Ctrl Pts',(-20.045563870015,-4.84346490737449,-0.936448778784566));
#47048=CARTESIAN_POINT('Ctrl Pts',(-20.0607620713755,-4.90270891386442,
-0.630029172173884));
#47049=CARTESIAN_POINT('Ctrl Pts',(-20.0759602727359,-4.92998463640529,
-0.317428729934899));
#47050=CARTESIAN_POINT('Ctrl Pts',(-20.0911584740964,-4.92710437571252,
-0.00432825790191715));
#47051=CARTESIAN_POINT('Ctrl Pts',(-20.3088415259036,-4.92810468982102,
-0.00410855472338207));
#47052=CARTESIAN_POINT('Ctrl Pts',(-20.2952713707191,-4.93060580175162,
-0.283522832407918));
#47053=CARTESIAN_POINT('Ctrl Pts',(-20.2817012155346,-4.90889778438975,
-0.562548496769959));
#47054=CARTESIAN_POINT('Ctrl Pts',(-20.2681310603502,-4.86160812861449,
-0.837169002561447));
#47055=CARTESIAN_POINT('Ctrl Pts',(-20.1885851719771,-4.58440439524805,
-2.44694662128967));
#47056=CARTESIAN_POINT('Ctrl Pts',(-20.109039283604,-3.42818988310517,-3.90535856893913));
#47057=CARTESIAN_POINT('Ctrl Pts',(-20.0294933952309,-1.9240876479818,-4.54246323682914));
#47058=CARTESIAN_POINT('Ctrl Pts',(-19.9499475068579,-0.419985412858412,
-5.17956790471916));
#47059=CARTESIAN_POINT('Ctrl Pts',(-19.8704016184848,1.43200454524547,-4.9953652928497));
#47060=CARTESIAN_POINT('Ctrl Pts',(-19.7908557301117,2.78114513946445,-4.07447140722498));
#47061=CARTESIAN_POINT('Ctrl Pts',(-19.7113098417387,4.13028573368341,-3.15357752160028));
#47062=CARTESIAN_POINT('Ctrl Pts',(-19.6317639533656,4.97657696401748,-1.49599236222033));
#47063=CARTESIAN_POINT('Ctrl Pts',(-19.5522180649925,4.93126330142958,0.136849505056872));
#47064=CARTESIAN_POINT('Ctrl Pts',(-19.4726721766194,4.88594963884169,1.76969137233409));
#47065=CARTESIAN_POINT('Ctrl Pts',(-19.3931262882463,3.94903108333184,3.37778994750857));
#47066=CARTESIAN_POINT('Ctrl Pts',(-19.3135803998733,2.55089407358275,4.22244300854623));
#47067=CARTESIAN_POINT('Ctrl Pts',(-19.2340345115002,1.15275706383363,5.06709606958391));
#47068=CARTESIAN_POINT('Ctrl Pts',(-19.1544886231271,-0.706598400154735,
5.14830361648474));
#47069=CARTESIAN_POINT('Ctrl Pts',(-19.074942734754,-2.17305178497508,4.42876184445237));
#47070=CARTESIAN_POINT('Ctrl Pts',(-18.995396846381,-3.63950516979541,3.70922007242002));
#47071=CARTESIAN_POINT('Ctrl Pts',(-18.9158509580079,-4.71305647544771,
2.18892898145449));
#47072=CARTESIAN_POINT('Ctrl Pts',(-18.8363050696348,-4.90055512820742,
0.566255216718109));
#47073=CARTESIAN_POINT('Ctrl Pts',(-18.8271505550577,-4.92213335412174,
0.379510295806119));
#47074=CARTESIAN_POINT('Ctrl Pts',(-18.8179960404807,-4.93197626646748,
0.191409368818455));
#47075=CARTESIAN_POINT('Ctrl Pts',(-18.8088415259036,-4.93057297854711,
0.00316028518611533));
#47076=CARTESIAN_POINT('Origin',(-14.75,0.,0.));
#47077=CARTESIAN_POINT('',(-17.0911584740964,-4.91873477802609,0.00299898967114021));
#47078=CARTESIAN_POINT('',(-17.3088415259036,-4.91816086074912,0.00255430743475421));
#47079=CARTESIAN_POINT('',(-14.75,-4.925,-6.03138548580071E-16));
#47080=CARTESIAN_POINT('Ctrl Pts',(-17.0911584740964,-4.91873477802609,
0.00299898967114021));
#47081=CARTESIAN_POINT('Ctrl Pts',(-17.121409612259,-4.92219933969977,0.628902743871938));
#47082=CARTESIAN_POINT('Ctrl Pts',(-17.1516607504217,-4.81148680932676,
1.25362658234333));
#47083=CARTESIAN_POINT('Ctrl Pts',(-17.1819118885843,-4.58098415721058,
1.83048430084528));
#47084=CARTESIAN_POINT('Ctrl Pts',(-17.2614577769574,-3.97487346688356,
3.34734159845876));
#47085=CARTESIAN_POINT('Ctrl Pts',(-17.3410036653305,-2.54049066060951,
4.53323527492929));
#47086=CARTESIAN_POINT('Ctrl Pts',(-17.4205495537035,-0.936739230126934,
4.84340874168148));
#47087=CARTESIAN_POINT('Ctrl Pts',(-17.5000954420766,0.667012200355664,
5.15358220843367));
#47088=CARTESIAN_POINT('Ctrl Pts',(-17.5796413304497,2.44013225504679,4.58803546546751));
#47089=CARTESIAN_POINT('Ctrl Pts',(-17.6591872188228,3.56811382315476,3.40656019604341));
#47090=CARTESIAN_POINT('Ctrl Pts',(-17.7387331071958,4.69609539126271,2.22508492661932));
#47091=CARTESIAN_POINT('Ctrl Pts',(-17.8182789955689,5.17893847278751,0.427681130737319));
#47092=CARTESIAN_POINT('Ctrl Pts',(-17.897824883942,4.79484245007892,-1.15998900993782));
#47093=CARTESIAN_POINT('Ctrl Pts',(-17.9773707723151,4.41074642737033,-2.74765915061299));
#47094=CARTESIAN_POINT('Ctrl Pts',(-18.0569166606881,3.15971130042833,-4.12559563608129));
#47095=CARTESIAN_POINT('Ctrl Pts',(-18.1364625490612,1.61641728001955,-4.66082436926233));
#47096=CARTESIAN_POINT('Ctrl Pts',(-18.2160084374343,0.0731232596108,-5.19605310244336));
#47097=CARTESIAN_POINT('Ctrl Pts',(-18.2955543258074,-1.76242965426471,
-4.88857408333716));
#47098=CARTESIAN_POINT('Ctrl Pts',(-18.3751002141804,-3.04705495732574,
-3.87963203297581));
#47099=CARTESIAN_POINT('Ctrl Pts',(-18.4471196341524,-4.21013165556918,
-2.96615400490252));
#47100=CARTESIAN_POINT('Ctrl Pts',(-18.5191390541244,-4.92160380860666,
-1.47767503842927));
#47101=CARTESIAN_POINT('Ctrl Pts',(-18.5911584740964,-4.93133925263252,
0.00269369058761092));
#47102=CARTESIAN_POINT('Ctrl Pts',(-18.8088415259036,-4.93057297854711,
0.00316028518611533));
#47103=CARTESIAN_POINT('Ctrl Pts',(-18.7384501521076,-4.91978274344346,
-1.4443344455465));
#47104=CARTESIAN_POINT('Ctrl Pts',(-18.6680587783116,-4.24406537670826,
-2.90058887915162));
#47105=CARTESIAN_POINT('Ctrl Pts',(-18.5976674045156,-3.12578352599411,
-3.8164856718825));
#47106=CARTESIAN_POINT('Ctrl Pts',(-18.5181215161425,-1.86206727115392,
-4.85149635723954));
#47107=CARTESIAN_POINT('Ctrl Pts',(-18.4385756277694,-0.0331887616064278,
-5.19646128944632));
#47108=CARTESIAN_POINT('Ctrl Pts',(-18.3590297393964,1.52073147789346,-4.69291607715336));
#47109=CARTESIAN_POINT('Ctrl Pts',(-18.2794838510233,3.07465171739332,-4.18937086486042));
#47110=CARTESIAN_POINT('Ctrl Pts',(-18.1999379626502,4.35361368684558,-2.83731550806776));
#47111=CARTESIAN_POINT('Ctrl Pts',(-18.1203920742771,4.77010859585846,-1.2578352510475));
#47112=CARTESIAN_POINT('Ctrl Pts',(-18.0408461859041,5.18660350487135,0.321645005972764));
#47113=CARTESIAN_POINT('Ctrl Pts',(-17.961300297531,4.74063135344486,2.12855016322063));
#47114=CARTESIAN_POINT('Ctrl Pts',(-17.8817544091579,3.63705558982148,3.33285345786593));
#47115=CARTESIAN_POINT('Ctrl Pts',(-17.8022085207848,2.53347982619808,4.53715675251125));
#47116=CARTESIAN_POINT('Ctrl Pts',(-17.7226626324118,0.772300450377784,
5.13885818455397));
#47117=CARTESIAN_POINT('Ctrl Pts',(-17.6431167440387,-0.837460542095409,
4.86155791650103));
#47118=CARTESIAN_POINT('Ctrl Pts',(-17.5635708556656,-2.44722153456857,
4.58425764844809));
#47119=CARTESIAN_POINT('Ctrl Pts',(-17.4840249672925,-3.90556414369463,
3.42795568029952));
#47120=CARTESIAN_POINT('Ctrl Pts',(-17.4044790789195,-4.5425786123982,1.92381524197179));
#47121=CARTESIAN_POINT('Ctrl Pts',(-17.3725998945808,-4.79787152683423,
1.32100884574773));
#47122=CARTESIAN_POINT('Ctrl Pts',(-17.3407207102422,-4.92124900075768,
0.662335296357207));
#47123=CARTESIAN_POINT('Ctrl Pts',(-17.3088415259036,-4.91816086074912,
0.00255430743475421));
#47124=CARTESIAN_POINT('Origin',(-14.75,0.,0.));
#47125=CARTESIAN_POINT('',(-15.5911584740964,-4.92035796642718,-0.00383015064837622));
#47126=CARTESIAN_POINT('',(-15.8088415259036,-4.92120003017842,-0.00410675641256026));
#47127=CARTESIAN_POINT('',(-14.75,-4.925,-6.03138548580071E-16));
#47128=CARTESIAN_POINT('Ctrl Pts',(-15.5911584740964,-4.92035796642718,
-0.00383015064837622));
#47129=CARTESIAN_POINT('Ctrl Pts',(-15.6441342820206,-4.9124462735778,1.09134504077847));
#47130=CARTESIAN_POINT('Ctrl Pts',(-15.6971100899448,-4.55169660768519,
2.19124987504687));
#47131=CARTESIAN_POINT('Ctrl Pts',(-15.750085897869,-3.87981475186871,3.04682229797494));
#47132=CARTESIAN_POINT('Ctrl Pts',(-15.829631786242,-2.87094973976422,4.33150810298851));
#47133=CARTESIAN_POINT('Ctrl Pts',(-15.9091776746151,-1.16058865962495,
5.06530836353102));
#47134=CARTESIAN_POINT('Ctrl Pts',(-15.9887235629882,0.465590576831222,
4.91114182640059));
#47135=CARTESIAN_POINT('Ctrl Pts',(-16.0682694513612,2.0917698132874,4.75697528927016));
#47136=CARTESIAN_POINT('Ctrl Pts',(-16.1478153397343,3.63376720606049,3.71484195446679));
#47137=CARTESIAN_POINT('Ctrl Pts',(-16.2273612281074,4.38324502138396,2.26346011821903));
#47138=CARTESIAN_POINT('Ctrl Pts',(-16.3069071164805,5.13272283670744,0.812078281971235));
#47139=CARTESIAN_POINT('Ctrl Pts',(-16.3864530048536,5.08968107458128,-1.04855205572096));
#47140=CARTESIAN_POINT('Ctrl Pts',(-16.4659988932266,4.27389156106992,-2.46372473066101));
#47141=CARTESIAN_POINT('Ctrl Pts',(-16.5455447815997,3.45810204755859,-3.87889740560104));
#47142=CARTESIAN_POINT('Ctrl Pts',(-16.6250906699728,1.86956478266209,-4.84861241778893));
#47143=CARTESIAN_POINT('Ctrl Pts',(-16.7046365583459,0.237996231203316,
-4.92741782460026));
#47144=CARTESIAN_POINT('Ctrl Pts',(-16.7841824467189,-1.39357232025546,
-5.00622323141159));
#47145=CARTESIAN_POINT('Ctrl Pts',(-16.863728335092,-3.06817215827651,-4.19411903284637));
#47146=CARTESIAN_POINT('Ctrl Pts',(-16.9432742234651,-4.01655279009705,
-2.86415647418555));
#47147=CARTESIAN_POINT('Ctrl Pts',(-16.9925689736755,-4.60426621320643,
-2.03997594821106));
#47148=CARTESIAN_POINT('Ctrl Pts',(-17.041863723886,-4.91308921515918,-1.01692194861672));
#47149=CARTESIAN_POINT('Ctrl Pts',(-17.0911584740964,-4.91873477802609,
0.00299898967114021));
#47150=CARTESIAN_POINT('Ctrl Pts',(-17.3088415259036,-4.91816086074912,
0.00255430743475421));
#47151=CARTESIAN_POINT('Ctrl Pts',(-17.2611748218691,-4.91354338201311,
-0.983969839246001));
#47152=CARTESIAN_POINT('Ctrl Pts',(-17.2135081178347,-4.62618522137736,
-1.9729699017009));
#47153=CARTESIAN_POINT('Ctrl Pts',(-17.1658414138002,-4.07430462011665,
-2.78138947246816));
#47154=CARTESIAN_POINT('Ctrl Pts',(-17.0862955254271,-3.15332983085048,
-4.13047484007342));
#47155=CARTESIAN_POINT('Ctrl Pts',(-17.0067496370541,-1.4956939240371,-4.97666666677702));
#47156=CARTESIAN_POINT('Ctrl Pts',(-16.927203748681,0.137145222933267,-4.93125508596819));
#47157=CARTESIAN_POINT('Ctrl Pts',(-16.8476578603079,1.76998436990362,-4.88584350515936));
#47158=CARTESIAN_POINT('Ctrl Pts',(-16.7681119719349,3.37802675703098,-3.94882851683809));
#47159=CARTESIAN_POINT('Ctrl Pts',(-16.6885660835618,4.2225959730343,-2.55064085742682));
#47160=CARTESIAN_POINT('Ctrl Pts',(-16.6090201951887,5.06716518903764,-1.15245319801552));
#47161=CARTESIAN_POINT('Ctrl Pts',(-16.5294743068156,5.14826123391693,0.706907132485781));
#47162=CARTESIAN_POINT('Ctrl Pts',(-16.4499284184425,4.42863152286466,2.17331736517013));
#47163=CARTESIAN_POINT('Ctrl Pts',(-16.3703825300695,3.7090018118124,3.63972759785445));
#47164=CARTESIAN_POINT('Ctrl Pts',(-16.2908366416964,2.18864634482861,4.71318773272181));
#47165=CARTESIAN_POINT('Ctrl Pts',(-16.2112907533233,0.565961339085978,
4.90058907660299));
#47166=CARTESIAN_POINT('Ctrl Pts',(-16.1317448649502,-1.05672366665665,
5.08799042048417));
#47167=CARTESIAN_POINT('Ctrl Pts',(-16.0521989765772,-2.78173821115814,
4.38933297337918));
#47168=CARTESIAN_POINT('Ctrl Pts',(-15.9726530882041,-3.81667311208576,
3.12555465326431));
#47169=CARTESIAN_POINT('Ctrl Pts',(-15.9180492341039,-4.52709869773482,
2.25804071360155));
#47170=CARTESIAN_POINT('Ctrl Pts',(-15.8634453800038,-4.91235438239858,
1.1242382374886));
#47171=CARTESIAN_POINT('Ctrl Pts',(-15.8088415259036,-4.92120003017842,
-0.00410675641256026));
#47172=CARTESIAN_POINT('Origin',(-14.75,0.,0.));
#47173=CARTESIAN_POINT('',(-14.0911584740964,-4.93264269199776,-0.00145718338004752));
#47174=CARTESIAN_POINT('',(-14.3088415259036,-4.93298263358733,-0.000852151517113329));
#47175=CARTESIAN_POINT('',(-14.75,-4.925,-6.03138548580071E-16));
#47176=CARTESIAN_POINT('Ctrl Pts',(-14.0911584740964,-4.93264269199776,
-0.00145718338004752));
#47177=CARTESIAN_POINT('Ctrl Pts',(-14.1668589517821,-4.92658863837471,
1.55348689693233));
#47178=CARTESIAN_POINT('Ctrl Pts',(-14.2425594294679,-4.13001266093176,
3.11377115163446));
#47179=CARTESIAN_POINT('Ctrl Pts',(-14.3182599071536,-2.86439733377493,
4.01638102506703));
#47180=CARTESIAN_POINT('Ctrl Pts',(-14.3978057955267,-1.5344916500192,4.96484141041069));
#47181=CARTESIAN_POINT('Ctrl Pts',(-14.4773516838997,0.313315942832746,
5.18711364580286));
#47182=CARTESIAN_POINT('Ctrl Pts',(-14.5568975722728,1.83020958498003,4.58109391950248));
#47183=CARTESIAN_POINT('Ctrl Pts',(-14.6364434606459,3.3471032271273,3.97507419320211));
#47184=CARTESIAN_POINT('Ctrl Pts',(-14.715989349019,4.53308291856992,2.5407625052092));
#47185=CARTESIAN_POINT('Ctrl Pts',(-14.7955352373921,4.84335255857077,0.937029678100604));
#47186=CARTESIAN_POINT('Ctrl Pts',(-14.8750811257651,5.15362219857162,-0.666703149008015));
#47187=CARTESIAN_POINT('Ctrl Pts',(-14.9546270141382,4.58818178713068,-2.43985711523233));
#47188=CARTESIAN_POINT('Ctrl Pts',(-15.0341729025113,3.40677416265819,-3.56790953205094));
#47189=CARTESIAN_POINT('Ctrl Pts',(-15.1137187908843,2.22536653818572,-4.69596194886955));
#47190=CARTESIAN_POINT('Ctrl Pts',(-15.1932646792574,0.427991700681723,
-5.17891281628248));
#47191=CARTESIAN_POINT('Ctrl Pts',(-15.2728105676305,-1.15970147061867,
-4.79491200370771));
#47192=CARTESIAN_POINT('Ctrl Pts',(-15.3523564560036,-2.74739464191907,
-4.41091119113294));
#47193=CARTESIAN_POINT('Ctrl Pts',(-15.4319023443767,-4.12540614701586,
-3.15995869857046));
#47194=CARTESIAN_POINT('Ctrl Pts',(-15.5114482327497,-4.6607274275294,-1.61669677754691));
#47195=CARTESIAN_POINT('Ctrl Pts',(-15.5380183131986,-4.83953653734212,
-1.10121327193814));
#47196=CARTESIAN_POINT('Ctrl Pts',(-15.5645883936475,-4.92432608553159,
-0.553116590668242));
#47197=CARTESIAN_POINT('Ctrl Pts',(-15.5911584740964,-4.92035796642718,
-0.00383015064837622));
#47198=CARTESIAN_POINT('Ctrl Pts',(-15.8088415259036,-4.92120003017842,
-0.00410675641256026));
#47199=CARTESIAN_POINT('Ctrl Pts',(-15.7838994916307,-4.92524055907015,
-0.519513955654037));
#47200=CARTESIAN_POINT('Ctrl Pts',(-15.7589574573578,-4.85074335816441,
-1.03378245448552));
#47201=CARTESIAN_POINT('Ctrl Pts',(-15.7340154230849,-4.69282487345136,
-1.52101290006915));
#47202=CARTESIAN_POINT('Ctrl Pts',(-15.6544695347118,-4.18918647653558,
-3.07490294016289));
#47203=CARTESIAN_POINT('Ctrl Pts',(-15.5749236463387,-2.83705442535027,
-4.35378382722562));
#47204=CARTESIAN_POINT('Ctrl Pts',(-15.4953777579656,-1.25754919479281,
-4.77018401717759));
#47205=CARTESIAN_POINT('Ctrl Pts',(-15.4158318695926,0.321956035764672,
-5.18658420712955));
#47206=CARTESIAN_POINT('Ctrl Pts',(-15.3362859812195,2.12883444569431,-4.74050369997076));
#47207=CARTESIAN_POINT('Ctrl Pts',(-15.2567400928464,3.33307155891485,-3.63685571864124));
#47208=CARTESIAN_POINT('Ctrl Pts',(-15.1771942044733,4.5373086721354,-2.53320773731172));
#47209=CARTESIAN_POINT('Ctrl Pts',(-15.0976483161003,5.13890448864684,-0.771992281811449));
#47210=CARTESIAN_POINT('Ctrl Pts',(-15.0181024277272,4.86150768690456,0.837752078617765));
#47211=CARTESIAN_POINT('Ctrl Pts',(-14.9385565393541,4.58411088516229,2.44749643904697));
#47212=CARTESIAN_POINT('Ctrl Pts',(-14.859010650981,3.42772146516635,3.90576970440512));
#47213=CARTESIAN_POINT('Ctrl Pts',(-14.779464762608,1.92354282904339,4.5426939716314));
#47214=CARTESIAN_POINT('Ctrl Pts',(-14.6999188742349,0.419364192920443,
5.17961823885768));
#47215=CARTESIAN_POINT('Ctrl Pts',(-14.6203729858618,-1.43260365932953,
4.99519350795208));
#47216=CARTESIAN_POINT('Ctrl Pts',(-14.5408270974887,-2.78163379546954,
4.07413781835645));
#47217=CARTESIAN_POINT('Ctrl Pts',(-14.463498573627,-4.09305932865878,3.17875682095258));
#47218=CARTESIAN_POINT('Ctrl Pts',(-14.3861700497653,-4.92919541411866,
1.58724007886021));
#47219=CARTESIAN_POINT('Ctrl Pts',(-14.3088415259036,-4.93298263358733,
-0.000852151517113329));
#47220=CARTESIAN_POINT('Origin',(-14.75,0.,0.));
#47221=CARTESIAN_POINT('',(-12.5911584740964,-4.92478776395509,0.00455105250847659));
#47222=CARTESIAN_POINT('',(-12.8088415259036,-4.92377532403654,0.00452825219503028));
#47223=CARTESIAN_POINT('',(-14.75,-4.925,-6.03138548580071E-16));
#47224=CARTESIAN_POINT('Ctrl Pts',(-12.5911584740964,-4.92478776395509,
0.00455105250847659));
#47225=CARTESIAN_POINT('Ctrl Pts',(-12.6100377331706,-4.92837678960448,
0.393954978247036));
#47226=CARTESIAN_POINT('Ctrl Pts',(-12.6289169922448,-4.88609691325311,
0.78258860004133));
#47227=CARTESIAN_POINT('Ctrl Pts',(-12.647796251319,-4.79498154009321,1.15941392712904));
#47228=CARTESIAN_POINT('Ctrl Pts',(-12.7273421396921,-4.41107593903318,
2.74713012334508));
#47229=CARTESIAN_POINT('Ctrl Pts',(-12.8068880280651,-3.16020608534884,
4.12521664311483));
#47230=CARTESIAN_POINT('Ctrl Pts',(-12.8864339164382,-1.61697626926029,
4.66063046903576));
#47231=CARTESIAN_POINT('Ctrl Pts',(-12.9659798048113,-0.0737464531717311,
5.19604429495669));
#47232=CARTESIAN_POINT('Ctrl Pts',(-13.0455256931844,1.76184332532101,4.8887854270288));
#47233=CARTESIAN_POINT('Ctrl Pts',(-13.1250715815575,3.04658962766721,3.87999745680921));
#47234=CARTESIAN_POINT('Ctrl Pts',(-13.2046174699305,4.33133593001341,2.87120948658962));
#47235=CARTESIAN_POINT('Ctrl Pts',(-13.2841633583036,5.06523875621307,1.16089241407827));
#47236=CARTESIAN_POINT('Ctrl Pts',(-13.3637092466767,4.91116973811745,-0.465296064516709));
#47237=CARTESIAN_POINT('Ctrl Pts',(-13.4432551350498,4.75710072002183,-2.09148454311171));
#47238=CARTESIAN_POINT('Ctrl Pts',(-13.5228010234228,3.71505985763101,-3.63354442779033));
#47239=CARTESIAN_POINT('Ctrl Pts',(-13.6023469117959,2.26372296869752,-4.38310927826887));
#47240=CARTESIAN_POINT('Ctrl Pts',(-13.681892800169,0.812386079764056,-5.13267412874741));
#47241=CARTESIAN_POINT('Ctrl Pts',(-13.7614386885421,-1.0482468357121,-5.08974394502581));
#47242=CARTESIAN_POINT('Ctrl Pts',(-13.8409845769151,-2.46346842939373,
-4.27403929809212));
#47243=CARTESIAN_POINT('Ctrl Pts',(-13.9205304652882,-3.87869002307536,
-3.45833465115842));
#47244=CARTESIAN_POINT('Ctrl Pts',(-14.0000763536613,-4.84850029496252,
-1.86985554101265));
#47245=CARTESIAN_POINT('Ctrl Pts',(-14.0796222420344,-4.92740354357634,
-0.238291718292194));
#47246=CARTESIAN_POINT('Ctrl Pts',(-14.0834676527217,-4.93121788774538,
-0.159418591229293));
#47247=CARTESIAN_POINT('Ctrl Pts',(-14.0873130634091,-4.93295022404004,
-0.0804447772164642));
#47248=CARTESIAN_POINT('Ctrl Pts',(-14.0911584740964,-4.93264269199776,
-0.00145718338004752));
#47249=CARTESIAN_POINT('Ctrl Pts',(-14.3088415259036,-4.93298263358733,
-0.000852151517113329));
#47250=CARTESIAN_POINT('Ctrl Pts',(-14.3066241613922,-4.93309123059174,
-0.0463900614183807));
#47251=CARTESIAN_POINT('Ctrl Pts',(-14.3044067968809,-4.93251544314009,
-0.0919251555741316));
#47252=CARTESIAN_POINT('Ctrl Pts',(-14.3021894323695,-4.93124685277319,
-0.137440940316469));
#47253=CARTESIAN_POINT('Ctrl Pts',(-14.2226435439964,-4.88573735390672,
-1.77027736110802));
#47254=CARTESIAN_POINT('Ctrl Pts',(-14.1430976556234,-3.94862593614372,
-3.37826355440545));
#47255=CARTESIAN_POINT('Ctrl Pts',(-14.0635517672503,-2.55038763209838,
-4.22274892233722));
#47256=CARTESIAN_POINT('Ctrl Pts',(-13.9840058788772,-1.15214932805305,
-5.06723429026899));
#47257=CARTESIAN_POINT('Ctrl Pts',(-13.9044599905041,0.707215862274635,
-5.14821883283511));
#47258=CARTESIAN_POINT('Ctrl Pts',(-13.8249141021311,2.17358293754952,-4.42850118535088));
#47259=CARTESIAN_POINT('Ctrl Pts',(-13.745368213758,3.6399500128244,-3.70878353786665));
#47260=CARTESIAN_POINT('Ctrl Pts',(-13.6658223253849,4.71331897304647,-2.18836370033207));
#47261=CARTESIAN_POINT('Ctrl Pts',(-13.5862764370118,4.90062300737523,-0.565667459418628));
#47262=CARTESIAN_POINT('Ctrl Pts',(-13.5067305486388,5.08792704170398,1.05702878149484));
#47263=CARTESIAN_POINT('Ctrl Pts',(-13.4271846602657,4.38916615013937,2.78200142578717));
#47264=CARTESIAN_POINT('Ctrl Pts',(-13.3476387718926,3.12532576929452,3.81686053856362));
#47265=CARTESIAN_POINT('Ctrl Pts',(-13.2680928835195,1.86148538844969,4.85171965134006));
#47266=CARTESIAN_POINT('Ctrl Pts',(-13.1885469951465,0.0325655183246379,
5.19646523260064));
#47267=CARTESIAN_POINT('Ctrl Pts',(-13.1090011067734,-1.52129431677496,
4.69273365287321));
#47268=CARTESIAN_POINT('Ctrl Pts',(-13.0294552184003,-3.07515415187458,
4.18900207314577));
#47269=CARTESIAN_POINT('Ctrl Pts',(-12.9499093300272,-4.35395395194874,
2.8367933324303));
#47270=CARTESIAN_POINT('Ctrl Pts',(-12.8703634416541,-4.77025942134235,
1.25726313401576));
#47271=CARTESIAN_POINT('Ctrl Pts',(-12.849856136404,-4.87758493511541,0.850052798028952));
#47272=CARTESIAN_POINT('Ctrl Pts',(-12.8293488311538,-4.92758625344338,
0.427733934129015));
#47273=CARTESIAN_POINT('Ctrl Pts',(-12.8088415259036,-4.92377532403654,
0.00452825219503028));
#47274=CARTESIAN_POINT('Origin',(-14.75,0.,0.));
#47275=CARTESIAN_POINT('',(-11.0911584740964,-4.91693014897725,-0.000625914149278983));
#47276=CARTESIAN_POINT('',(-11.3088415259036,-4.91711289028958,-0.00117313378838655));
#47277=CARTESIAN_POINT('',(-14.75,-4.925,-6.03138548580071E-16));
#47278=CARTESIAN_POINT('Ctrl Pts',(-11.0911584740964,-4.91693014897725,
-0.000625914149278983));
#47279=CARTESIAN_POINT('Ctrl Pts',(-11.1327624029322,-4.91595655984975,
0.8609597041095));
#47280=CARTESIAN_POINT('Ctrl Pts',(-11.1743663317679,-4.70077081773724,
1.72300021548812));
#47281=CARTESIAN_POINT('Ctrl Pts',(-11.2159702606036,-4.27418701974417,
2.46321211926741));
#47282=CARTESIAN_POINT('Ctrl Pts',(-11.2955161489767,-3.45856724232153,
3.87848262660126));
#47283=CARTESIAN_POINT('Ctrl Pts',(-11.3750620373498,-1.87014629263889,
4.84838815470011));
#47284=CARTESIAN_POINT('Ctrl Pts',(-11.4546079257229,-0.238587204524135,
4.92738924483267));
#47285=CARTESIAN_POINT('Ctrl Pts',(-11.5341538140959,1.39297188359064,5.00639033496524));
#47286=CARTESIAN_POINT('Ctrl Pts',(-11.613699702469,3.06766911013748,4.19448698713153));
#47287=CARTESIAN_POINT('Ctrl Pts',(-11.6932455908421,4.01620924559344,2.86463818306347));
#47288=CARTESIAN_POINT('Ctrl Pts',(-11.7727914792152,4.96474938104939,1.53478937899541));
#47289=CARTESIAN_POINT('Ctrl Pts',(-11.8523373675882,5.18713242541439,-0.313004881306989));
#47290=CARTESIAN_POINT('Ctrl Pts',(-11.9318832559613,4.58120366532001,-1.82993486253306));
#47291=CARTESIAN_POINT('Ctrl Pts',(-12.0114291443344,3.97527490522564,-3.34686484375911));
#47292=CARTESIAN_POINT('Ctrl Pts',(-12.0909750327075,2.54103434067188,-4.53293054590886));
#47293=CARTESIAN_POINT('Ctrl Pts',(-12.1705209210806,0.937320122704561,
-4.84329635804258));
#47294=CARTESIAN_POINT('Ctrl Pts',(-12.2500668094536,-0.666394095262762,
-5.1536621701763));
#47295=CARTESIAN_POINT('Ctrl Pts',(-12.3296126978267,-2.43958196664368,
-4.588328092294));
#47296=CARTESIAN_POINT('Ctrl Pts',(-12.4091585861998,-3.56770522811629,
-3.4069881170217));
#47297=CARTESIAN_POINT('Ctrl Pts',(-12.4698252154987,-4.42808201322696,
-2.50602496453717));
#47298=CARTESIAN_POINT('Ctrl Pts',(-12.5304918447975,-4.91325478547539,
-1.24675989764379));
#47299=CARTESIAN_POINT('Ctrl Pts',(-12.5911584740964,-4.92478776395509,
0.00455105250847659));
#47300=CARTESIAN_POINT('Ctrl Pts',(-12.8088415259036,-4.92377532403654,
0.00452825219503028));
#47301=CARTESIAN_POINT('Ctrl Pts',(-12.7498029427807,-4.91280402040514,
-1.21384069126802));
#47302=CARTESIAN_POINT('Ctrl Pts',(-12.6907643596578,-4.45583175677877,
-2.43955966583319));
#47303=CARTESIAN_POINT('Ctrl Pts',(-12.6317257765349,-3.63665583438227,
-3.33328964797749));
#47304=CARTESIAN_POINT('Ctrl Pts',(-12.5521798881619,-2.53293563931553,
-4.53746057544264));
#47305=CARTESIAN_POINT('Ctrl Pts',(-12.4726339997888,-0.771684110468958,
-5.13895077425935));
#47306=CARTESIAN_POINT('Ctrl Pts',(-12.3930881114157,0.838043612127357,
-4.86145743982533));
#47307=CARTESIAN_POINT('Ctrl Pts',(-12.3135422230426,2.44777133472372,-4.58396410539131));
#47308=CARTESIAN_POINT('Ctrl Pts',(-12.2339963346695,3.90597525106984,-3.42748723770652));
#47309=CARTESIAN_POINT('Ctrl Pts',(-12.1544504462965,4.54280931452835,-1.92327040919758));
#47310=CARTESIAN_POINT('Ctrl Pts',(-12.0749045579234,5.17964337798684,-0.419053580688679));
#47311=CARTESIAN_POINT('Ctrl Pts',(-11.9953586695503,4.99510758855781,1.43290320864429));
#47312=CARTESIAN_POINT('Ctrl Pts',(-11.9158127811772,4.07397100194497,2.78187810846774));
#47313=CARTESIAN_POINT('Ctrl Pts',(-11.8362668928042,3.15283441533213,4.13085300829118));
#47314=CARTESIAN_POINT('Ctrl Pts',(-11.7567210044311,1.49509703153545,4.97684601860504));
#47315=CARTESIAN_POINT('Ctrl Pts',(-11.677175116058,-0.137736657205341,
4.93123860184462));
#47316=CARTESIAN_POINT('Ctrl Pts',(-11.5976292276849,-1.77057034594614,
4.88563118508419));
#47317=CARTESIAN_POINT('Ctrl Pts',(-11.5180833393119,-3.37850033963107,
3.94842334124948));
#47318=CARTESIAN_POINT('Ctrl Pts',(-11.4385374509388,-4.22290185645441,
2.55013439759839));
#47319=CARTESIAN_POINT('Ctrl Pts',(-11.3953054759271,-4.68182117990154,
1.79018572008053));
#47320=CARTESIAN_POINT('Ctrl Pts',(-11.3520735009153,-4.91521278868756,
0.894044916314203));
#47321=CARTESIAN_POINT('Ctrl Pts',(-11.3088415259036,-4.91711289028958,
-0.00117313378838655));
#47322=CARTESIAN_POINT('Origin',(-14.75,0.,0.));
#47323=CARTESIAN_POINT('',(-9.59115847409641,-4.92709248349153,-0.00433039759252629));
#47324=CARTESIAN_POINT('',(-9.80884152590359,-4.92809314710804,-0.00411155299795817));
#47325=CARTESIAN_POINT('',(-14.75,-4.925,-6.03138548580071E-16));
#47326=CARTESIAN_POINT('Ctrl Pts',(-9.59115847409641,-4.92709248349153,
-0.00433039759252629));
#47327=CARTESIAN_POINT('Ctrl Pts',(-9.6554870726937,-4.91489864183716,1.32092114795559));
#47328=CARTESIAN_POINT('Ctrl Pts',(-9.71981567129099,-4.36249459000914,
2.65513262914084));
#47329=CARTESIAN_POINT('Ctrl Pts',(-9.78414426988828,-3.40720205913308,
3.56750091135165));
#47330=CARTESIAN_POINT('Ctrl Pts',(-9.86369015826136,-2.2259297373092,4.69569501342137));
#47331=CARTESIAN_POINT('Ctrl Pts',(-9.94323604663443,-0.428612835952052,
5.17886144739986));
#47332=CARTESIAN_POINT('Ctrl Pts',(-10.0227819350075,1.15912637946997,4.79505105923515));
#47333=CARTESIAN_POINT('Ctrl Pts',(-10.1023278233806,2.74686559489197,4.41124067107045));
#47334=CARTESIAN_POINT('Ctrl Pts',(-10.1818737117537,4.12502712437884,3.16045346076258));
#47335=CARTESIAN_POINT('Ctrl Pts',(-10.2614196001267,4.66053349378172,1.61725575515876));
#47336=CARTESIAN_POINT('Ctrl Pts',(-10.3409654884998,5.19603986318461,0.0740580495549087));
#47337=CARTESIAN_POINT('Ctrl Pts',(-10.4205113768729,4.88889107250348,-1.76155015134491));
#47338=CARTESIAN_POINT('Ctrl Pts',(-10.500057265246,3.88018014779652,-3.04635694640356));
#47339=CARTESIAN_POINT('Ctrl Pts',(-10.579603153619,2.87146922308957,-4.3311637414622));
#47340=CARTESIAN_POINT('Ctrl Pts',(-10.6591490419921,1.16119616435681,-5.06516913067968));
#47341=CARTESIAN_POINT('Ctrl Pts',(-10.7386949303652,-0.465001550528919,
-4.91119763217294));
#47342=CARTESIAN_POINT('Ctrl Pts',(-10.8182408187383,-2.09119926541465,
-4.75722613366619));
#47343=CARTESIAN_POINT('Ctrl Pts',(-10.8977867071114,-3.63332163645336,
-3.71527774743521));
#47344=CARTESIAN_POINT('Ctrl Pts',(-10.9773325954844,-4.3829735193914,-2.26398581103529));
#47345=CARTESIAN_POINT('Ctrl Pts',(-11.0152745550218,-4.74054399840997,
-1.5717456330203));
#47346=CARTESIAN_POINT('Ctrl Pts',(-11.0532165145591,-4.91781804298907,
-0.786374942684098));
#47347=CARTESIAN_POINT('Ctrl Pts',(-11.0911584740964,-4.91693014897725,
-0.000625914149278983));
#47348=CARTESIAN_POINT('Ctrl Pts',(-11.3088415259036,-4.91711289028958,
-0.00117313378838655));
#47349=CARTESIAN_POINT('Ctrl Pts',(-11.2725276125423,-4.91870893407279,
-0.753136714034694));
#47350=CARTESIAN_POINT('Ctrl Pts',(-11.2362136991809,-4.7569730771308,-1.5044492332048));
#47351=CARTESIAN_POINT('Ctrl Pts',(-11.1998997858196,-4.42837083191147,
-2.1738485021124));
#47352=CARTESIAN_POINT('Ctrl Pts',(-11.1203538974465,-3.70856525058346,
-3.64017241470453));
#47353=CARTESIAN_POINT('Ctrl Pts',(-11.0408080090734,-2.18808104796575,
-4.71345019642131));
#47354=CARTESIAN_POINT('Ctrl Pts',(-10.9612621207003,-0.565373577716975,
-4.90065692052403));
#47355=CARTESIAN_POINT('Ctrl Pts',(-10.8817162323273,1.05733389253182,-5.08786364462675));
#47356=CARTESIAN_POINT('Ctrl Pts',(-10.8021703439542,2.78226463041168,-4.38899931111538));
#47357=CARTESIAN_POINT('Ctrl Pts',(-10.7226244555811,3.81704795131542,-3.12509687408555));
#47358=CARTESIAN_POINT('Ctrl Pts',(-10.643078567208,4.85183127221915,-1.86119443705574));
#47359=CARTESIAN_POINT('Ctrl Pts',(-10.563532678835,5.1964671761468,-0.0322538965074959));
#47360=CARTESIAN_POINT('Ctrl Pts',(-10.4839867904619,4.6926424154192,1.52157572801001));
#47361=CARTESIAN_POINT('Ctrl Pts',(-10.4044409020888,4.1888176546916,3.07540535252754));
#47362=CARTESIAN_POINT('Ctrl Pts',(-10.3248950137157,2.83653222930873,4.35412406101433));
#47363=CARTESIAN_POINT('Ctrl Pts',(-10.2453491253427,1.25697706871738,4.77033480835247));
#47364=CARTESIAN_POINT('Ctrl Pts',(-10.1658032369696,-0.322578091873937,
5.1865455556906));
#47365=CARTESIAN_POINT('Ctrl Pts',(-10.0862573485965,-2.12940298767373,
4.74024834188012));
#47366=CARTESIAN_POINT('Ctrl Pts',(-10.0067114602234,-3.33350772505308,
3.6364559370453));
#47367=CARTESIAN_POINT('Ctrl Pts',(-9.94075481545016,-4.33190890024233,
2.72123020963015));
#47368=CARTESIAN_POINT('Ctrl Pts',(-9.87479817067687,-4.91593144188893,
1.35396723904141));
#47369=CARTESIAN_POINT('Ctrl Pts',(-9.80884152590359,-4.92809314710804,
-0.00411155299795817));
#47370=CARTESIAN_POINT('Origin',(-14.75,0.,0.));
#47371=CARTESIAN_POINT('',(-8.09115847409641,-4.93134763236354,0.00268789096151988));
#47372=CARTESIAN_POINT('',(-8.3088415259036,-4.93058250867777,0.00315514943839852));
#47373=CARTESIAN_POINT('',(-14.75,-4.925,-6.03138548580071E-16));
#47374=CARTESIAN_POINT('Ctrl Pts',(-8.09115847409641,-4.93134763236354,
0.00268789096151988));
#47375=CARTESIAN_POINT('Ctrl Pts',(-8.09866585408217,-4.93236070319556,
0.157002391239283));
#47376=CARTESIAN_POINT('Ctrl Pts',(-8.10617323406794,-4.92574782328456,
0.311228913952019));
#47377=CARTESIAN_POINT('Ctrl Pts',(-8.11368061405371,-4.91122550856618,
0.464707034867637));
#47378=CARTESIAN_POINT('Ctrl Pts',(-8.19322650242678,-4.7573515302013,2.09091398019483));
#47379=CARTESIAN_POINT('Ctrl Pts',(-8.27277239079985,-3.71549562387871,
3.63309883205044));
#47380=CARTESIAN_POINT('Ctrl Pts',(-8.35231827917293,-2.2642486452318,4.38283774475274));
#47381=CARTESIAN_POINT('Ctrl Pts',(-8.431864167546,-0.813001666584828,5.13257665745506));
#47382=CARTESIAN_POINT('Ctrl Pts',(-8.51141005591908,1.0476363843865,5.089869631004));
#47383=CARTESIAN_POINT('Ctrl Pts',(-8.59095594429216,2.46295580028325,4.27433472602514));
#47384=CARTESIAN_POINT('Ctrl Pts',(-8.67050183266523,3.87827521617993,3.45879982104632));
#47385=CARTESIAN_POINT('Ctrl Pts',(-8.75004772103831,4.84827599700209,1.87043703753978));
#47386=CARTESIAN_POINT('Ctrl Pts',(-8.82959360941138,4.9273749283692,0.238882689898267));
#47387=CARTESIAN_POINT('Ctrl Pts',(-8.90913949778446,5.0064738597363,-1.39267165774325));
#47388=CARTESIAN_POINT('Ctrl Pts',(-8.98868538615753,4.19467094164835,-3.06741756951973));
#47389=CARTESIAN_POINT('Ctrl Pts',(-9.0682312745306,2.86487902205042,-4.01603745167696));
#47390=CARTESIAN_POINT('Ctrl Pts',(-9.14777716290368,1.53508710245243,-4.96465733383422));
#47391=CARTESIAN_POINT('Ctrl Pts',(-9.22732305127675,-0.312693818655589,
-5.18715118637216));
#47392=CARTESIAN_POINT('Ctrl Pts',(-9.30686893964983,-1.82966013350537,
-4.58131339466273));
#47393=CARTESIAN_POINT('Ctrl Pts',(-9.38641482802291,-3.3466264483551,-3.97547560295332));
#47394=CARTESIAN_POINT('Ctrl Pts',(-9.46596071639599,-4.53277815694662,
-2.54130616699661));
#47395=CARTESIAN_POINT('Ctrl Pts',(-9.54550660476906,-4.84324014009708,
-0.937610563937788));
#47396=CARTESIAN_POINT('Ctrl Pts',(-9.56072389454484,-4.9026321471334,-0.630820342557176));
#47397=CARTESIAN_POINT('Ctrl Pts',(-9.57594118432063,-4.9299770049327,-0.317826062571257));
#47398=CARTESIAN_POINT('Ctrl Pts',(-9.59115847409641,-4.92709248349153,
-0.00433039759252629));
#47399=CARTESIAN_POINT('Ctrl Pts',(-9.80884152590359,-4.92809314710804,
-0.00411155299795817));
#47400=CARTESIAN_POINT('Ctrl Pts',(-9.7952522823038,-4.93059885938888,-0.283920563844114));
#47401=CARTESIAN_POINT('Ctrl Pts',(-9.781663038704,-4.90882931597747,-0.563339710114124));
#47402=CARTESIAN_POINT('Ctrl Pts',(-9.7680737951042,-4.86140717526349,-0.838335142623281));
#47403=CARTESIAN_POINT('Ctrl Pts',(-9.68852790673113,-4.58381730913562,
-2.44804622159789));
#47404=CARTESIAN_POINT('Ctrl Pts',(-9.60898201835805,-3.42725299792094,
-3.90618078368793));
#47405=CARTESIAN_POINT('Ctrl Pts',(-9.52943612998497,-1.9229979824355,-4.54292464108855));
#47406=CARTESIAN_POINT('Ctrl Pts',(-9.4498902416119,-0.418742966950077,
-5.17966849848915));
#47407=CARTESIAN_POINT('Ctrl Pts',(-9.37034435323882,1.43320275280612,-4.99502165120035));
#47408=CARTESIAN_POINT('Ctrl Pts',(-9.29079846486575,2.78212241146185,-4.07380417088284));
#47409=CARTESIAN_POINT('Ctrl Pts',(-9.21125257649268,4.1310420701176,-3.15258669056531));
#47410=CARTESIAN_POINT('Ctrl Pts',(-9.13170668811961,4.97693566767287,-1.49479857721911));
#47411=CARTESIAN_POINT('Ctrl Pts',(-9.05216079974653,4.93123033318249,0.138032373598989));
#47412=CARTESIAN_POINT('Ctrl Pts',(-8.97261491137345,4.8855249986921,1.77086332441709));
#47413=CARTESIAN_POINT('Ctrl Pts',(-8.89306902300037,3.94822073215603,3.37873711270705));
#47414=CARTESIAN_POINT('Ctrl Pts',(-8.8135231346273,2.54988115392759,4.22305477538536));
#47415=CARTESIAN_POINT('Ctrl Pts',(-8.73397724625422,1.15154157569918,5.06737243806365));
#47416=CARTESIAN_POINT('Ctrl Pts',(-8.65443135788115,-0.707833314221602,
5.14813397513033));
#47417=CARTESIAN_POINT('Ctrl Pts',(-8.57488546950808,-2.17411405885781,
4.428240462547));
#47418=CARTESIAN_POINT('Ctrl Pts',(-8.495339581135,-3.64039480349401,3.70834694996368));
#47419=CARTESIAN_POINT('Ctrl Pts',(-8.41579369276192,-4.71358140284566,
2.18779838773033));
#47420=CARTESIAN_POINT('Ctrl Pts',(-8.33624780438885,-4.90069081604919,
0.565079693981939));
#47421=CARTESIAN_POINT('Ctrl Pts',(-8.3271123782271,-4.92217934629819,0.378719001918263));
#47422=CARTESIAN_POINT('Ctrl Pts',(-8.31797695206535,-4.93198112784769,
0.191010756085821));
#47423=CARTESIAN_POINT('Ctrl Pts',(-8.3088415259036,-4.93058250867777,0.00315514943839852));
#47424=CARTESIAN_POINT('Origin',(-14.75,0.,0.));
#47425=CARTESIAN_POINT('',(-6.5911584740964,-4.91874206214364,0.00300395193210873));
#47426=CARTESIAN_POINT('',(-6.8088415259036,-4.91816702752264,0.00255975366377111));
#47427=CARTESIAN_POINT('',(-14.75,-4.925,-6.03138548580071E-16));
#47428=CARTESIAN_POINT('Ctrl Pts',(-6.5911584740964,-4.91874206214364,0.00300395193210873));
#47429=CARTESIAN_POINT('Ctrl Pts',(-6.62139052384371,-4.92221047690888,
0.628510441243254));
#47430=CARTESIAN_POINT('Ctrl Pts',(-6.65162257359103,-4.81164202146414,
1.2528364358832));
#47431=CARTESIAN_POINT('Ctrl Pts',(-6.68185462333834,-4.5814231074921,1.8293853978311));
#47432=CARTESIAN_POINT('Ctrl Pts',(-6.76140051171141,-3.97567628631209,
3.34638804078933));
#47433=CARTESIAN_POINT('Ctrl Pts',(-6.84094640008449,-2.54157798418442,
4.53262575168735));
#47434=CARTESIAN_POINT('Ctrl Pts',(-6.92049228845757,-0.937901001819111,
4.8431839047693));
#47435=CARTESIAN_POINT('Ctrl Pts',(-7.00003817683064,0.665775980546221,
5.15374205785124));
#47436=CARTESIAN_POINT('Ctrl Pts',(-7.07958406520371,2.43903164314918,4.58862065311707));
#47437=CARTESIAN_POINT('Ctrl Pts',(-7.15912995357679,3.5672965817681,3.40741598897341));
#47438=CARTESIAN_POINT('Ctrl Pts',(-7.23867584194987,4.69556152038701,2.22621132482977));
#47439=CARTESIAN_POINT('Ctrl Pts',(-7.31822173032295,5.17883573502188,0.428923401276672));
#47440=CARTESIAN_POINT('Ctrl Pts',(-7.39776761869602,4.79512056112791,-1.15883882763304));
#47441=CARTESIAN_POINT('Ctrl Pts',(-7.4773135070691,4.41140538723394,-2.74660105654276));
#47442=CARTESIAN_POINT('Ctrl Pts',(-7.55685939544217,3.16070082481106,-4.12483759080913));
#47443=CARTESIAN_POINT('Ctrl Pts',(-7.63640528381525,1.61753523524406,-4.66043650177258));
#47444=CARTESIAN_POINT('Ctrl Pts',(-7.71595117218832,0.0743696456770546,
-5.19603541273603));
#47445=CARTESIAN_POINT('Ctrl Pts',(-7.7954970605614,-1.76125697103409,-4.88899670039663));
#47446=CARTESIAN_POINT('Ctrl Pts',(-7.87504294893448,-3.04612425418612,
-3.88036282482753));
#47447=CARTESIAN_POINT('Ctrl Pts',(-7.94708145732179,-4.20972836304737,
-2.96692177349214));
#47448=CARTESIAN_POINT('Ctrl Pts',(-8.0191199657091,-4.92162651637264,-1.47806657246253));
#47449=CARTESIAN_POINT('Ctrl Pts',(-8.09115847409641,-4.93134763236354,
0.00268789096151988));
#47450=CARTESIAN_POINT('Ctrl Pts',(-8.3088415259036,-4.93058250867777,0.00315514943839852));
#47451=CARTESIAN_POINT('Ctrl Pts',(-8.23843106369227,-4.91980277925207,
-1.44472476977317));
#47452=CARTESIAN_POINT('Ctrl Pts',(-8.16802060148095,-4.24367279446414,
-2.90135853255996));
#47453=CARTESIAN_POINT('Ctrl Pts',(-8.09761013926962,-3.12486796763837,
-3.8172353503401));
#47454=CARTESIAN_POINT('Ctrl Pts',(-8.01806425089654,-1.86090347896865,
-4.85194287565023));
#47455=CARTESIAN_POINT('Ctrl Pts',(-7.93851836252347,-0.0319422745738374,
-5.19646910100704));
#47456=CARTESIAN_POINT('Ctrl Pts',(-7.85897247415039,1.52185713377351,-4.69255116109043));
#47457=CARTESIAN_POINT('Ctrl Pts',(-7.77942658577732,3.07565654212083,-4.18863322117384));
#47458=CARTESIAN_POINT('Ctrl Pts',(-7.69988069740424,4.35429415442072,-2.83627111598379));
#47459=CARTESIAN_POINT('Ctrl Pts',(-7.62033480903117,4.77041017820713,-1.25669099889733));
#47460=CARTESIAN_POINT('Ctrl Pts',(-7.54078892065809,5.18652620199355,0.322889118189166));
#47461=CARTESIAN_POINT('Ctrl Pts',(-7.46124303228501,4.7401206372665,2.12968724717213));
#47462=CARTESIAN_POINT('Ctrl Pts',(-7.38169714391194,3.63625602663207,3.33372579013805));
#47463=CARTESIAN_POINT('Ctrl Pts',(-7.30215125553886,2.53239141599764,4.53776433310397));
#47464=CARTESIAN_POINT('Ctrl Pts',(-7.22260536716579,0.771067759455849,
5.13904329005283));
#47465=CARTESIAN_POINT('Ctrl Pts',(-7.14305947879271,-0.838626670106471,
4.86135689322456));
#47466=CARTESIAN_POINT('Ctrl Pts',(-7.06351359041964,-2.44832109966874,
4.58367049639629));
#47467=CARTESIAN_POINT('Ctrl Pts',(-6.98396770204656,-3.90638630225154,
3.42701874579095));
#47468=CARTESIAN_POINT('Ctrl Pts',(-6.90442181367349,-4.54303995130782,
1.92272554874775));
#47469=CARTESIAN_POINT('Ctrl Pts',(-6.87256171775019,-4.79803548588176,
1.32021891346095));
#47470=CARTESIAN_POINT('Ctrl Pts',(-6.8407016218269,-4.92126012648956,0.661943615096396));
#47471=CARTESIAN_POINT('Ctrl Pts',(-6.8088415259036,-4.91816702752264,0.00255975366377111));
#47472=CARTESIAN_POINT('Origin',(-14.75,0.,0.));
#47473=CARTESIAN_POINT('',(-5.0911584740964,-4.92034850444268,-0.00382654489779644));
#47474=CARTESIAN_POINT('',(-5.30884152590359,-4.92118977299025,-0.00410386901592228));
#47475=CARTESIAN_POINT('',(-14.75,-4.925,-6.03138548580071E-16));
#47476=CARTESIAN_POINT('Ctrl Pts',(-5.0911584740964,-4.92034850444268,-0.00382654489779644));
#47477=CARTESIAN_POINT('Ctrl Pts',(-5.14411519360526,-4.91244809502025,
1.09095932864311));
#47478=CARTESIAN_POINT('Ctrl Pts',(-5.19707191311412,-4.55198007497204,
2.19046632634003));
#47479=CARTESIAN_POINT('Ctrl Pts',(-5.25002863262299,-3.88054548599257,
3.0458915476704));
#47480=CARTESIAN_POINT('Ctrl Pts',(-5.32957452099606,-2.87198866147391,
4.3308193112958));
#47481=CARTESIAN_POINT('Ctrl Pts',(-5.40912040936913,-1.16180365248812,
5.06502982514693));
#47482=CARTESIAN_POINT('Ctrl Pts',(-5.4886662977422,0.464412516539281,4.91125336903979));
#47483=CARTESIAN_POINT('Ctrl Pts',(-5.56821218611528,2.09062868556668,4.75747691293265));
#47484=CARTESIAN_POINT('Ctrl Pts',(-5.64775807448836,3.63287601463573,3.71571348686722));
#47485=CARTESIAN_POINT('Ctrl Pts',(-5.72730396286143,4.38270195487139,2.26451147037829));
#47486=CARTESIAN_POINT('Ctrl Pts',(-5.80684985123451,5.13252789510707,0.813309453889311));
#47487=CARTESIAN_POINT('Ctrl Pts',(-5.88639573960759,5.08993244650934,-1.04733115302316));
#47488=CARTESIAN_POINT('Ctrl Pts',(-5.96594162798066,4.27448241666476,-2.46269947196908));
#47489=CARTESIAN_POINT('Ctrl Pts',(-6.04548751635374,3.45903238682021,-3.87806779091495));
#47490=CARTESIAN_POINT('Ctrl Pts',(-6.12503340472681,1.87072777572881,-4.84816382189425));
#47491=CARTESIAN_POINT('Ctrl Pts',(-6.20457929309989,0.239178174554097,
-4.92736059443231));
#47492=CARTESIAN_POINT('Ctrl Pts',(-6.28412518147296,-1.39237142662062,
-5.00655736697037));
#47493=CARTESIAN_POINT('Ctrl Pts',(-6.36367106984604,-3.06716601787869,
-4.19485488106719));
#47494=CARTESIAN_POINT('Ctrl Pts',(-6.44321695821912,-4.01586564339155,
-2.86511985060641));
#47495=CARTESIAN_POINT('Ctrl Pts',(-6.49253079684488,-4.604004404473,-2.04076123134479));
#47496=CARTESIAN_POINT('Ctrl Pts',(-6.54184463547064,-4.91308446209832,
-1.01730814503372));
#47497=CARTESIAN_POINT('Ctrl Pts',(-6.5911584740964,-4.91874206214364,0.00300395193210873));
#47498=CARTESIAN_POINT('Ctrl Pts',(-6.8088415259036,-4.91816702752264,0.00255975366377111));
#47499=CARTESIAN_POINT('Ctrl Pts',(-6.76115573345382,-4.91353750990542,
-0.984356357220146));
#47500=CARTESIAN_POINT('Ctrl Pts',(-6.71346994100404,-4.62593290938502,
-1.97375585426302));
#47501=CARTESIAN_POINT('Ctrl Pts',(-6.66578414855426,-4.07363732517796,
-2.78236670443132));
#47502=CARTESIAN_POINT('Ctrl Pts',(-6.58623826018119,-3.15233895446205,
-4.13123111708606));
#47503=CARTESIAN_POINT('Ctrl Pts',(-6.5066923718081,-1.49450011750048,-4.97702529891446));
#47504=CARTESIAN_POINT('Ctrl Pts',(-6.42714648343503,0.138328089510376,
-4.93122204682461));
#47505=CARTESIAN_POINT('Ctrl Pts',(-6.34760059506195,1.77115629652118,-4.88541879473476));
#47506=CARTESIAN_POINT('Ctrl Pts',(-6.26805470668888,3.37897387358129,-3.94801810872673));
#47507=CARTESIAN_POINT('Ctrl Pts',(-6.18850881831581,4.22320767910246,-2.54962790101466));
#47508=CARTESIAN_POINT('Ctrl Pts',(-6.10896292994273,5.06744148462366,-1.15123769330255));
#47509=CARTESIAN_POINT('Ctrl Pts',(-6.02941704156966,5.14809151860588,0.708142036113649));
#47510=CARTESIAN_POINT('Ctrl Pts',(-5.94987115319658,4.42811007730965,2.17437960764566));
#47511=CARTESIAN_POINT('Ctrl Pts',(-5.8703252648235,3.70812863601341,3.64061717917766));
#47512=CARTESIAN_POINT('Ctrl Pts',(-5.79077937645043,2.18751571943878,4.71371259282546));
#47513=CARTESIAN_POINT('Ctrl Pts',(-5.71123348807735,0.564785808115402,
4.9007246942176));
#47514=CARTESIAN_POINT('Ctrl Pts',(-5.63168759970428,-1.05794410320798,
5.08773679560975));
#47515=CARTESIAN_POINT('Ctrl Pts',(-5.5521417113312,-2.78279100928007,4.38866558474619));
#47516=CARTESIAN_POINT('Ctrl Pts',(-5.47259582295812,-3.81742273544663,
3.1246390494413));
#47517=CARTESIAN_POINT('Ctrl Pts',(-5.41801105727328,-4.5273919305612,2.25725804886157));
#47518=CARTESIAN_POINT('Ctrl Pts',(-5.36342629158844,-4.9123547098068,1.12385261058705));
#47519=CARTESIAN_POINT('Ctrl Pts',(-5.30884152590359,-4.92118977299025,
-0.00410386901592228));
#47520=CARTESIAN_POINT('Origin',(-14.75,0.,0.));
#47521=CARTESIAN_POINT('',(-3.5911584740964,-4.93263795678916,-0.00146375725000258));
#47522=CARTESIAN_POINT('',(-3.80884152590359,-4.93297963225018,-0.000859328946059894));
#47523=CARTESIAN_POINT('',(-14.75,-4.925,-6.03138548580071E-16));
#47524=CARTESIAN_POINT('Ctrl Pts',(-3.5911584740964,-4.93263795678916,-0.00146375725000258));
#47525=CARTESIAN_POINT('Ctrl Pts',(-3.66683986336681,-4.9265598841513,1.55309257837791));
#47526=CARTESIAN_POINT('Ctrl Pts',(-3.74252125263721,-4.13044035554753,
3.11300803879703));
#47527=CARTESIAN_POINT('Ctrl Pts',(-3.81820264190762,-2.8653605731944,4.01569365331712));
#47528=CARTESIAN_POINT('Ctrl Pts',(-3.8977485302807,-1.53568235084381,4.96447286866741));
#47529=CARTESIAN_POINT('Ctrl Pts',(-3.97729441865377,0.31207168483266,5.18718866129924));
#47530=CARTESIAN_POINT('Ctrl Pts',(-4.05684030702685,1.82911060574424,4.58153289102084));
#47531=CARTESIAN_POINT('Ctrl Pts',(-4.13638619539992,3.34614952665579,3.97587712074245));
#47532=CARTESIAN_POINT('Ctrl Pts',(-4.215932083773,4.53247333280247,2.54184978755386));
#47533=CARTESIAN_POINT('Ctrl Pts',(-4.29547797214607,4.84312767798418,0.938191390916231));
#47534=CARTESIAN_POINT('Ctrl Pts',(-4.37502386051915,5.15378202316589,-0.665467005721419));
#47535=CARTESIAN_POINT('Ctrl Pts',(-4.45456974889223,4.58876690738262,-2.43875646580811));
#47536=CARTESIAN_POINT('Ctrl Pts',(-4.53411563726531,3.40762989303727,-3.56709221570014));
#47537=CARTESIAN_POINT('Ctrl Pts',(-4.61366152563838,2.22649287869195,-4.69542796559215));
#47538=CARTESIAN_POINT('Ctrl Pts',(-4.69320741401145,0.429233965784571,
-5.17881000528951));
#47539=CARTESIAN_POINT('Ctrl Pts',(-4.77275330238453,-1.15855126458436,
-4.79519005809945));
#47540=CARTESIAN_POINT('Ctrl Pts',(-4.8522991907576,-2.74633649495327,-4.4115701109094));
#47541=CARTESIAN_POINT('Ctrl Pts',(-4.93184507913068,-4.12464804278375,
-3.16094817683195));
#47542=CARTESIAN_POINT('Ctrl Pts',(-5.01139096750375,-4.66033949667325,
-1.6178147030934));
#47543=CARTESIAN_POINT('Ctrl Pts',(-5.03798013636797,-4.83940080100846,
-1.10200380007321));
#47544=CARTESIAN_POINT('Ctrl Pts',(-5.06456930523218,-4.92431524033904,
-0.553510262690519));
#47545=CARTESIAN_POINT('Ctrl Pts',(-5.0911584740964,-4.92034850444268,-0.00382654489779644));
#47546=CARTESIAN_POINT('Ctrl Pts',(-5.30884152590359,-4.92118977299025,
-0.00410386901592228));
#47547=CARTESIAN_POINT('Ctrl Pts',(-5.28388040321536,-4.92522996796614,
-0.519908227999806));
#47548=CARTESIAN_POINT('Ctrl Pts',(-5.25891928052713,-4.85061618972318,
-1.03457312761624));
#47549=CARTESIAN_POINT('Ctrl Pts',(-5.2339581578389,-4.69245989025258,-1.52213853308082));
#47550=CARTESIAN_POINT('Ctrl Pts',(-5.15441226946583,-4.18844877263093,
-3.07590772055185));
#47551=CARTESIAN_POINT('Ctrl Pts',(-5.07486638109275,-2.83600999112659,
-4.35446423574767));
#47552=CARTESIAN_POINT('Ctrl Pts',(-4.99532049271967,-1.25640492385531,
-4.77048553279394));
#47553=CARTESIAN_POINT('Ctrl Pts',(-4.9157746043466,0.323200143415984,-5.18650682984021));
#47554=CARTESIAN_POINT('Ctrl Pts',(-4.83622871597352,2.1299714964542,-4.73999290873692));
#47555=CARTESIAN_POINT('Ctrl Pts',(-4.75668282760045,3.33394384188576,-3.63605609952002));
#47556=CARTESIAN_POINT('Ctrl Pts',(-4.67713693922737,4.53791618731733,-2.53211929030309));
#47557=CARTESIAN_POINT('Ctrl Pts',(-4.5975910508543,5.13908952514219,-0.770759592972526));
#47558=CARTESIAN_POINT('Ctrl Pts',(-4.51804516248122,4.86130659629173,0.83891818762146));
#47559=CARTESIAN_POINT('Ctrl Pts',(-4.43849927410815,4.58352366744127,2.44859596821542));
#47560=CARTESIAN_POINT('Ctrl Pts',(-4.35895338573507,3.42678447191547,3.90659183207286));
#47561=CARTESIAN_POINT('Ctrl Pts',(-4.27940749736199,1.92245310317772,4.54315525853296));
#47562=CARTESIAN_POINT('Ctrl Pts',(-4.19986160898891,0.418121734439937,
5.17971868499307));
#47563=CARTESIAN_POINT('Ctrl Pts',(-4.12031572061584,-1.43380180750975,
4.99484967405592));
#47564=CARTESIAN_POINT('Ctrl Pts',(-4.04076983224277,-2.78261097786045,
4.07347043921392));
#47565=CARTESIAN_POINT('Ctrl Pts',(-3.96346039679638,-4.09349803459511,
3.17799601640553));
#47566=CARTESIAN_POINT('Ctrl Pts',(-3.88615096134998,-4.92916340173032,
1.58684352759606));
#47567=CARTESIAN_POINT('Ctrl Pts',(-3.80884152590359,-4.93297963225018,
-0.000859328946059894));
#47568=CARTESIAN_POINT('Origin',(-14.75,0.,0.));
#47569=CARTESIAN_POINT('',(-2.09115847409639,-4.92479967433243,0.00455076259524401));
#47570=CARTESIAN_POINT('',(-2.3088415259036,-4.92378694620037,0.00452865572044409));
#47571=CARTESIAN_POINT('',(-14.75,-4.925,-6.03138548580071E-16));
#47572=CARTESIAN_POINT('Ctrl Pts',(-2.09115847409639,-4.92479967433243,
0.00455076259524401));
#47573=CARTESIAN_POINT('Ctrl Pts',(-2.11001864475527,-4.92838960899571,
0.393565332838783));
#47574=CARTESIAN_POINT('Ctrl Pts',(-2.12887881541415,-4.8861997157664,0.781810208141141));
#47575=CARTESIAN_POINT('Ctrl Pts',(-2.14773898607303,-4.79526872833564,
1.15827977445631));
#47576=CARTESIAN_POINT('Ctrl Pts',(-2.22728487444611,-4.41175225297358,
2.74610242143037));
#47577=CARTESIAN_POINT('Ctrl Pts',(-2.30683076281919,-3.16119502426286,
4.12445761712042));
#47578=CARTESIAN_POINT('Ctrl Pts',(-2.38637665119226,-1.61808937757221,
4.66023409988841));
#47579=CARTESIAN_POINT('Ctrl Pts',(-2.46592253956534,-0.0749837308815521,
5.19601058265641));
#47580=CARTESIAN_POINT('Ctrl Pts',(-2.54546842793841,1.76067033378902,4.88920835250233));
#47581=CARTESIAN_POINT('Ctrl Pts',(-2.62501431631149,3.04565633625721,3.88073249588954));
#47582=CARTESIAN_POINT('Ctrl Pts',(-2.70456020468456,4.33064233872542,2.87225663927674));
#47583=CARTESIAN_POINT('Ctrl Pts',(-2.78410609305764,5.06496027899121,1.16210715620522));
#47584=CARTESIAN_POINT('Ctrl Pts',(-2.86365198143071,4.91128251100273,-0.464120269161797));
#47585=CARTESIAN_POINT('Ctrl Pts',(-2.94319786980379,4.75760474301426,-2.09034769452876));
#47586=CARTESIAN_POINT('Ctrl Pts',(-3.02274375817687,3.71593126677153,-3.63265306219127));
#47587=CARTESIAN_POINT('Ctrl Pts',(-3.10228964654994,2.26477361062453,-4.38256496537029));
#47588=CARTESIAN_POINT('Ctrl Pts',(-3.18183553492302,0.813615954477467,
-5.13247686854935));
#47589=CARTESIAN_POINT('Ctrl Pts',(-3.26138142329609,-1.04702588157384,
-5.08999530724491));
#47590=CARTESIAN_POINT('Ctrl Pts',(-3.34092731166917,-2.46244278226107,
-4.27463070863102));
#47591=CARTESIAN_POINT('Ctrl Pts',(-3.42047320004224,-3.87785968294825,
-3.45926611001717));
#47592=CARTESIAN_POINT('Ctrl Pts',(-3.50001908841532,-4.84805164827134,
-1.87101847409385));
#47593=CARTESIAN_POINT('Ctrl Pts',(-3.57956497678839,-4.92734642642051,
-0.239473337097873));
#47594=CARTESIAN_POINT('Ctrl Pts',(-3.58342947589106,-4.93119872608391,
-0.160209595792822));
#47595=CARTESIAN_POINT('Ctrl Pts',(-3.58729397499373,-4.93294831983193,
-0.0808436632215555));
#47596=CARTESIAN_POINT('Ctrl Pts',(-3.5911584740964,-4.93263795678916,-0.00146375725000258));
#47597=CARTESIAN_POINT('Ctrl Pts',(-3.80884152590359,-4.93297963225018,
-0.000859328946059894));
#47598=CARTESIAN_POINT('Ctrl Pts',(-3.80660507297691,-4.93309003041654,
-0.0467893332167884));
#47599=CARTESIAN_POINT('Ctrl Pts',(-3.80436862005022,-4.93250428457465,
-0.0927164506168972));
#47600=CARTESIAN_POINT('Ctrl Pts',(-3.80213216712354,-4.93121376103269,
-0.138623755771863));
#47601=CARTESIAN_POINT('Ctrl Pts',(-3.72258627875046,-4.8853125751026,-1.77144925716878));
#47602=CARTESIAN_POINT('Ctrl Pts',(-3.64304039037739,-3.94781540449082,
-3.37921080121581));
#47603=CARTESIAN_POINT('Ctrl Pts',(-3.56349450200431,-2.54937460381079,
-4.2233606619699));
#47604=CARTESIAN_POINT('Ctrl Pts',(-3.48394861363124,-1.15093380313076,
-5.06751052272398));
#47605=CARTESIAN_POINT('Ctrl Pts',(-3.40440272525816,0.708450627617543,
-5.14804870018514));
#47606=CARTESIAN_POINT('Ctrl Pts',(-3.32485683688509,2.17464508120495,-4.42797949508699));
#47607=CARTESIAN_POINT('Ctrl Pts',(-3.24531094851201,3.64083953479237,-3.70791028998884));
#47608=CARTESIAN_POINT('Ctrl Pts',(-3.16576506013894,4.71384401121892,-2.18723370233138));
#47609=CARTESIAN_POINT('Ctrl Pts',(-3.08621917176586,4.90075868413978,-0.564492267726287));
#47610=CARTESIAN_POINT('Ctrl Pts',(-3.00667328339279,5.08767335706064,1.05824916687883));
#47611=CARTESIAN_POINT('Ctrl Pts',(-2.92712739501971,4.38849822647583,2.78305544843154));
#47612=CARTESIAN_POINT('Ctrl Pts',(-2.84758150664664,3.12440987169467,3.8176107737941));
#47613=CARTESIAN_POINT('Ctrl Pts',(-2.76803561827356,1.86032151691353,4.85216609915665));
#47614=CARTESIAN_POINT('Ctrl Pts',(-2.68848972990048,0.0313199379360557,
5.19647046832902));
#47615=CARTESIAN_POINT('Ctrl Pts',(-2.60894384152741,-1.5224194503301,4.69236732243377));
#47616=CARTESIAN_POINT('Ctrl Pts',(-2.52939795315433,-3.07615883859628,
4.18826417653852));
#47617=CARTESIAN_POINT('Ctrl Pts',(-2.44985206478126,-4.35463603615115,
2.8357535155756));
#47618=CARTESIAN_POINT('Ctrl Pts',(-2.37030617640818,-4.77056178492771,
1.25612130118806));
#47619=CARTESIAN_POINT('Ctrl Pts',(-2.34981795957332,-4.87768959633853,
0.849263725144446));
#47620=CARTESIAN_POINT('Ctrl Pts',(-2.32932974273846,-4.92759608937386,
0.427338996020449));
#47621=CARTESIAN_POINT('Ctrl Pts',(-2.3088415259036,-4.92378694620037,0.00452865572044409));
#47622=CARTESIAN_POINT('Origin',(-14.75,0.,0.));
#47623=CARTESIAN_POINT('',(-0.591158474096391,-4.91621514884034,-0.00190685489401573));
#47624=CARTESIAN_POINT('',(-0.808841525903593,-4.91703434725887,-0.0013692803956027));
#47625=CARTESIAN_POINT('',(-14.75,-4.925,-6.03138548580071E-16));
#47626=CARTESIAN_POINT('Ctrl Pts',(-0.591158474096391,-4.91617236260859,
-0.00191614214703012));
#47627=CARTESIAN_POINT('Ctrl Pts',(-0.632743314516819,-4.91557730725517,
0.859927749670198));
#47628=CARTESIAN_POINT('Ctrl Pts',(-0.674328154937247,-4.70120063118156,
1.72260089528099));
#47629=CARTESIAN_POINT('Ctrl Pts',(-0.715912995357675,-4.27522171387068,
2.46297048332456));
#47630=CARTESIAN_POINT('Ctrl Pts',(-0.795458883730751,-3.46038459863554,
3.87919226053746));
#47631=CARTESIAN_POINT('Ctrl Pts',(-0.875004772103829,-1.87128956129306,
4.84790224489492));
#47632=CARTESIAN_POINT('Ctrl Pts',(-0.954550660476906,-0.23953077630217,
4.92691531448512));
#47633=CARTESIAN_POINT('Ctrl Pts',(-1.03409654884998,1.39222800868875,5.00592838407533));
#47634=CARTESIAN_POINT('Ctrl Pts',(-1.11364243722306,3.06665054132806,4.19524453889832));
#47635=CARTESIAN_POINT('Ctrl Pts',(-1.19318832559614,4.01539704249259,2.86581937781023));
#47636=CARTESIAN_POINT('Ctrl Pts',(-1.27273421396921,4.96414354365708,1.53639421672219));
#47637=CARTESIAN_POINT('Ctrl Pts',(-1.35228010234228,5.1872140133468,-0.311772260276884));
#47638=CARTESIAN_POINT('Ctrl Pts',(-1.43182599071535,4.58170765220235,-1.82894951483846));
#47639=CARTESIAN_POINT('Ctrl Pts',(-1.51137187908843,3.9762012910579,-3.34612676940009));
#47640=CARTESIAN_POINT('Ctrl Pts',(-1.59091776746151,2.54211809907922,-4.53231480152423));
#47641=CARTESIAN_POINT('Ctrl Pts',(-1.67046365583459,0.938447910619046,
-4.84301219015054));
#47642=CARTESIAN_POINT('Ctrl Pts',(-1.75000954420766,-0.665222277841155,
-5.15370957877686));
#47643=CARTESIAN_POINT('Ctrl Pts',(-1.82955543258074,-2.43847946278283,
-4.58891632390535));
#47644=CARTESIAN_POINT('Ctrl Pts',(-1.90910132095381,-3.56687019424698,
-3.40787464734053));
#47645=CARTESIAN_POINT('Ctrl Pts',(-1.96978703866801,-4.42772174548972,
-2.50685558452536));
#47646=CARTESIAN_POINT('Ctrl Pts',(-2.0304727563822,-4.91324846594047,-1.24716794257944));
#47647=CARTESIAN_POINT('Ctrl Pts',(-2.09115847409639,-4.92479967433243,
0.00455076259524401));
#47648=CARTESIAN_POINT('Ctrl Pts',(-2.3088415259036,-4.92378694620037,0.00452865572044409));
#47649=CARTESIAN_POINT('Ctrl Pts',(-2.24978385436538,-4.912807019143,-1.21423012654258));
#47650=CARTESIAN_POINT('Ctrl Pts',(-2.19072618282717,-4.45550843625236,
-2.44034737679679));
#47651=CARTESIAN_POINT('Ctrl Pts',(-2.13166851128896,-3.63585440375436,
-3.33416659713051));
#47652=CARTESIAN_POINT('Ctrl Pts',(-2.05212262291588,-2.53184697380615,
-4.53806851324942));
#47653=CARTESIAN_POINT('Ctrl Pts',(-1.9725767345428,-0.770457813911437,
-5.13911857767506));
#47654=CARTESIAN_POINT('Ctrl Pts',(-1.89303084616973,0.839206332661352,
-4.86124723150085));
#47655=CARTESIAN_POINT('Ctrl Pts',(-1.81348495779665,2.4488704792341,-4.58337588532665));
#47656=CARTESIAN_POINT('Ctrl Pts',(-1.73393906942358,3.90680961248493,-3.42658312855265));
#47657=CARTESIAN_POINT('Ctrl Pts',(-1.65439318105051,4.54327701636474,-1.9221980209477));
#47658=CARTESIAN_POINT('Ctrl Pts',(-1.57484729267743,5.17974442024456,-0.417812913342702));
#47659=CARTESIAN_POINT('Ctrl Pts',(-1.49530140430435,4.99474009475331,1.43416454509326));
#47660=CARTESIAN_POINT('Ctrl Pts',(-1.41575551593128,4.0732911268349,2.78288857953561));
#47661=CARTESIAN_POINT('Ctrl Pts',(-1.3362096275582,3.15184215891648,4.13161261397798));
#47662=CARTESIAN_POINT('Ctrl Pts',(-1.25666373918512,1.49394854857088,4.97708322442672));
#47663=CARTESIAN_POINT('Ctrl Pts',(-1.17711785081204,-0.138895601305483,
4.93114147431309));
#47664=CARTESIAN_POINT('Ctrl Pts',(-1.09757196243897,-1.77173975118177,
4.88519972419945));
#47665=CARTESIAN_POINT('Ctrl Pts',(-1.0180260740659,-3.37953444058883,3.94784561352353));
#47666=CARTESIAN_POINT('Ctrl Pts',(-0.938480185692825,-4.22355933348682,
2.54924407639987));
#47667=CARTESIAN_POINT('Ctrl Pts',(-0.895267299096415,-4.6820714291754,
1.7894611277975));
#47668=CARTESIAN_POINT('Ctrl Pts',(-0.852054412500004,-4.91518370582573,
0.893557208022445));
#47669=CARTESIAN_POINT('Ctrl Pts',(-0.808841525903593,-4.91703434725887,
-0.0013692803956027));
#47670=CARTESIAN_POINT('Origin',(-32.3478126690739,0.,0.));
#47671=CARTESIAN_POINT('',(-0.0978126690738565,-4.06323934281354,-0.00157601073016207));
#47672=CARTESIAN_POINT('',(0.,-4.0705,-4.82875428449296E-13));
#47673=CARTESIAN_POINT('',(-32.3478126690739,-4.0705,-4.82875428449296E-13));
#47674=CARTESIAN_POINT('',(0.,-3.73359974356529,-1.6214817929441));
#47675=CARTESIAN_POINT('Ctrl Pts',(-0.0978126690738567,-4.06320398010117,
-0.00158368662129781));
#47676=CARTESIAN_POINT('Ctrl Pts',(-0.0652084460492417,-4.06358958070638,
-0.560065388179513));
#47677=CARTESIAN_POINT('Ctrl Pts',(-0.0326042230246268,-3.95536025262438,
-1.1181257750272));
#47678=CARTESIAN_POINT('Ctrl Pts',(-1.16714363868065E-14,-3.73764785372991,
-1.62671566533116));
#47679=CARTESIAN_POINT('Origin',(0.,0.,0.));
#47680=CARTESIAN_POINT('Origin',(-32.3478126690739,0.,0.));
#47681=CARTESIAN_POINT('',(-1.59781266907385,-4.07033443134419,0.00376119373461055));
#47682=CARTESIAN_POINT('',(-1.30218733092609,-4.06391640822685,-0.00113170677241647));
#47683=CARTESIAN_POINT('',(-32.3478126690739,-4.0705,-4.82875428449296E-13));
#47684=CARTESIAN_POINT('Ctrl Pts',(-1.59781266907385,-4.07033443134419,
0.00376119373461031));
#47685=CARTESIAN_POINT('Ctrl Pts',(-1.53712695135966,-4.06078738692598,
-1.0307811391412));
#47686=CARTESIAN_POINT('Ctrl Pts',(-1.3968953452724,-3.13350059127503,-3.43660489264461));
#47687=CARTESIAN_POINT('Ctrl Pts',(-1.17711785081205,0.915788038447374,
-4.72632807804377));
#47688=CARTESIAN_POINT('Ctrl Pts',(-0.938480185692821,4.47158639354322,
-1.78518388428051));
#47689=CARTESIAN_POINT('Ctrl Pts',(-0.699842520573601,3.91848486245357,
2.79733082310517));
#47690=CARTESIAN_POINT('Ctrl Pts',(-0.461204855454373,-0.233233057815519,
4.80741524450186));
#47691=CARTESIAN_POINT('Ctrl Pts',(-0.260528238287788,-3.54660683376317,
2.78758749144531));
#47692=CARTESIAN_POINT('Ctrl Pts',(-0.139397509494285,-4.06271216836188,
0.7107281025446));
#47693=CARTESIAN_POINT('Ctrl Pts',(-0.0978126690738567,-4.06320398010117,
-0.00158368662129781));
#47694=CARTESIAN_POINT('',(0.,-2.75129702511903,2.99988915288068));
#47695=CARTESIAN_POINT('Origin',(0.,0.,0.));
#47696=CARTESIAN_POINT('Ctrl Pts',(-1.30218733092609,-4.06391640822685,
-0.00113170677241654));
#47697=CARTESIAN_POINT('Ctrl Pts',(-1.26585432914943,-4.06520244032274,
-0.623026454755739));
#47698=CARTESIAN_POINT('Ctrl Pts',(-1.1499754389997,-3.63835675138479,-2.6046490156767));
#47699=CARTESIAN_POINT('Ctrl Pts',(-0.9545506604769,-0.551158953576692,
-4.78140835552346));
#47700=CARTESIAN_POINT('Ctrl Pts',(-0.715912995357679,3.72696190987269,
-3.05177387808086));
#47701=CARTESIAN_POINT('Ctrl Pts',(-0.477275330238447,4.57725222884596,
1.49154630755727));
#47702=CARTESIAN_POINT('Ctrl Pts',(-0.278410609305757,1.78830202401348,
4.11849926473408));
#47703=CARTESIAN_POINT('Ctrl Pts',(-0.119318832559607,-1.02190788268887,
4.1117895186236));
#47704=CARTESIAN_POINT('Ctrl Pts',(-0.0397729441865359,-2.25151393523441,
3.45825666525491));
#47705=CARTESIAN_POINT('Ctrl Pts',(0.,-2.75129702511903,2.99988915288068));
#47706=CARTESIAN_POINT('Origin',(-32.3478126690739,0.,0.));
#47707=CARTESIAN_POINT('',(-3.09781266907385,-4.07681275190056,-0.00120979165237837));
#47708=CARTESIAN_POINT('',(-2.8021873309261,-4.06949741411341,0.00374292245829216));
#47709=CARTESIAN_POINT('',(-32.3478126690739,-4.0705,-4.82875428449296E-13));
#47710=CARTESIAN_POINT('Ctrl Pts',(-3.09781266907385,-4.07681275190056,
-0.00120979165237874));
#47711=CARTESIAN_POINT('Ctrl Pts',(-3.09394816997118,-4.07706926616768,
-0.0668170824659285));
#47712=CARTESIAN_POINT('Ctrl Pts',(-3.01053778249544,-4.04585841086343,
-1.48261925960601));
#47713=CARTESIAN_POINT('Ctrl Pts',(-2.84758150664664,-2.40317998874982,
-4.17175730007125));
#47714=CARTESIAN_POINT('Ctrl Pts',(-2.60894384152741,2.21026727641583,-4.27709000786183));
#47715=CARTESIAN_POINT('Ctrl Pts',(-2.37030617640818,4.79308872923565,-0.452955592184536));
#47716=CARTESIAN_POINT('Ctrl Pts',(-2.13166851128895,2.97235298759993,3.78734702964848));
#47717=CARTESIAN_POINT('Ctrl Pts',(-1.89303084616973,-1.57913728868941,
4.54806082325786));
#47718=CARTESIAN_POINT('Ctrl Pts',(-1.71507889876469,-3.89136234884321,
1.99954296889815));
#47719=CARTESIAN_POINT('Ctrl Pts',(-1.61667283973273,-4.0733015032319,0.325280748694308));
#47720=CARTESIAN_POINT('Ctrl Pts',(-1.59781266907385,-4.07033443134419,
0.00376119373461031));
#47721=CARTESIAN_POINT('Ctrl Pts',(-2.8021873309261,-4.06949741411341,0.00374292245829196));
#47722=CARTESIAN_POINT('Ctrl Pts',(-2.7431296593879,-4.06042253226819,-1.00355811778553));
#47723=CARTESIAN_POINT('Ctrl Pts',(-2.60452609947661,-3.17339021123584,
-3.38188525686312));
#47724=CARTESIAN_POINT('Ctrl Pts',(-2.38637665119226,0.819002242401078,
-4.74423481374027));
#47725=CARTESIAN_POINT('Ctrl Pts',(-2.14773898607304,4.43395122223712,-1.87597598138563));
#47726=CARTESIAN_POINT('Ctrl Pts',(-1.90910132095381,3.97523440584382,2.71598802545506));
#47727=CARTESIAN_POINT('Ctrl Pts',(-1.67046365583458,-0.135500177452599,
4.81232596646912));
#47728=CARTESIAN_POINT('Ctrl Pts',(-1.46815899249201,-3.51506103565612,
2.84202137248833));
#47729=CARTESIAN_POINT('Ctrl Pts',(-1.34540021752251,-4.06238685777956,
0.738522764518305));
#47730=CARTESIAN_POINT('Ctrl Pts',(-1.30218733092609,-4.06391640822685,
-0.00113170677241654));
#47731=CARTESIAN_POINT('Origin',(-32.3478126690739,0.,0.));
#47732=CARTESIAN_POINT('',(-4.59781266907386,-4.0666555507277,-0.00316262964624325));
#47733=CARTESIAN_POINT('',(-4.30218733092609,-4.0770951458019,-0.000710233193596532));
#47734=CARTESIAN_POINT('',(-32.3478126690739,-4.0705,-4.82875428449296E-13));
#47735=CARTESIAN_POINT('Ctrl Pts',(-4.59781266907386,-4.0666555507277,-0.00316262964624277));
#47736=CARTESIAN_POINT('Ctrl Pts',(-4.57122350020965,-4.06993404787816,
-0.457474827265511));
#47737=CARTESIAN_POINT('Ctrl Pts',(-4.46508844297236,-3.78979273029454,
-2.26701044287803));
#47738=CARTESIAN_POINT('Ctrl Pts',(-4.27940749736198,-1.13066914665236,
-4.67978735413588));
#47739=CARTESIAN_POINT('Ctrl Pts',(-4.04076983224278,3.32562064318893,-3.48124526728007));
#47740=CARTESIAN_POINT('Ctrl Pts',(-3.80213216712354,4.72657132062792,0.915612446800854));
#47741=CARTESIAN_POINT('Ctrl Pts',(-3.56349450200431,1.78509047620951,4.4712723004521));
#47742=CARTESIAN_POINT('Ctrl Pts',(-3.32872133598775,-2.72220888913037,
3.92799287505321));
#47743=CARTESIAN_POINT('Ctrl Pts',(-3.17349405834426,-4.07178924029207,
1.28362707416973));
#47744=CARTESIAN_POINT('Ctrl Pts',(-3.09781266907385,-4.07681275190056,
-0.00120979165237874));
#47745=CARTESIAN_POINT('Ctrl Pts',(-4.30218733092609,-4.0770951458019,-0.000710233193597031));
#47746=CARTESIAN_POINT('Ctrl Pts',(-4.29995087799942,-4.07718638960619,
-0.038671265149509));
#47747=CARTESIAN_POINT('Ctrl Pts',(-4.21816853669967,-4.05948324093355,
-1.42673845965056));
#47748=CARTESIAN_POINT('Ctrl Pts',(-4.05684030702684,-2.48802037989938,
-4.12171998606955));
#47749=CARTESIAN_POINT('Ctrl Pts',(-3.81820264190762,2.12230915839156,-4.32141378384957));
#47750=CARTESIAN_POINT('Ctrl Pts',(-3.5795649767884,4.78281558760628,-0.550907763508576));
#47751=CARTESIAN_POINT('Ctrl Pts',(-3.34092731166917,3.04921617498962,3.72573627855867));
#47752=CARTESIAN_POINT('Ctrl Pts',(-3.10228964654994,-1.48577931367711,
4.57943634031457));
#47753=CARTESIAN_POINT('Ctrl Pts',(-2.92270965296892,-3.87125352580713,
2.05582519611215));
#47754=CARTESIAN_POINT('Ctrl Pts',(-2.82267554776097,-4.07264566127848,
0.35319459559373));
#47755=CARTESIAN_POINT('Ctrl Pts',(-2.8021873309261,-4.06949741411341,0.00374292245829196));
#47756=CARTESIAN_POINT('Origin',(-32.3478126690739,0.,0.));
#47757=CARTESIAN_POINT('',(-6.09781266907385,-4.06532783024481,0.00248275864732798));
#47758=CARTESIAN_POINT('',(-5.80218733092609,-4.06735085704707,-0.00339183732646908));
#47759=CARTESIAN_POINT('',(-32.3478126690739,-4.0705,-4.82875428449296E-13));
#47760=CARTESIAN_POINT('Ctrl Pts',(-6.09781266907385,-4.06532783024481,
0.00248275864732861));
#47761=CARTESIAN_POINT('Ctrl Pts',(-6.0484988304481,-4.06065183816668,-0.840802599870245));
#47762=CARTESIAN_POINT('Ctrl Pts',(-5.91963910344927,-3.39313702767653,
-3.05113638265515));
#47763=CARTESIAN_POINT('Ctrl Pts',(-5.71123348807733,0.233422028762872,
-4.80877700124299));
#47764=CARTESIAN_POINT('Ctrl Pts',(-5.47259582295814,4.171611218274,-2.40343127894775));
#47765=CARTESIAN_POINT('Ctrl Pts',(-5.23395815783889,4.27722630874114,2.21001293857749));
#47766=CARTESIAN_POINT('Ctrl Pts',(-4.99532049271968,0.453235799314355,
4.7930574212978));
#47767=CARTESIAN_POINT('Ctrl Pts',(-4.78327199646466,-3.31468772914499,
3.17542596303663));
#47768=CARTESIAN_POINT('Ctrl Pts',(-4.65076938858272,-4.06012588239192,
0.901675116191023));
#47769=CARTESIAN_POINT('Ctrl Pts',(-4.59781266907386,-4.0666555507277,-0.00316262964624277));
#47770=CARTESIAN_POINT('Ctrl Pts',(-5.80218733092609,-4.06735085704707,
-0.00339183732646849));
#47771=CARTESIAN_POINT('Ctrl Pts',(-5.77722620823787,-4.07069006794027,
-0.429702830878314));
#47772=CARTESIAN_POINT('Ctrl Pts',(-5.67271919717658,-3.81249861092392,
-2.21063503182293));
#47773=CARTESIAN_POINT('Ctrl Pts',(-5.48866629774222,-1.22616783934351,
-4.65567735364785));
#47774=CARTESIAN_POINT('Ctrl Pts',(-5.25002863262297,3.25370797337249,-3.54854948612432));
#47775=CARTESIAN_POINT('Ctrl Pts',(-5.01139096750376,4.74431268704714,0.818728472038551));
#47776=CARTESIAN_POINT('Ctrl Pts',(-4.77275330238453,1.87618665939981,4.43381811498155));
#47777=CARTESIAN_POINT('Ctrl Pts',(-4.53635209019197,-2.67261016863284,
3.97973264573628));
#47778=CARTESIAN_POINT('Ctrl Pts',(-4.3794967663725,-4.07394104096335,1.31152214803601));
#47779=CARTESIAN_POINT('Ctrl Pts',(-4.30218733092609,-4.0770951458019,-0.000710233193597031));
#47780=CARTESIAN_POINT('Origin',(-32.3478126690739,0.,0.));
#47781=CARTESIAN_POINT('',(-7.59781266907386,-4.07574630203772,0.00222153505732406));
#47782=CARTESIAN_POINT('',(-7.3021873309261,-4.06485256559003,0.00211562990566405));
#47783=CARTESIAN_POINT('',(-32.3478126690739,-4.0705,-4.82875428449296E-13));
#47784=CARTESIAN_POINT('Ctrl Pts',(-7.59781266907386,-4.07574630203772,
0.00222153505732401));
#47785=CARTESIAN_POINT('Ctrl Pts',(-7.52577416068655,-4.06771182434402,
-1.22161827070251));
#47786=CARTESIAN_POINT('Ctrl Pts',(-7.37418976392616,-2.82963048299844,
-3.81092663700425));
#47787=CARTESIAN_POINT('Ctrl Pts',(-7.14305947879272,1.57860706315775,-4.5482767971816));
#47788=CARTESIAN_POINT('Ctrl Pts',(-6.90442181367349,4.6797195025539,-1.13094980465497));
#47789=CARTESIAN_POINT('Ctrl Pts',(-6.66578414855425,3.48144476711953,3.32541191686152));
#47790=CARTESIAN_POINT('Ctrl Pts',(-6.42714648343504,-0.91532914635784,
4.72662613694493));
#47791=CARTESIAN_POINT('Ctrl Pts',(-6.23782265694156,-3.7363609545651,2.39316384250277));
#47792=CARTESIAN_POINT('Ctrl Pts',(-6.12804471882117,-4.06819446624524,
0.519462284483144));
#47793=CARTESIAN_POINT('Ctrl Pts',(-6.09781266907385,-4.06532783024481,
0.00248275864732861));
#47794=CARTESIAN_POINT('Ctrl Pts',(-7.3021873309261,-4.06485256559003,0.0021156299056644));
#47795=CARTESIAN_POINT('Ctrl Pts',(-7.25450153847633,-4.06102628102932,
-0.813568030876496));
#47796=CARTESIAN_POINT('Ctrl Pts',(-7.12726985765349,-3.42680090686785,
-2.99539080099765));
#47797=CARTESIAN_POINT('Ctrl Pts',(-6.92049228845756,0.134999037069343,
-4.81254552210429));
#47798=CARTESIAN_POINT('Ctrl Pts',(-6.68185462333835,4.1215704771241,-2.48826765871595));
#47799=CARTESIAN_POINT('Ctrl Pts',(-6.44321695821911,4.32154162229638,2.12205022265777));
#47800=CARTESIAN_POINT('Ctrl Pts',(-6.20457929309988,0.551193473920355,
4.78278213002022));
#47801=CARTESIAN_POINT('Ctrl Pts',(-5.99090275066888,-3.27821055126197,
3.23074519309206));
#47802=CARTESIAN_POINT('Ctrl Pts',(-5.85677209661095,-4.06004869975013,
0.928861330231892));
#47803=CARTESIAN_POINT('Ctrl Pts',(-5.80218733092609,-4.06735085704707,
-0.00339183732646849));
#47804=CARTESIAN_POINT('Origin',(-32.3478126690739,0.,0.));
#47805=CARTESIAN_POINT('',(-9.09781266907386,-4.07222943229488,-0.00357906261956567));
#47806=CARTESIAN_POINT('',(-8.8021873309261,-4.07511392925337,0.00260772300212458));
#47807=CARTESIAN_POINT('',(-32.3478126690739,-4.0705,-4.82875428449296E-13));
#47808=CARTESIAN_POINT('Ctrl Pts',(-9.09781266907386,-4.07222943229488,
-0.003579062619565));
#47809=CARTESIAN_POINT('Ctrl Pts',(-9.08259537929808,-4.07461348194488,
-0.262682434050171));
#47810=CARTESIAN_POINT('Ctrl Pts',(-8.98783220114923,-3.93387284883695,
-1.87362564859038));
#47811=CARTESIAN_POINT('Ctrl Pts',(-8.8135231346273,-1.78562688897607,-4.47105789459565));
#47812=CARTESIAN_POINT('Ctrl Pts',(-8.57488546950807,2.79593183551325,-3.91938608134342));
#47813=CARTESIAN_POINT('Ctrl Pts',(-8.33624780438884,4.80879098967182,0.233133655034067));
#47814=CARTESIAN_POINT('Ctrl Pts',(-8.09761013926962,2.40368143941586,4.17146708260569));
#47815=CARTESIAN_POINT('Ctrl Pts',(-7.85897247415039,-2.20975644067261,
4.27735882951057));
#47816=CARTESIAN_POINT('Ctrl Pts',(-7.69237331741847,-4.01320701615423,
1.60783980898199));
#47817=CARTESIAN_POINT('Ctrl Pts',(-7.60532004905963,-4.07658360250915,
0.129762077875785));
#47818=CARTESIAN_POINT('Ctrl Pts',(-7.59781266907386,-4.07574630203772,
0.00222153505732401));
#47819=CARTESIAN_POINT('Ctrl Pts',(-8.8021873309261,-4.07511392925337,0.00260772300212448));
#47820=CARTESIAN_POINT('Ctrl Pts',(-8.73177686871478,-4.06620451024253,
-1.1940613554039));
#47821=CARTESIAN_POINT('Ctrl Pts',(-8.58182051813039,-2.87606084879853,
-3.7580704643467));
#47822=CARTESIAN_POINT('Ctrl Pts',(-8.35231827917293,1.48523158453539,-4.57961857379977));
#47823=CARTESIAN_POINT('Ctrl Pts',(-8.1136806140537,4.65560380841346,-1.22644703115444));
#47824=CARTESIAN_POINT('Ctrl Pts',(-7.87504294893448,3.54874460969979,3.25349517231261));
#47825=CARTESIAN_POINT('Ctrl Pts',(-7.63640528381524,-0.818443985601727,
4.74436176780107));
#47826=CARTESIAN_POINT('Ctrl Pts',(-7.44545341114579,-3.71128559220026,
2.44953276936589));
#47827=CARTESIAN_POINT('Ctrl Pts',(-7.33404742684941,-4.06740900403576,
0.547094717816802));
#47828=CARTESIAN_POINT('Ctrl Pts',(-7.3021873309261,-4.06485256559003,0.0021156299056644));
#47829=CARTESIAN_POINT('Origin',(-32.3478126690739,0.,0.));
#47830=CARTESIAN_POINT('',(-10.5978126690739,-4.06383028861155,-0.000517316456022591));
#47831=CARTESIAN_POINT('',(-10.3021873309261,-4.07305647823417,-0.00339818811806003));
#47832=CARTESIAN_POINT('',(-32.3478126690739,-4.0705,-4.82875428449296E-13));
#47833=CARTESIAN_POINT('Ctrl Pts',(-10.5978126690739,-4.06383028861155,
-0.000517316456022585));
#47834=CARTESIAN_POINT('Ctrl Pts',(-10.5598707095365,-4.06456413075875,
-0.649936894253117));
#47835=CARTESIAN_POINT('Ctrl Pts',(-10.4423828616261,-3.6108734382595,-2.65990611006904));
#47836=CARTESIAN_POINT('Ctrl Pts',(-10.2453491253427,-0.453810659605433,
-4.79300302197796));
#47837=CARTESIAN_POINT('Ctrl Pts',(-10.0067114602234,3.78679836713871,-2.97304224828663));
#47838=CARTESIAN_POINT('Ctrl Pts',(-9.76807379510421,4.54837145493611,1.57833430913225));
#47839=CARTESIAN_POINT('Ctrl Pts',(-9.52943612998497,1.131230436189,4.67965167333008));
#47840=CARTESIAN_POINT('Ctrl Pts',(-9.30601575464153,-3.04102820872573,
3.55803793366217));
#47841=CARTESIAN_POINT('Ctrl Pts',(-9.16214126767116,-4.06215125311643,
1.09173797619339));
#47842=CARTESIAN_POINT('Ctrl Pts',(-9.09781266907386,-4.07222943229488,
-0.003579062619565));
#47843=CARTESIAN_POINT('Ctrl Pts',(-10.3021873309261,-4.07305647823417,
-0.00339818811806027));
#47844=CARTESIAN_POINT('Ctrl Pts',(-10.2885980873263,-4.07512744307457,
-0.234659625407061));
#47845=CARTESIAN_POINT('Ctrl Pts',(-10.1954629553534,-3.95181437733735,
-1.8174227959994));
#47846=CARTESIAN_POINT('Ctrl Pts',(-10.0227819350075,-1.8767184363934,-4.43359301827195));
#47847=CARTESIAN_POINT('Ctrl Pts',(-9.78414426988828,2.71516687463254,-3.97576256635973));
#47848=CARTESIAN_POINT('Ctrl Pts',(-9.54550660476906,4.8125536089566,0.134710437930172));
#47849=CARTESIAN_POINT('Ctrl Pts',(-9.30686893964983,2.48851481691486,4.12142125330121));
#47850=CARTESIAN_POINT('Ctrl Pts',(-9.06823127453061,-2.12179106496689,
4.32166886952238));
#47851=CARTESIAN_POINT('Ctrl Pts',(-8.9000040716227,-3.99762873478501,1.66388105000583));
#47852=CARTESIAN_POINT('Ctrl Pts',(-8.81132275708786,-4.07626988444755,
0.157869905105551));
#47853=CARTESIAN_POINT('Ctrl Pts',(-8.8021873309261,-4.07511392925337,0.00260772300212448));
#47854=CARTESIAN_POINT('Origin',(-32.3478126690739,0.,0.));
#47855=CARTESIAN_POINT('',(-12.0978126690739,-4.07032458744755,0.00376143334710477));
#47856=CARTESIAN_POINT('',(-11.8021873309261,-4.06398132384238,-0.00096959209926889));
#47857=CARTESIAN_POINT('',(-32.3478126690739,-4.0705,-4.82875428449296E-13));
#47858=CARTESIAN_POINT('Ctrl Pts',(-12.0978126690739,-4.07032458744755,
0.00376143334710491));
#47859=CARTESIAN_POINT('Ctrl Pts',(-12.037146039775,-4.06079261000553,-1.03044389103757));
#47860=CARTESIAN_POINT('Ctrl Pts',(-11.8969335221031,-3.13401642257978,
-3.43588983608773));
#47861=CARTESIAN_POINT('Ctrl Pts',(-11.677175116058,0.914762246840484,-4.7267358838015));
#47862=CARTESIAN_POINT('Ctrl Pts',(-11.4385374509388,4.47095080603802,-1.78589500627826));
#47863=CARTESIAN_POINT('Ctrl Pts',(-11.1998997858196,3.91955374080681,2.79569679264203));
#47864=CARTESIAN_POINT('Ctrl Pts',(-10.9612621207003,-0.232845280914501,
4.80880496159049));
#47865=CARTESIAN_POINT('Ctrl Pts',(-10.7605664151184,-3.54512857250201,
2.78629205291713));
#47866=CARTESIAN_POINT('Ctrl Pts',(-10.6394165979096,-4.06302561966876,
0.711581010269389));
#47867=CARTESIAN_POINT('Ctrl Pts',(-10.5978126690739,-4.06383028861155,
-0.000517316456022585));
#47868=CARTESIAN_POINT('Ctrl Pts',(-11.8021873309261,-4.06398132384238,
-0.000969592099269029));
#47869=CARTESIAN_POINT('Ctrl Pts',(-11.7658734175648,-4.06530044997824,
-0.622465582635642));
#47870=CARTESIAN_POINT('Ctrl Pts',(-11.6500136158304,-3.63881171341208,
-2.60363619702803));
#47871=CARTESIAN_POINT('Ctrl Pts',(-11.4546079257229,-0.551767098271795,
-4.78271598680431));
#47872=CARTESIAN_POINT('Ctrl Pts',(-11.2159702606036,3.72518553231084,-3.04988719316482));
#47873=CARTESIAN_POINT('Ctrl Pts',(-10.9773325954844,4.57970763196809,1.48495695118139));
#47874=CARTESIAN_POINT('Ctrl Pts',(-10.7386949303652,1.22672621632081,4.65553025243742));
#47875=CARTESIAN_POINT('Ctrl Pts',(-10.5136465088458,-2.99816785865763,
3.6119546083943));
#47876=CARTESIAN_POINT('Ctrl Pts',(-10.3681439756994,-4.06300485973803,
1.11905048660218));
#47877=CARTESIAN_POINT('Ctrl Pts',(-10.3021873309261,-4.07305647823417,
-0.00339818811806027));
#47878=CARTESIAN_POINT('Origin',(-32.3478126690739,0.,0.));
#47879=CARTESIAN_POINT('',(-13.5978126690739,-4.07681666553846,-0.0012043583654883));
#47880=CARTESIAN_POINT('',(-13.3021873309261,-4.06948780842451,0.00374258894561955));
#47881=CARTESIAN_POINT('',(-32.3478126690739,-4.0705,-4.82875428449296E-13));
#47882=CARTESIAN_POINT('Ctrl Pts',(-13.5978126690739,-4.07681666553846,
-0.00120435836548843));
#47883=CARTESIAN_POINT('Ctrl Pts',(-13.5939672583865,-4.07707083999085,
-0.0664874041950833));
#47884=CARTESIAN_POINT('Ctrl Pts',(-13.5105759593261,-4.04602154531668,
-1.48196385087443));
#47885=CARTESIAN_POINT('Ctrl Pts',(-13.3476387718926,-2.40418173141341,
-4.17117876454601));
#47886=CARTESIAN_POINT('Ctrl Pts',(-13.1090011067734,2.20924341525388,-4.27762382820403));
#47887=CARTESIAN_POINT('Ctrl Pts',(-12.8703634416541,4.79297579923065,-0.454098085715957));
#47888=CARTESIAN_POINT('Ctrl Pts',(-12.6317257765349,2.97326932976115,3.78662007285696));
#47889=CARTESIAN_POINT('Ctrl Pts',(-12.3930881114157,-1.57806154943975,
4.54846609634954));
#47890=CARTESIAN_POINT('Ctrl Pts',(-12.2151170755953,-3.89111272737449,
2.00017169269057));
#47891=CARTESIAN_POINT('Ctrl Pts',(-12.1166919281481,-4.07329090803759,
0.325602789635245));
#47892=CARTESIAN_POINT('Ctrl Pts',(-12.0978126690739,-4.07032458744755,
0.00376143334710491));
#47893=CARTESIAN_POINT('Ctrl Pts',(-13.3021873309261,-4.06948780842451,
0.00374258894561951));
#47894=CARTESIAN_POINT('Ctrl Pts',(-13.2431487478032,-4.06042005381897,
-1.00323625051947));
#47895=CARTESIAN_POINT('Ctrl Pts',(-13.1045642763073,-3.17385622399582,
-3.38123201716333));
#47896=CARTESIAN_POINT('Ctrl Pts',(-12.8864339164382,0.817874959696777,
-4.74445989460021));
#47897=CARTESIAN_POINT('Ctrl Pts',(-12.647796251319,4.43348046720131,-1.87698430683722));
#47898=CARTESIAN_POINT('Ctrl Pts',(-12.4091585861998,3.9759253824068,2.71492845112022));
#47899=CARTESIAN_POINT('Ctrl Pts',(-12.1705209210805,-0.134421838351238,
4.81256167862222));
#47900=CARTESIAN_POINT('Ctrl Pts',(-11.9681971693227,-3.51458600877433,
2.84237865671728));
#47901=CARTESIAN_POINT('Ctrl Pts',(-11.8454193059378,-4.06241089469102,
0.738925854183665));
#47902=CARTESIAN_POINT('Ctrl Pts',(-11.8021873309261,-4.06398132384238,
-0.000969592099269029));
#47903=CARTESIAN_POINT('Origin',(-32.3478126690739,0.,0.));
#47904=CARTESIAN_POINT('',(-15.0978126690739,-4.06666337103388,-0.00316560979000432));
#47905=CARTESIAN_POINT('',(-14.8021873309261,-4.07709762639944,-0.00070430106655972));
#47906=CARTESIAN_POINT('',(-32.3478126690739,-4.0705,-4.82875428449296E-13));
#47907=CARTESIAN_POINT('Ctrl Pts',(-15.0978126690739,-4.06666337103388,
-0.00316560979000423));
#47908=CARTESIAN_POINT('Ctrl Pts',(-15.071242588625,-4.06994301140227,-0.457149458338325));
#47909=CARTESIAN_POINT('Ctrl Pts',(-14.965126619803,-3.79006310537379,-2.26634942371038));
#47910=CARTESIAN_POINT('Ctrl Pts',(-14.7794647626079,-1.13179168699179,
-4.67951596436188));
#47911=CARTESIAN_POINT('Ctrl Pts',(-14.5408270974888,3.32478553700414,-3.48204296590229));
#47912=CARTESIAN_POINT('Ctrl Pts',(-14.3021894323695,4.72679073178803,0.914478792178541));
#47913=CARTESIAN_POINT('Ctrl Pts',(-14.0635517672503,1.78616311715816,4.47084370140194));
#47914=CARTESIAN_POINT('Ctrl Pts',(-13.8287595128184,-2.72163337242562,
3.9286021789031));
#47915=CARTESIAN_POINT('Ctrl Pts',(-13.6735131467596,-4.07181300558473,
1.28395297745419));
#47916=CARTESIAN_POINT('Ctrl Pts',(-13.5978126690739,-4.07681666553846,
-0.00120435836548843));
#47917=CARTESIAN_POINT('Ctrl Pts',(-14.8021873309261,-4.07709762639944,
-0.000704301066560046));
#47918=CARTESIAN_POINT('Ctrl Pts',(-14.7999699664147,-4.07718738154795,
-0.0383412680213716));
#47919=CARTESIAN_POINT('Ctrl Pts',(-14.7182067135303,-4.05963949617112,
-1.42608358607219));
#47920=CARTESIAN_POINT('Ctrl Pts',(-14.5568975722728,-2.48900910600372,
-4.12112276102026));
#47921=CARTESIAN_POINT('Ctrl Pts',(-14.3182599071536,2.12127272581082,-4.32192331767929));
#47922=CARTESIAN_POINT('Ctrl Pts',(-14.0796222420344,4.78268288982128,-0.552053907312987));
#47923=CARTESIAN_POINT('Ctrl Pts',(-13.8409845769151,3.05011057970114,3.72500262990027));
#47924=CARTESIAN_POINT('Ctrl Pts',(-13.6023469117959,-1.48468231248816,
4.57979667366944));
#47925=CARTESIAN_POINT('Ctrl Pts',(-13.4227478297996,-3.8710120869076,2.05648068706029));
#47926=CARTESIAN_POINT('Ctrl Pts',(-13.3226946361763,-4.0726375319069,0.353521010938116));
#47927=CARTESIAN_POINT('Ctrl Pts',(-13.3021873309261,-4.06948780842451,
0.00374258894561951));
#47928=CARTESIAN_POINT('Origin',(-32.3478126690739,0.,0.));
#47929=CARTESIAN_POINT('',(-16.5978126690739,-4.06532180994014,0.00247865735123198));
#47930=CARTESIAN_POINT('',(-16.3021873309261,-4.06735933458706,-0.00339422375240483));
#47931=CARTESIAN_POINT('',(-32.3478126690739,-4.0705,-4.82875428449296E-13));
#47932=CARTESIAN_POINT('Ctrl Pts',(-16.5978126690739,-4.06532180994014,
0.00247865735123177));
#47933=CARTESIAN_POINT('Ctrl Pts',(-16.5485179188634,-4.06065576655941,
-0.840483409511789));
#47934=CARTESIAN_POINT('Ctrl Pts',(-16.4196772802799,-3.39353668499773,
-3.05048344280494));
#47935=CARTESIAN_POINT('Ctrl Pts',(-16.2112907533233,0.232268530165553,
-4.80883285354733));
#47936=CARTESIAN_POINT('Ctrl Pts',(-15.9726530882041,4.17103458301497,-2.40443186444421));
#47937=CARTESIAN_POINT('Ctrl Pts',(-15.7340154230849,4.27775630447756,2.20898689062749));
#47938=CARTESIAN_POINT('Ctrl Pts',(-15.4953777579657,0.454385510193501,
4.79294855924697));
#47939=CARTESIAN_POINT('Ctrl Pts',(-15.2833101732953,-3.31426516276753,
3.17607544524493));
#47940=CARTESIAN_POINT('Ctrl Pts',(-15.1507884769981,-4.06012437697437,
0.9019939062919));
#47941=CARTESIAN_POINT('Ctrl Pts',(-15.0978126690739,-4.06666337103388,
-0.00316560979000423));
#47942=CARTESIAN_POINT('Ctrl Pts',(-16.3021873309261,-4.06735933458706,
-0.0033942237524047));
#47943=CARTESIAN_POINT('Ctrl Pts',(-16.2772452966532,-4.07069882146085,
-0.42937696578519));
#47944=CARTESIAN_POINT('Ctrl Pts',(-16.1727573740072,-3.81276059892577,
-2.20997410073169));
#47945=CARTESIAN_POINT('Ctrl Pts',(-15.9887235629882,-1.22728457340874,
-4.65538309025602));
#47946=CARTESIAN_POINT('Ctrl Pts',(-15.7500858978689,3.25285668605437,-3.54932986930775));
#47947=CARTESIAN_POINT('Ctrl Pts',(-15.5114482327497,4.74450893241555,0.817590442335157));
#47948=CARTESIAN_POINT('Ctrl Pts',(-15.2728105676305,1.8772501705311,4.43336790018713));
#47949=CARTESIAN_POINT('Ctrl Pts',(-15.0363902670226,-2.67202280013241,
3.98033711867999));
#47950=CARTESIAN_POINT('Ctrl Pts',(-14.8795158547878,-4.07396749912098,
1.31184989664949));
#47951=CARTESIAN_POINT('Ctrl Pts',(-14.8021873309261,-4.07709762639944,
-0.000704301066560046));
#47952=CARTESIAN_POINT('Origin',(-32.3478126690739,0.,0.));
#47953=CARTESIAN_POINT('',(-18.0978126690739,-4.0757393762113,0.00222632843356818));
#47954=CARTESIAN_POINT('',(-17.8021873309261,-4.06484746876737,0.00211112861108809));
#47955=CARTESIAN_POINT('',(-32.3478126690739,-4.0705,-4.82875428449296E-13));
#47956=CARTESIAN_POINT('Ctrl Pts',(-18.0978126690739,-4.0757393762113,0.00222632843356826));
#47957=CARTESIAN_POINT('Ctrl Pts',(-18.0257932491019,-4.06769305643308,
-1.22129466881777));
#47958=CARTESIAN_POINT('Ctrl Pts',(-17.8742279407568,-2.83018048694797,
-3.8103087610216));
#47959=CARTESIAN_POINT('Ctrl Pts',(-17.6431167440387,1.5775160130308,-4.54865533010503));
#47960=CARTESIAN_POINT('Ctrl Pts',(-17.4044790789195,4.6794480846352,-1.13207230628853));
#47961=CARTESIAN_POINT('Ctrl Pts',(-17.1658414138002,3.48224234046452,3.3245767197852));
#47962=CARTESIAN_POINT('Ctrl Pts',(-16.927203748681,-0.914195334228,4.72684556277623));
#47963=CARTESIAN_POINT('Ctrl Pts',(-16.7378608337722,-3.73607127850369,
2.39382482140684));
#47964=CARTESIAN_POINT('Ctrl Pts',(-16.6280638072365,-4.06818526137017,
0.519786521610059));
#47965=CARTESIAN_POINT('Ctrl Pts',(-16.5978126690739,-4.06532180994014,
0.00247865735123177));
#47966=CARTESIAN_POINT('Ctrl Pts',(-17.8021873309261,-4.06484746876737,
0.00211112861108823));
#47967=CARTESIAN_POINT('Ctrl Pts',(-17.7545206268917,-4.0610311343114,-0.813248574751964));
#47968=CARTESIAN_POINT('Ctrl Pts',(-17.6273080344841,-3.42719055604098,
-2.99473654818825));
#47969=CARTESIAN_POINT('Ctrl Pts',(-17.4205495537035,0.133844637744424,
-4.81257776603306));
#47970=CARTESIAN_POINT('Ctrl Pts',(-17.1819118885843,4.1209734926491,-2.4892562371223));
#47971=CARTESIAN_POINT('Ctrl Pts',(-16.9432742234651,4.32205051844462,2.12101354478971));
#47972=CARTESIAN_POINT('Ctrl Pts',(-16.7046365583459,0.55234071436891,4.78264977563894));
#47973=CARTESIAN_POINT('Ctrl Pts',(-16.4909409274995,-3.27777761810244,
3.23139288635401));
#47974=CARTESIAN_POINT('Ctrl Pts',(-16.3567911850263,-4.06004842914805,
0.929180049887315));
#47975=CARTESIAN_POINT('Ctrl Pts',(-16.3021873309261,-4.06735933458706,
-0.0033942237524047));
#47976=CARTESIAN_POINT('Origin',(-32.3478126690739,0.,0.));
#47977=CARTESIAN_POINT('',(-19.5978126690739,-4.07223926118534,-0.00357729417079465));
#47978=CARTESIAN_POINT('',(-19.3021873309261,-4.07510605262456,0.00261196768466351));
#47979=CARTESIAN_POINT('',(-32.3478126690739,-4.0705,-4.82875428449296E-13));
#47980=CARTESIAN_POINT('Ctrl Pts',(-19.5978126690739,-4.07223926118534,
-0.00357729417079473));
#47981=CARTESIAN_POINT('Ctrl Pts',(-19.5826144677134,-4.07461978933759,
-0.262354039634738));
#47982=CARTESIAN_POINT('Ctrl Pts',(-19.4878703779799,-3.9340869821028,-1.87296646703573));
#47983=CARTESIAN_POINT('Ctrl Pts',(-19.3135803998733,-1.78669931964703,
-4.4706294438965));
#47984=CARTESIAN_POINT('Ctrl Pts',(-19.074942734754,2.79499160370957,-3.92005663462335));
#47985=CARTESIAN_POINT('Ctrl Pts',(-18.8363050696348,4.80884677358576,0.231980153537627));
#47986=CARTESIAN_POINT('Ctrl Pts',(-18.5976674045156,2.4046819888283,4.1708903864842));
#47987=CARTESIAN_POINT('Ctrl Pts',(-18.3590297393964,-2.20873035805718,
4.27788876536757));
#47988=CARTESIAN_POINT('Ctrl Pts',(-18.1924114942491,-4.01302793193152,
1.60849660347309));
#47989=CARTESIAN_POINT('Ctrl Pts',(-18.1053391374749,-4.07658026567666,
0.130091730952273));
#47990=CARTESIAN_POINT('Ctrl Pts',(-18.0978126690739,-4.0757393762113,0.00222632843356826));
#47991=CARTESIAN_POINT('Ctrl Pts',(-19.3021873309261,-4.07510605262456,
0.00261196768466343));
#47992=CARTESIAN_POINT('Ctrl Pts',(-19.2317959571301,-4.06618795069759,
-1.19373875342118));
#47993=CARTESIAN_POINT('Ctrl Pts',(-19.081858694961,-2.87659949644564,-3.75744888720017));
#47994=CARTESIAN_POINT('Ctrl Pts',(-18.8523755444189,1.48413301908516,-4.57997470766269));
#47995=CARTESIAN_POINT('Ctrl Pts',(-18.6137378792997,4.6553094840529,-1.22756374533297));
#47996=CARTESIAN_POINT('Ctrl Pts',(-18.3751002141804,3.54952493031783,3.25264383390203));
#47997=CARTESIAN_POINT('Ctrl Pts',(-18.1364625490612,-0.817305922033317,
4.74455795316888));
#47998=CARTESIAN_POINT('Ctrl Pts',(-17.9454915879764,-3.71098714745764,
2.45019360063996));
#47999=CARTESIAN_POINT('Ctrl Pts',(-17.8340665152647,-4.06739980864662,
0.547418441384662));
#48000=CARTESIAN_POINT('Ctrl Pts',(-17.8021873309261,-4.06484746876737,
0.00211112861108823));
#48001=CARTESIAN_POINT('Origin',(-32.3478126690739,0.,0.));
#48002=CARTESIAN_POINT('',(-21.0978126690739,-4.06383152666866,-0.000522675918812766));
#48003=CARTESIAN_POINT('',(-20.8021873309261,-4.07306601825716,-0.00339571005182004));
#48004=CARTESIAN_POINT('',(-32.3478126690739,-4.0705,-4.82875428449296E-13));
#48005=CARTESIAN_POINT('Ctrl Pts',(-21.0978126690739,-4.06383152666866,
-0.00052267591881365));
#48006=CARTESIAN_POINT('Ctrl Pts',(-21.0598897979519,-4.06457261097563,
-0.649615040927229));
#48007=CARTESIAN_POINT('Ctrl Pts',(-20.9424210384568,-3.6112055683889,-2.65924661123667));
#48008=CARTESIAN_POINT('Ctrl Pts',(-20.7454063905886,-0.454960354245989,
-4.79289402757069));
#48009=CARTESIAN_POINT('Ctrl Pts',(-20.5067687254694,3.78608510831067,-2.97395051002756));
#48010=CARTESIAN_POINT('Ctrl Pts',(-20.2681310603502,4.54874992244621,1.57724323631644));
#48011=CARTESIAN_POINT('Ctrl Pts',(-20.0294933952309,1.13235292151423,4.67938018808041));
#48012=CARTESIAN_POINT('Ctrl Pts',(-19.8060539314722,-3.04053113635729,
3.55867154707108));
#48013=CARTESIAN_POINT('Ctrl Pts',(-19.6621603560865,-4.06216033955295,
1.09205794767961));
#48014=CARTESIAN_POINT('Ctrl Pts',(-19.5978126690739,-4.07223926118534,
-0.00357729417079473));
#48015=CARTESIAN_POINT('Ctrl Pts',(-20.8021873309261,-4.07306601825716,
-0.0033957100518197));
#48016=CARTESIAN_POINT('Ctrl Pts',(-20.7886171757417,-4.07513318091976,
-0.234330901384573));
#48017=CARTESIAN_POINT('Ctrl Pts',(-20.6955011321841,-3.95202089787016,
-1.81676406404286));
#48018=CARTESIAN_POINT('Ctrl Pts',(-20.5228392002535,-1.87778187766528,
-4.43314271832978));
#48019=CARTESIAN_POINT('Ctrl Pts',(-20.2842015351343,2.71421312200688,-3.97641374475733));
#48020=CARTESIAN_POINT('Ctrl Pts',(-20.045563870015,4.81258578377826,0.133556036718511));
#48021=CARTESIAN_POINT('Ctrl Pts',(-19.8069262048958,2.48950335928912,4.12082420945821));
#48022=CARTESIAN_POINT('Ctrl Pts',(-19.5682885397766,-2.12075435614108,
4.32217770366716));
#48023=CARTESIAN_POINT('Ctrl Pts',(-19.4000422484533,-3.99744242114115,
1.66453839875525));
#48024=CARTESIAN_POINT('Ctrl Pts',(-19.3113418455032,-4.07626586652913,
0.158199357517422));
#48025=CARTESIAN_POINT('Ctrl Pts',(-19.3021873309261,-4.07510605262456,
0.00261196768466343));
#48026=CARTESIAN_POINT('Origin',(-32.3478126690739,0.,0.));
#48027=CARTESIAN_POINT('',(-22.5978126690739,-4.07031468847398,0.00376156571352546));
#48028=CARTESIAN_POINT('',(-22.3021873309261,-4.06398364289261,-0.000974823831897398));
#48029=CARTESIAN_POINT('',(-32.3478126690739,-4.0705,-4.82875428449296E-13));
#48030=CARTESIAN_POINT('Ctrl Pts',(-22.5978126690739,-4.07031468847398,
0.00376156571352537));
#48031=CARTESIAN_POINT('Ctrl Pts',(-22.5371651281903,-4.06078745327604,
-1.03012477253975));
#48032=CARTESIAN_POINT('Ctrl Pts',(-22.3969716989337,-3.13448885277667,
-3.4352501825917));
#48033=CARTESIAN_POINT('Ctrl Pts',(-22.177232381304,0.913628408435968,-4.7269551737383));
#48034=CARTESIAN_POINT('Ctrl Pts',(-21.9385947161847,4.47052229104313,-1.7869674112637));
#48035=CARTESIAN_POINT('Ctrl Pts',(-21.6999570510656,3.92022423769407,2.79475652063351));
#48036=CARTESIAN_POINT('Ctrl Pts',(-21.4613193859463,-0.231691776071347,
4.80886067632815));
#48037=CARTESIAN_POINT('Ctrl Pts',(-21.2606045919491,-3.54477519825892,
2.78695006207459));
#48038=CARTESIAN_POINT('Ctrl Pts',(-21.1394356863249,-4.06301813453931,
0.71190182958246));
#48039=CARTESIAN_POINT('Ctrl Pts',(-21.0978126690739,-4.06383152666866,
-0.00052267591881365));
#48040=CARTESIAN_POINT('Ctrl Pts',(-22.3021873309261,-4.06398364289261,
-0.000974823831896773));
#48041=CARTESIAN_POINT('Ctrl Pts',(-22.2658925059801,-4.06530923181794,
-0.622143240829621));
#48042=CARTESIAN_POINT('Ctrl Pts',(-22.150051792661,-3.63913463819147,-2.60297621081044));
#48043=CARTESIAN_POINT('Ctrl Pts',(-21.9546651909688,-0.552914322524486,
-4.78258349567352));
#48044=CARTESIAN_POINT('Ctrl Pts',(-21.7160275258496,3.72445384229878,-3.05078067349642));
#48045=CARTESIAN_POINT('Ctrl Pts',(-21.4773898607304,4.58006369995296,1.4838583643783));
#48046=CARTESIAN_POINT('Ctrl Pts',(-21.2387521956112,1.22784291284316,4.65523586110807));
#48047=CARTESIAN_POINT('Ctrl Pts',(-21.0136846856764,-2.99765973840581,
3.61258525206308));
#48048=CARTESIAN_POINT('Ctrl Pts',(-20.8681630641147,-4.06301583309485,
1.11937100559103));
#48049=CARTESIAN_POINT('Ctrl Pts',(-20.8021873309261,-4.07306601825716,
-0.0033957100518197));
#48050=CARTESIAN_POINT('Origin',(-32.3478126690739,0.,0.));
#48051=CARTESIAN_POINT('',(-24.0978126690739,-4.07682073202661,-0.00119862600692145));
#48052=CARTESIAN_POINT('',(-23.8021873309261,-4.06947811712022,0.00374200930701507));
#48053=CARTESIAN_POINT('',(-32.3478126690739,-4.0705,-4.82875428449296E-13));
#48054=CARTESIAN_POINT('Ctrl Pts',(-24.0978126690739,-4.07682073202661,
-0.0011986260069221));
#48055=CARTESIAN_POINT('Ctrl Pts',(-24.0939863468019,-4.07707257100012,
-0.0661574373907974));
#48056=CARTESIAN_POINT('Ctrl Pts',(-24.0106141361567,-4.04618464425921,
-1.48130837178561));
#48057=CARTESIAN_POINT('Ctrl Pts',(-23.8476960371386,-2.40518220884904,
-4.17060195021093));
#48058=CARTESIAN_POINT('Ctrl Pts',(-23.6090583720194,2.20821726762825,-4.27815364006511));
#48059=CARTESIAN_POINT('Ctrl Pts',(-23.3704207069001,4.7928667366398,-0.455247774302161));
#48060=CARTESIAN_POINT('Ctrl Pts',(-23.1317830417809,2.97417754833123,3.7859067598156));
#48061=CARTESIAN_POINT('Ctrl Pts',(-22.8931453766616,-1.57697045372341,
4.54884449829819));
#48062=CARTESIAN_POINT('Ctrl Pts',(-22.715155252426,-3.89088098364765,2.00083174485514));
#48063=CARTESIAN_POINT('Ctrl Pts',(-22.6167110165634,-4.07328346509314,
0.325930329695141));
#48064=CARTESIAN_POINT('Ctrl Pts',(-22.5978126690739,-4.07031468847398,
0.00376156571352537));
#48065=CARTESIAN_POINT('Ctrl Pts',(-23.8021873309261,-4.06947811712022,
0.00374200930701521));
#48066=CARTESIAN_POINT('Ctrl Pts',(-23.7431678362185,-4.06041648348459,
-1.00291735298318));
#48067=CARTESIAN_POINT('Ctrl Pts',(-23.6046024531379,-3.17431791098803,
-3.38058997938746));
#48068=CARTESIAN_POINT('Ctrl Pts',(-23.3864911816842,0.816736872430108,
-4.74465594332464));
#48069=CARTESIAN_POINT('Ctrl Pts',(-23.1478535165649,4.43303010358293,-1.87804772118901));
#48070=CARTESIAN_POINT('Ctrl Pts',(-22.9092158514458,3.97657650355884,2.71397465949093));
#48071=CARTESIAN_POINT('Ctrl Pts',(-22.6705781863265,-0.13326743518637,
4.81259378419344));
#48072=CARTESIAN_POINT('Ctrl Pts',(-22.4682353461533,-3.5142230495247,2.84303582389633));
#48073=CARTESIAN_POINT('Ctrl Pts',(-22.3454383943532,-4.06240399260436,
0.739246258441231));
#48074=CARTESIAN_POINT('Ctrl Pts',(-22.3021873309261,-4.06398364289261,
-0.000974823831896773));
#48075=CARTESIAN_POINT('Origin',(-32.3478126690739,0.,0.));
#48076=CARTESIAN_POINT('',(-25.5978126690739,-4.06667116509479,-0.00316860155561062));
#48077=CARTESIAN_POINT('',(-25.3021873309261,-4.07710011149971,-0.000698316132069499));
#48078=CARTESIAN_POINT('',(-32.3478126690739,-4.0705,-4.82875428449296E-13));
#48079=CARTESIAN_POINT('Ctrl Pts',(-25.5978126690739,-4.06667116509479,
-0.00316860155561056));
#48080=CARTESIAN_POINT('Ctrl Pts',(-25.5712616770403,-4.06995198256812,
-0.456824073053871));
#48081=CARTESIAN_POINT('Ctrl Pts',(-25.4651647966337,-3.79033356389561,
-2.26568828448685));
#48082=CARTESIAN_POINT('Ctrl Pts',(-25.2795220278539,-1.132913999441,-4.67924443383647));
#48083=CARTESIAN_POINT('Ctrl Pts',(-25.0408843627347,3.32395012330801,-3.48284034246832));
#48084=CARTESIAN_POINT('Ctrl Pts',(-24.8022466976155,4.72700999182265,0.913344916409211));
#48085=CARTESIAN_POINT('Ctrl Pts',(-24.5636090324962,1.78723547660136,4.47041513471273));
#48086=CARTESIAN_POINT('Ctrl Pts',(-24.3287976896491,-2.72105741290232,
3.9292109076427));
#48087=CARTESIAN_POINT('Ctrl Pts',(-24.1735322351749,-4.07183705933901,
1.28427935068815));
#48088=CARTESIAN_POINT('Ctrl Pts',(-24.0978126690739,-4.07682073202661,
-0.0011986260069221));
#48089=CARTESIAN_POINT('Ctrl Pts',(-25.3021873309261,-4.07710011149971,
-0.000698316132069399));
#48090=CARTESIAN_POINT('Ctrl Pts',(-25.2999890548301,-4.0771883891112,-0.0380112202494885));
#48091=CARTESIAN_POINT('Ctrl Pts',(-25.2182448903609,-4.05979569108433,
-1.42542869581234));
#48092=CARTESIAN_POINT('Ctrl Pts',(-25.0569548375188,-2.48999755919744,
-4.12052561435965));
#48093=CARTESIAN_POINT('Ctrl Pts',(-24.8183171723996,2.12023594681246,-4.32243201928095));
#48094=CARTESIAN_POINT('Ctrl Pts',(-24.5796795072803,4.78255033466597,-0.553201127887688));
#48095=CARTESIAN_POINT('Ctrl Pts',(-24.3410418421611,3.05100401366679,3.72427088853368));
#48096=CARTESIAN_POINT('Ctrl Pts',(-24.1024041770419,-1.48358370303888,
4.58015267461461));
#48097=CARTESIAN_POINT('Ctrl Pts',(-23.9227860066302,-3.87077237514414,
2.05714104990295));
#48098=CARTESIAN_POINT('Ctrl Pts',(-23.8227137245916,-4.07262966323526,
0.353848130340812));
#48099=CARTESIAN_POINT('Ctrl Pts',(-23.8021873309261,-4.06947811712022,
0.00374200930701521));
#48100=CARTESIAN_POINT('Origin',(-32.3478126690739,0.,0.));
#48101=CARTESIAN_POINT('',(-27.0978126690739,-4.06530890290629,0.00247015883041497));
#48102=CARTESIAN_POINT('',(-26.8021873309261,-4.0673676331488,-0.00339676908166275));
#48103=CARTESIAN_POINT('',(-32.3478126690739,-4.0705,-4.82875428449296E-13));
#48104=CARTESIAN_POINT('Ctrl Pts',(-27.0978126690739,-4.06530890290629,
0.0024701588304149));
#48105=CARTESIAN_POINT('Ctrl Pts',(-27.0485370072788,-4.06065548839014,
-0.840166902292313));
#48106=CARTESIAN_POINT('Ctrl Pts',(-26.9197154571106,-3.39394710335117,
-3.04982355875152));
#48107=CARTESIAN_POINT('Ctrl Pts',(-26.7113480185693,0.231122040344854,
-4.80889290141546));
#48108=CARTESIAN_POINT('Ctrl Pts',(-26.4727103534501,4.17045404914302,-2.40542998080026));
#48109=CARTESIAN_POINT('Ctrl Pts',(-26.2340726883308,4.27828796113812,2.20795949931288));
#48110=CARTESIAN_POINT('Ctrl Pts',(-25.9954350232116,0.45553419918425,4.79284005902739));
#48111=CARTESIAN_POINT('Ctrl Pts',(-25.7833483501259,-3.31384212136007,
3.1767246763176));
#48112=CARTESIAN_POINT('Ctrl Pts',(-25.6508075654134,-4.06012276262123,
0.902312619466092));
#48113=CARTESIAN_POINT('Ctrl Pts',(-25.5978126690739,-4.06667116509479,
-0.00316860155561056));
#48114=CARTESIAN_POINT('Ctrl Pts',(-26.8021873309261,-4.0673676331488,-0.00339676908166248));
#48115=CARTESIAN_POINT('Ctrl Pts',(-26.7772643850685,-4.07070764203952,
-0.429051031665485));
#48116=CARTESIAN_POINT('Ctrl Pts',(-26.6727955508379,-3.81302358814286,
-2.20931218578228));
#48117=CARTESIAN_POINT('Ctrl Pts',(-26.4887808282342,-1.22840035655279,
-4.65508935177024));
#48118=CARTESIAN_POINT('Ctrl Pts',(-26.2501431631149,3.25200474977257,-3.55010962682765));
#48119=CARTESIAN_POINT('Ctrl Pts',(-26.0115054979957,4.74470515142096,0.816452129912828));
#48120=CARTESIAN_POINT('Ctrl Pts',(-25.7728678328764,1.87831343359306,4.43291758398628));
#48121=CARTESIAN_POINT('Ctrl Pts',(-25.5364284438533,-2.67143520246076,
3.98094140217226));
#48122=CARTESIAN_POINT('Ctrl Pts',(-25.3795349432031,-4.07399401282602,
1.31217773515604));
#48123=CARTESIAN_POINT('Ctrl Pts',(-25.3021873309261,-4.07710011149971,
-0.000698316132069399));
#48124=CARTESIAN_POINT('Origin',(-32.3478126690739,0.,0.));
#48125=CARTESIAN_POINT('',(-28.5978126690739,-4.07533558288693,0.00197868943318482));
#48126=CARTESIAN_POINT('',(-28.3021873309261,-4.06480101368718,0.00206955444756823));
#48127=CARTESIAN_POINT('',(-32.3478126690739,-4.0705,-4.82875428449296E-13));
#48128=CARTESIAN_POINT('Ctrl Pts',(-28.5978126690739,-4.07533558288693,
0.00197868943318465));
#48129=CARTESIAN_POINT('Ctrl Pts',(-28.5258123375172,-4.0671548117311,-1.22130223361166));
#48130=CARTESIAN_POINT('Ctrl Pts',(-28.3742661175874,-2.83137270070474,
-3.80928172890928));
#48131=CARTESIAN_POINT('Ctrl Pts',(-28.1431740092847,1.57677629758835,-4.54925739906848));
#48132=CARTESIAN_POINT('Ctrl Pts',(-27.9045363441654,4.67899334175034,-1.13307817052668));
#48133=CARTESIAN_POINT('Ctrl Pts',(-27.6658986790463,3.48313507021902,3.32368060727122));
#48134=CARTESIAN_POINT('Ctrl Pts',(-27.4272610139269,-0.913111142894123,
4.72709634916456));
#48135=CARTESIAN_POINT('Ctrl Pts',(-27.2378990106029,-3.7357712242627,2.39447925508501));
#48136=CARTESIAN_POINT('Ctrl Pts',(-27.1280828956518,-4.06816751315389,
0.520105312452931));
#48137=CARTESIAN_POINT('Ctrl Pts',(-27.0978126690739,-4.06530890290629,
0.0024701588304149));
#48138=CARTESIAN_POINT('Ctrl Pts',(-28.3021873309261,-4.06480101368718,
0.00206955444756761));
#48139=CARTESIAN_POINT('Ctrl Pts',(-28.254539715307,-4.06101200920254,-0.812950610202758));
#48140=CARTESIAN_POINT('Ctrl Pts',(-28.1273462113148,-3.42764719991074,
-2.99402214660032));
#48141=CARTESIAN_POINT('Ctrl Pts',(-27.9206068189495,0.132734120902733,
-4.81264906024345));
#48142=CARTESIAN_POINT('Ctrl Pts',(-27.6819691538303,4.12035340306242,-2.4902241816421));
#48143=CARTESIAN_POINT('Ctrl Pts',(-27.4433314887111,4.32257108085691,2.11996606838733));
#48144=CARTESIAN_POINT('Ctrl Pts',(-27.2046938235918,0.55348171480276,4.78252270942354));
#48145=CARTESIAN_POINT('Ctrl Pts',(-26.9909791043302,-3.27734231397027,
3.2320385418624));
#48146=CARTESIAN_POINT('Ctrl Pts',(-26.8568102734416,-4.06004742651346,
0.929498100146529));
#48147=CARTESIAN_POINT('Ctrl Pts',(-26.8021873309261,-4.0673676331488,-0.00339676908166248));
#48148=CARTESIAN_POINT('Ctrl Pts',(-30.0683458050225,-1.79217368492187,
3.65473442716069));
#48149=CARTESIAN_POINT('Ctrl Pts',(-30.028572860836,-2.40105433738203,3.3561573610714));
#48150=CARTESIAN_POINT('Ctrl Pts',(-29.9490269724629,-3.45744192369399,
2.44891896771775));
#48151=CARTESIAN_POINT('Ctrl Pts',(-29.7899351957168,-4.48692818459232,
-0.165939112378094));
#48152=CARTESIAN_POINT('Ctrl Pts',(-29.5910704747841,-3.05580029857719,
-3.71995065683383));
#48153=CARTESIAN_POINT('Ctrl Pts',(-29.3524328096649,1.48524338711596,-4.58231611323432));
#48154=CARTESIAN_POINT('Ctrl Pts',(-29.1137951445456,4.65387018191312,-1.22765401651987));
#48155=CARTESIAN_POINT('Ctrl Pts',(-28.8751574794264,3.55090078994383,3.25125842872222));
#48156=CARTESIAN_POINT('Ctrl Pts',(-28.6365198143072,-0.816478135197904,
4.74503193420896));
#48157=CARTESIAN_POINT('Ctrl Pts',(-28.3978821491879,-4.4326431471991,1.8784345171529));
#48158=CARTESIAN_POINT('Ctrl Pts',(-28.1592444840687,-3.97698621643786,
-2.71342222480818));
#48159=CARTESIAN_POINT('Ctrl Pts',(-27.9206068189495,0.132734120902733,
-4.81264906024345));
#48160=CARTESIAN_POINT('Ctrl Pts',(-27.6819691538303,4.12035340306242,-2.4902241816421));
#48161=CARTESIAN_POINT('Ctrl Pts',(-27.4433314887111,4.32257108085691,2.11996606838733));
#48162=CARTESIAN_POINT('Ctrl Pts',(-27.2046938235918,0.55348171480276,4.78252270942354));
#48163=CARTESIAN_POINT('Ctrl Pts',(-26.9660561584726,-3.72408468243647,
3.05122444962453));
#48164=CARTESIAN_POINT('Ctrl Pts',(-26.7274184933533,-4.58024332037796,
-1.48330752890949));
#48165=CARTESIAN_POINT('Ctrl Pts',(-26.4887808282342,-1.22840035655279,
-4.65508935177024));
#48166=CARTESIAN_POINT('Ctrl Pts',(-26.2501431631149,3.25200474977257,-3.55010962682765));
#48167=CARTESIAN_POINT('Ctrl Pts',(-26.0115054979957,4.74470515142096,0.816452129912828));
#48168=CARTESIAN_POINT('Ctrl Pts',(-25.7728678328764,1.87831343359306,4.43291758398628));
#48169=CARTESIAN_POINT('Ctrl Pts',(-25.5342301677573,-2.71373612241715,
3.97673919017804));
#48170=CARTESIAN_POINT('Ctrl Pts',(-25.295592502638,-4.81260180106317,-0.132978803016981));
#48171=CARTESIAN_POINT('Ctrl Pts',(-25.0569548375188,-2.48999755919744,
-4.12052561435965));
#48172=CARTESIAN_POINT('Ctrl Pts',(-24.8183171723996,2.12023594681246,-4.32243201928095));
#48173=CARTESIAN_POINT('Ctrl Pts',(-24.5796795072803,4.78255033466597,-0.553201127887688));
#48174=CARTESIAN_POINT('Ctrl Pts',(-24.3410418421611,3.05100401366679,3.72427088853368));
#48175=CARTESIAN_POINT('Ctrl Pts',(-24.1024041770419,-1.48358370303888,
4.58015267461461));
#48176=CARTESIAN_POINT('Ctrl Pts',(-23.8637665119226,-4.65516222209766,
1.22812207654118));
#48177=CARTESIAN_POINT('Ctrl Pts',(-23.6251288468034,-3.54991501369184,
-3.25221809482192));
#48178=CARTESIAN_POINT('Ctrl Pts',(-23.3864911816842,0.816736872430108,
-4.74465594332464));
#48179=CARTESIAN_POINT('Ctrl Pts',(-23.1478535165649,4.43303010358293,-1.87804772118901));
#48180=CARTESIAN_POINT('Ctrl Pts',(-22.9092158514458,3.97657650355884,2.71397465949093));
#48181=CARTESIAN_POINT('Ctrl Pts',(-22.6705781863265,-0.13326743518637,
4.81259378419344));
#48182=CARTESIAN_POINT('Ctrl Pts',(-22.4319405212073,-4.12067491146169,
2.48975047251535));
#48183=CARTESIAN_POINT('Ctrl Pts',(-22.1933028560881,-4.32230487333938,
-2.12049515987218));
#48184=CARTESIAN_POINT('Ctrl Pts',(-21.9546651909688,-0.552914322524486,
-4.78258349567352));
#48185=CARTESIAN_POINT('Ctrl Pts',(-21.7160275258496,3.72445384229878,-3.05078067349642));
#48186=CARTESIAN_POINT('Ctrl Pts',(-21.4773898607304,4.58006369995296,1.4838583643783));
#48187=CARTESIAN_POINT('Ctrl Pts',(-21.2387521956112,1.22784291284316,4.65523586110807));
#48188=CARTESIAN_POINT('Ctrl Pts',(-21.0001145304919,-3.25243097005294,
3.54971997856348));
#48189=CARTESIAN_POINT('Ctrl Pts',(-20.7614768653727,-4.74460695685984,
-0.817021398792471));
#48190=CARTESIAN_POINT('Ctrl Pts',(-20.5228392002535,-1.87778187766528,
-4.43314271832978));
#48191=CARTESIAN_POINT('Ctrl Pts',(-20.2842015351343,2.71421312200688,-3.97641374475733));
#48192=CARTESIAN_POINT('Ctrl Pts',(-20.045563870015,4.81258578377826,0.133556036718511));
#48193=CARTESIAN_POINT('Ctrl Pts',(-19.8069262048958,2.48950335928912,4.12082420945821));
#48194=CARTESIAN_POINT('Ctrl Pts',(-19.5682885397766,-2.12075435614108,
4.32217770366716));
#48195=CARTESIAN_POINT('Ctrl Pts',(-19.3296508746574,-4.7826166442574,0.552627519438542));
#48196=CARTESIAN_POINT('Ctrl Pts',(-19.0910132095381,-3.05055731986689,
-3.72463678489262));
#48197=CARTESIAN_POINT('Ctrl Pts',(-18.8523755444189,1.48413301908516,-4.57997470766269));
#48198=CARTESIAN_POINT('Ctrl Pts',(-18.6137378792997,4.6553094840529,-1.22756374533297));
#48199=CARTESIAN_POINT('Ctrl Pts',(-18.3751002141804,3.54952493031783,3.25264383390203));
#48200=CARTESIAN_POINT('Ctrl Pts',(-18.1364625490612,-0.817305922033317,
4.74455795316888));
#48201=CARTESIAN_POINT('Ctrl Pts',(-17.897824883942,-4.43325531722986,1.87751602747407));
#48202=CARTESIAN_POINT('Ctrl Pts',(-17.6591872188228,-3.97625097160617,
-2.71445157480656));
#48203=CARTESIAN_POINT('Ctrl Pts',(-17.4205495537035,0.133844637744424,
-4.81257776603306));
#48204=CARTESIAN_POINT('Ctrl Pts',(-17.1819118885843,4.1209734926491,-2.4892562371223));
#48205=CARTESIAN_POINT('Ctrl Pts',(-16.9432742234651,4.32205051844462,2.12101354478971));
#48206=CARTESIAN_POINT('Ctrl Pts',(-16.7046365583459,0.55234071436891,4.78264977563894));
#48207=CARTESIAN_POINT('Ctrl Pts',(-16.4659988932266,-3.72481971409399,
3.05033395526876));
#48208=CARTESIAN_POINT('Ctrl Pts',(-16.2273612281074,-4.57988569890107,
-1.48440766845576));
#48209=CARTESIAN_POINT('Ctrl Pts',(-15.9887235629882,-1.22728457340874,
-4.65538309025602));
#48210=CARTESIAN_POINT('Ctrl Pts',(-15.7500858978689,3.25285668605437,-3.54932986930775));
#48211=CARTESIAN_POINT('Ctrl Pts',(-15.5114482327497,4.74450893241555,0.817590442335157));
#48212=CARTESIAN_POINT('Ctrl Pts',(-15.2728105676305,1.8772501705311,4.43336790018713));
#48213=CARTESIAN_POINT('Ctrl Pts',(-15.0341729025113,-2.71469001784463,
3.97608818415582));
#48214=CARTESIAN_POINT('Ctrl Pts',(-14.795535237392,-4.81256973098103,-0.134133238289019));
#48215=CARTESIAN_POINT('Ctrl Pts',(-14.5568975722728,-2.48900910600372,
-4.12112276102026));
#48216=CARTESIAN_POINT('Ctrl Pts',(-14.3182599071536,2.12127272581082,-4.32192331767929));
#48217=CARTESIAN_POINT('Ctrl Pts',(-14.0796222420344,4.78268288982128,-0.552053907312987));
#48218=CARTESIAN_POINT('Ctrl Pts',(-13.8409845769151,3.05011057970114,3.72500262990027));
#48219=CARTESIAN_POINT('Ctrl Pts',(-13.6023469117959,-1.48468231248816,
4.57979667366944));
#48220=CARTESIAN_POINT('Ctrl Pts',(-13.3637092466767,-4.65545667971761,
1.22700539707102));
#48221=CARTESIAN_POINT('Ctrl Pts',(-13.1250715815574,-3.5491347955337,-3.25306952650887));
#48222=CARTESIAN_POINT('Ctrl Pts',(-12.8864339164382,0.817874959696777,
-4.74445989460021));
#48223=CARTESIAN_POINT('Ctrl Pts',(-12.647796251319,4.43348046720131,-1.87698430683722));
#48224=CARTESIAN_POINT('Ctrl Pts',(-12.4091585861998,3.9759253824068,2.71492845112022));
#48225=CARTESIAN_POINT('Ctrl Pts',(-12.1705209210805,-0.134421838351238,
4.81256167862222));
#48226=CARTESIAN_POINT('Ctrl Pts',(-11.9318832559613,-4.12127201457121,
2.48876196593426));
#48227=CARTESIAN_POINT('Ctrl Pts',(-11.6932455908421,-4.32179610137161,
-2.12153189920346));
#48228=CARTESIAN_POINT('Ctrl Pts',(-11.4546079257229,-0.551767098271795,
-4.78271598680431));
#48229=CARTESIAN_POINT('Ctrl Pts',(-11.2159702606036,3.72518553231084,-3.04988719316482));
#48230=CARTESIAN_POINT('Ctrl Pts',(-10.9773325954844,4.57970763196809,1.48495695118139));
#48231=CARTESIAN_POINT('Ctrl Pts',(-10.7386949303652,1.22672621632081,4.65553025243742));
#48232=CARTESIAN_POINT('Ctrl Pts',(-10.500057265246,-3.25328235526483,3.54893970899639));
#48233=CARTESIAN_POINT('Ctrl Pts',(-10.2614196001267,-4.74441083972299,
-0.81815947411722));
#48234=CARTESIAN_POINT('Ctrl Pts',(-10.0227819350075,-1.8767184363934,-4.43359301827195));
#48235=CARTESIAN_POINT('Ctrl Pts',(-9.78414426988828,2.71516687463254,-3.97576256635973));
#48236=CARTESIAN_POINT('Ctrl Pts',(-9.54550660476906,4.8125536089566,0.134710437930172));
#48237=CARTESIAN_POINT('Ctrl Pts',(-9.30686893964983,2.48851481691486,4.12142125330121));
#48238=CARTESIAN_POINT('Ctrl Pts',(-9.06823127453061,-2.12179106496689,
4.32166886952238));
#48239=CARTESIAN_POINT('Ctrl Pts',(-8.82959360941138,-4.78274906658767,
0.551480287245675));
#48240=CARTESIAN_POINT('Ctrl Pts',(-8.59095594429215,-3.04966379566106,
-3.72536842132379));
#48241=CARTESIAN_POINT('Ctrl Pts',(-8.35231827917293,1.48523158453539,-4.57961857379977));
#48242=CARTESIAN_POINT('Ctrl Pts',(-8.1136806140537,4.65560380841346,-1.22644703115444));
#48243=CARTESIAN_POINT('Ctrl Pts',(-7.87504294893448,3.54874460969979,3.25349517231261));
#48244=CARTESIAN_POINT('Ctrl Pts',(-7.63640528381524,-0.818443985601727,
4.74436176780107));
#48245=CARTESIAN_POINT('Ctrl Pts',(-7.39776761869602,-4.43370555338651,
1.87645255916802));
#48246=CARTESIAN_POINT('Ctrl Pts',(-7.1591299535768,-3.97559973603849,-2.71540528831811));
#48247=CARTESIAN_POINT('Ctrl Pts',(-6.92049228845756,0.134999037069343,
-4.81254552210429));
#48248=CARTESIAN_POINT('Ctrl Pts',(-6.68185462333835,4.1215704771241,-2.48826765871595));
#48249=CARTESIAN_POINT('Ctrl Pts',(-6.44321695821911,4.32154162229638,2.12205022265777));
#48250=CARTESIAN_POINT('Ctrl Pts',(-6.20457929309988,0.551193473920355,
4.78278213002022));
#48251=CARTESIAN_POINT('Ctrl Pts',(-5.96594162798067,-3.72555129633323,
3.04944038556121));
#48252=CARTESIAN_POINT('Ctrl Pts',(-5.72730396286143,-4.57952950032639,
-1.48550620942175));
#48253=CARTESIAN_POINT('Ctrl Pts',(-5.48866629774222,-1.22616783934351,
-4.65567735364785));
#48254=CARTESIAN_POINT('Ctrl Pts',(-5.25002863262297,3.25370797337249,-3.54854948612432));
#48255=CARTESIAN_POINT('Ctrl Pts',(-5.01139096750376,4.74431268704714,0.818728472038551));
#48256=CARTESIAN_POINT('Ctrl Pts',(-4.77275330238453,1.87618665939981,4.43381811498155));
#48257=CARTESIAN_POINT('Ctrl Pts',(-4.5341156372653,-2.71564366192391,3.97543680999486));
#48258=CARTESIAN_POINT('Ctrl Pts',(-4.29547797214608,-4.812537476128,-0.135287479444116));
#48259=CARTESIAN_POINT('Ctrl Pts',(-4.05684030702684,-2.48802037989938,
-4.12171998606955));
#48260=CARTESIAN_POINT('Ctrl Pts',(-3.81820264190762,2.12230915839156,-4.32141378384957));
#48261=CARTESIAN_POINT('Ctrl Pts',(-3.5795649767884,4.78281558760628,-0.550907763508576));
#48262=CARTESIAN_POINT('Ctrl Pts',(-3.34092731166917,3.04921617498962,3.72573627855867));
#48263=CARTESIAN_POINT('Ctrl Pts',(-3.10228964654994,-1.48577931367711,
4.57943634031457));
#48264=CARTESIAN_POINT('Ctrl Pts',(-2.86365198143072,-4.65575379041631,
1.22589645476151));
#48265=CARTESIAN_POINT('Ctrl Pts',(-2.62501431631149,-3.54834876796527,
-3.25393575552032));
#48266=CARTESIAN_POINT('Ctrl Pts',(-2.38637665119226,0.819002242401078,
-4.74423481374027));
#48267=CARTESIAN_POINT('Ctrl Pts',(-2.14773898607304,4.43395122223712,-1.87597598138563));
#48268=CARTESIAN_POINT('Ctrl Pts',(-1.90910132095381,3.97523440584382,2.71598802545506));
#48269=CARTESIAN_POINT('Ctrl Pts',(-1.67046365583458,-0.135500177452599,
4.81232596646912));
#48270=CARTESIAN_POINT('Ctrl Pts',(-1.43182599071536,-4.12201486774593,
2.48816358626208));
#48271=CARTESIAN_POINT('Ctrl Pts',(-1.19318832559613,-4.32100676816269,
-2.12331775762679));
#48272=CARTESIAN_POINT('Ctrl Pts',(-0.9545506604769,-0.551158953576692,
-4.78140835552346));
#48273=CARTESIAN_POINT('Ctrl Pts',(-0.715912995357679,3.72696190987269,
-3.05177387808086));
#48274=CARTESIAN_POINT('Ctrl Pts',(-0.477275330238447,4.57725222884596,
1.49154630755727));
#48275=CARTESIAN_POINT('Ctrl Pts',(-0.278410609305757,1.78830202401348,
4.11849926473408));
#48276=CARTESIAN_POINT('Ctrl Pts',(-0.119318832559607,-1.02190788268887,
4.1117895186236));
#48277=CARTESIAN_POINT('Ctrl Pts',(-0.0397729441865359,-2.25151393523441,
3.45825666525491));
#48278=CARTESIAN_POINT('Ctrl Pts',(0.,-2.75129702511903,2.99988915288068));
#48279=CARTESIAN_POINT('Ctrl Pts',(-29.9038972033484,-1.91758108071807,
3.91047455474608));
#48280=CARTESIAN_POINT('Ctrl Pts',(-29.8641242591618,-2.56906817116925,
3.59100455142768));
#48281=CARTESIAN_POINT('Ctrl Pts',(-29.7845783707887,-3.69937650370433,
2.62028213013966));
#48282=CARTESIAN_POINT('Ctrl Pts',(-29.6254865940426,-4.80090108994663,
-0.177550705673484));
#48283=CARTESIAN_POINT('Ctrl Pts',(-29.4266218731099,-3.26962999641403,
-3.98025429162597));
#48284=CARTESIAN_POINT('Ctrl Pts',(-29.1879842079907,1.58917332809701,-4.90296379114112));
#48285=CARTESIAN_POINT('Ctrl Pts',(-28.9493465428715,4.97952485746032,-1.31355913522901));
#48286=CARTESIAN_POINT('Ctrl Pts',(-28.7107088777522,3.79937515632038,3.47876531381764));
#48287=CARTESIAN_POINT('Ctrl Pts',(-28.472071212633,-0.873611211930994,
5.07706565551933));
#48288=CARTESIAN_POINT('Ctrl Pts',(-28.2334335475137,-4.74281745578375,
2.00987801671541));
#48289=CARTESIAN_POINT('Ctrl Pts',(-27.9947958823946,-4.25527592056482,
-2.90329400887223));
#48290=CARTESIAN_POINT('Ctrl Pts',(-27.7561582172753,0.142022194137876,
-5.14941429154002));
#48291=CARTESIAN_POINT('Ctrl Pts',(-27.5175205521561,4.40867522944874,-2.66447767738084));
#48292=CARTESIAN_POINT('Ctrl Pts',(-27.2788828870369,4.62504309400783,2.26831074393387));
#48293=CARTESIAN_POINT('Ctrl Pts',(-27.0402452219176,0.59221161082695,5.1171798486122));
#48294=CARTESIAN_POINT('Ctrl Pts',(-26.8016075567984,-3.98467759576748,
3.26473395232318));
#48295=CARTESIAN_POINT('Ctrl Pts',(-26.5629698916792,-4.90074595455584,
-1.58710200816697));
#48296=CARTESIAN_POINT('Ctrl Pts',(-26.3243322265599,-1.31435770042331,
-4.9808293387569));
#48297=CARTESIAN_POINT('Ctrl Pts',(-26.0856945614408,3.47956385870106,-3.79852863154653));
#48298=CARTESIAN_POINT('Ctrl Pts',(-25.8470568963215,5.07671600609805,0.873583386925484));
#48299=CARTESIAN_POINT('Ctrl Pts',(-25.6084192312023,2.00974846033062,4.74311109629157));
#48300=CARTESIAN_POINT('Ctrl Pts',(-25.3697815660831,-2.90362987147378,
4.25501160863666));
#48301=CARTESIAN_POINT('Ctrl Pts',(-25.1311439009638,-5.14936372539749,
-0.14228399788883));
#48302=CARTESIAN_POINT('Ctrl Pts',(-24.8925062358446,-2.66423519702527,
-4.40885949123555));
#48303=CARTESIAN_POINT('Ctrl Pts',(-24.6538685707254,2.26859950710815,-4.62489430159482));
#48304=CARTESIAN_POINT('Ctrl Pts',(-24.4152309056061,5.11720940693162,-0.591911389835893));
#48305=CARTESIAN_POINT('Ctrl Pts',(-24.1765932404869,3.26449809135411,3.98487683164073));
#48306=CARTESIAN_POINT('Ctrl Pts',(-23.9379555753677,-1.58739750758757,
4.90064896585306));
#48307=CARTESIAN_POINT('Ctrl Pts',(-23.6993179102485,-4.9809073081872,1.31405994776134));
#48308=CARTESIAN_POINT('Ctrl Pts',(-23.4606802451292,-3.79832040035196,
-3.47979213257527));
#48309=CARTESIAN_POINT('Ctrl Pts',(-23.22204258001,0.873888054307114,-5.07666335466403));
#48310=CARTESIAN_POINT('Ctrl Pts',(-22.9834049148908,4.74323148944965,-2.00946415469484));
#48311=CARTESIAN_POINT('Ctrl Pts',(-22.7447672497716,4.25483753801745,2.90388510018491));
#48312=CARTESIAN_POINT('Ctrl Pts',(-22.5061295846524,-0.142592827101065,
5.14935514754711));
#48313=CARTESIAN_POINT('Ctrl Pts',(-22.2674919195331,-4.40901923540582,
2.66397082044679));
#48314=CARTESIAN_POINT('Ctrl Pts',(-22.0288542544139,-4.624758258613,-2.26887685860782));
#48315=CARTESIAN_POINT('Ctrl Pts',(-21.7902165892947,-0.591604515260647,
-5.11724488838146));
#48316=CARTESIAN_POINT('Ctrl Pts',(-21.5515789241754,3.98507258759985,-3.26425912295005));
#48317=CARTESIAN_POINT('Ctrl Pts',(-21.3129412590562,4.90055376518737,1.58769138836067));
#48318=CARTESIAN_POINT('Ctrl Pts',(-21.074303593937,1.31376124957698,4.98098610008909));
#48319=CARTESIAN_POINT('Ctrl Pts',(-20.8356659288178,-3.4800199037556,3.7981117176359));
#48320=CARTESIAN_POINT('Ctrl Pts',(-20.5970282636985,-5.0766109403702,-0.874192490408381));
#48321=CARTESIAN_POINT('Ctrl Pts',(-20.3583905985793,-2.00917970876428,
-4.74335198441606));
#48322=CARTESIAN_POINT('Ctrl Pts',(-20.11975293346,2.90414024912104,-4.25466339016496));
#48323=CARTESIAN_POINT('Ctrl Pts',(-19.8811152683409,5.14934658730268,0.142901623532206));
#48324=CARTESIAN_POINT('Ctrl Pts',(-19.6424776032216,2.66370641546674,4.40917898053317));
#48325=CARTESIAN_POINT('Ctrl Pts',(-19.4038399381024,-2.26915419214175,
4.62462219023996));
#48326=CARTESIAN_POINT('Ctrl Pts',(-19.1652022729832,-5.11728035653827,
0.591297643122014));
#48327=CARTESIAN_POINT('Ctrl Pts',(-18.9265646078639,-3.26402014014505,
-3.985268331606));
#48328=CARTESIAN_POINT('Ctrl Pts',(-18.6879269427447,1.58798526203712,-4.90045854565949));
#48329=CARTESIAN_POINT('Ctrl Pts',(-18.4492892776255,4.98106487480121,-1.31346254731367));
#48330=CARTESIAN_POINT('Ctrl Pts',(-18.2106516125063,3.79790302088468,3.48024766275753));
#48331=CARTESIAN_POINT('Ctrl Pts',(-17.9720139473871,-0.874496923169711,
5.07655850764482));
#48332=CARTESIAN_POINT('Ctrl Pts',(-17.7333762822678,-4.74347246242682,
2.00889525569968));
#48333=CARTESIAN_POINT('Ctrl Pts',(-17.4947386171486,-4.25448922695873,
-2.90439538766098));
#48334=CARTESIAN_POINT('Ctrl Pts',(-17.2561009520293,0.143210419421708,
-5.14933800851558));
#48335=CARTESIAN_POINT('Ctrl Pts',(-17.0174632869101,4.40933870981885,-2.66344200092047));
#48336=CARTESIAN_POINT('Ctrl Pts',(-16.7788256217909,4.62448610522848,2.26943151752217));
#48337=CARTESIAN_POINT('Ctrl Pts',(-16.5401879566717,0.590990768860884,
5.11731580628902));
#48338=CARTESIAN_POINT('Ctrl Pts',(-16.3015502915524,-3.98546406128254,
3.2637811456039));
#48339=CARTESIAN_POINT('Ctrl Pts',(-16.0629126264332,-4.90036330850768,
-1.58827913000388));
#48340=CARTESIAN_POINT('Ctrl Pts',(-15.824274961314,-1.31316384032749,-4.98114363160013));
#48341=CARTESIAN_POINT('Ctrl Pts',(-15.5856372961948,3.48047540924424,-3.79769431047581));
#48342=CARTESIAN_POINT('Ctrl Pts',(-15.3469996310755,5.07650605666312,0.874801352786364));
#48343=CARTESIAN_POINT('Ctrl Pts',(-15.1083619659563,2.00861079541087,4.74359292337918));
#48344=CARTESIAN_POINT('Ctrl Pts',(-14.8697243008371,-2.90465051575626,
4.25431504845271));
#48345=CARTESIAN_POINT('Ctrl Pts',(-14.6310866357179,-5.1493294112106,-0.143519214796206));
#48346=CARTESIAN_POINT('Ctrl Pts',(-14.3924489705986,-2.66317757679605,
-4.4094984232478));
#48347=CARTESIAN_POINT('Ctrl Pts',(-14.1538113054794,2.26970883474132,-4.62435000358661));
#48348=CARTESIAN_POINT('Ctrl Pts',(-13.9151736403602,5.11735123763705,-0.590683892474468));
#48349=CARTESIAN_POINT('Ctrl Pts',(-13.676535975241,3.26354213932567,3.98565977662667));
#48350=CARTESIAN_POINT('Ctrl Pts',(-13.4378983101217,-1.58857299225892,
4.90026805373337));
#48351=CARTESIAN_POINT('Ctrl Pts',(-13.1992606450025,-4.98122237048603,
1.31286512861896));
#48352=CARTESIAN_POINT('Ctrl Pts',(-12.9606229798833,-3.79748558640983,
-3.48070314321456));
#48353=CARTESIAN_POINT('Ctrl Pts',(-12.7219853147641,0.87510577925706,-5.0764535874255));
#48354=CARTESIAN_POINT('Ctrl Pts',(-12.4833476496448,4.74371336727283,-2.00832632789875));
#48355=CARTESIAN_POINT('Ctrl Pts',(-12.2447099845256,4.25414085464746,2.90490563340592));
#48356=CARTESIAN_POINT('Ctrl Pts',(-12.0060723194064,-0.143828009654572,
5.14932079538778));
#48357=CARTESIAN_POINT('Ctrl Pts',(-11.7674346542871,-4.40965812081948,
2.66291314309442));
#48358=CARTESIAN_POINT('Ctrl Pts',(-11.5287969891679,-4.6242138853148,-2.26998614379823));
#48359=CARTESIAN_POINT('Ctrl Pts',(-11.2901593240487,-0.590377013963862,
-5.11738665058224));
#48360=CARTESIAN_POINT('Ctrl Pts',(-11.0515216589295,3.98585547763773,-3.26330312131122));
#48361=CARTESIAN_POINT('Ctrl Pts',(-10.8128839938102,4.90017278133687,1.58886684880117));
#48362=CARTESIAN_POINT('Ctrl Pts',(-10.574246328691,1.31256641218918,4.98130109145864));
#48363=CARTESIAN_POINT('Ctrl Pts',(-10.3356086635718,-3.48093086466773,
3.79727684868749));
#48364=CARTESIAN_POINT('Ctrl Pts',(-10.0969709984526,-5.07640109993208,
-0.875410202580779));
#48365=CARTESIAN_POINT('Ctrl Pts',(-9.85833333333333,-2.00804185316436,
-4.74383379410727));
#48366=CARTESIAN_POINT('Ctrl Pts',(-9.61969566821411,2.90516074060913,-4.25396664554368));
#48367=CARTESIAN_POINT('Ctrl Pts',(-9.38105800309488,5.14931216104712,0.14413680399584));
#48368=CARTESIAN_POINT('Ctrl Pts',(-9.14242033797565,2.66264869981656,4.40981780253313));
#48369=CARTESIAN_POINT('Ctrl Pts',(-8.90378267285642,-2.27026344469205,
4.62407775041392));
#48370=CARTESIAN_POINT('Ctrl Pts',(-8.6651450077372,-5.11742204512421,0.590070133329444));
#48371=CARTESIAN_POINT('Ctrl Pts',(-8.42650734261798,-3.26306409156187,
-3.98605116431367));
#48372=CARTESIAN_POINT('Ctrl Pts',(-8.18786967749874,1.58916069963059,-4.90007749132113));
#48373=CARTESIAN_POINT('Ctrl Pts',(-7.94923201237953,4.98137979451584,-1.31226769103422));
#48374=CARTESIAN_POINT('Ctrl Pts',(-7.71059434726029,3.79706809731301,3.48115857359343));
#48375=CARTESIAN_POINT('Ctrl Pts',(-7.47195668214107,-0.875714622763106,
5.07634859420128));
#48376=CARTESIAN_POINT('Ctrl Pts',(-7.23331901702185,-4.74395420386913,
2.00775737117387));
#48377=CARTESIAN_POINT('Ctrl Pts',(-6.99468135190261,-4.25379242116686,
-2.90541583729795));
#48378=CARTESIAN_POINT('Ctrl Pts',(-6.7560436867834,0.144445597866564,-5.14930350831713));
#48379=CARTESIAN_POINT('Ctrl Pts',(-6.51740602166415,4.40997746829655,-2.66238424671687));
#48380=CARTESIAN_POINT('Ctrl Pts',(-6.27876835654495,4.62394159906029,2.27054073694845));
#48381=CARTESIAN_POINT('Ctrl Pts',(-6.04013069142569,0.58976325023493,5.11745742217124));
#48382=CARTESIAN_POINT('Ctrl Pts',(-5.80149302630649,-3.9862468360062,3.26282504833503));
#48383=CARTESIAN_POINT('Ctrl Pts',(-5.56285536118725,-4.89998218492935,
-1.58945454139984));
#48384=CARTESIAN_POINT('Ctrl Pts',(-5.32421769606804,-1.31196896276975,
-4.98145848607974));
#48385=CARTESIAN_POINT('Ctrl Pts',(-5.08558003094879,3.48138626541249,-3.79685931996075));
#48386=CARTESIAN_POINT('Ctrl Pts',(-4.84694236582958,5.07629607902044,0.876019016145047));
#48387=CARTESIAN_POINT('Ctrl Pts',(-4.60830470071035,2.00747286506312,4.74407464196444));
#48388=CARTESIAN_POINT('Ctrl Pts',(-4.36966703559112,-2.90567089110244,
4.25361809436949));
#48389=CARTESIAN_POINT('Ctrl Pts',(-4.1310293704719,-5.14929489932346,-0.144754224003302));
#48390=CARTESIAN_POINT('Ctrl Pts',(-3.89239170535267,-2.66211966455929,
-4.41013743913397));
#48391=CARTESIAN_POINT('Ctrl Pts',(-3.65375404023344,2.27081779171631,-4.62380481511515));
#48392=CARTESIAN_POINT('Ctrl Pts',(-3.41511637511422,5.11749322095267,-0.589457547230361));
#48393=CARTESIAN_POINT('Ctrl Pts',(-3.17647870999498,3.26258514862341,3.98644476236722));
#48394=CARTESIAN_POINT('Ctrl Pts',(-2.93784104487577,-1.58974675613189,
4.89988250604351));
#48395=CARTESIAN_POINT('Ctrl Pts',(-2.69920337975654,-4.98154027151287,
1.31167858804524));
#48396=CARTESIAN_POINT('Ctrl Pts',(-2.46056571463731,-3.79664455654379,
-3.48162998662147));
#48397=CARTESIAN_POINT('Ctrl Pts',(-2.22192804951808,0.876311943595137,
-5.07621275652709));
#48398=CARTESIAN_POINT('Ctrl Pts',(-1.98329038439886,4.74421706340335,-2.00724744484995));
#48399=CARTESIAN_POINT('Ctrl Pts',(-1.74465271927963,4.25340152698323,2.90603935147979));
#48400=CARTESIAN_POINT('Ctrl Pts',(-1.5060150541604,-0.144981805559941,
5.14906858927122));
#48401=CARTESIAN_POINT('Ctrl Pts',(-1.26737738904118,-4.41045295516259,
2.66227289179059));
#48402=CARTESIAN_POINT('Ctrl Pts',(-1.02873972392195,-4.62336931849601,
-2.27189696770677));
#48403=CARTESIAN_POINT('Ctrl Pts',(-0.790102058802722,-0.589726314329404,
-5.11598751777173));
#48404=CARTESIAN_POINT('Ctrl Pts',(-0.551464393683503,3.98775615726128,
-3.26532182704867));
#48405=CARTESIAN_POINT('Ctrl Pts',(-0.312826728564268,4.89754556132347,
1.5959172955446));
#48406=CARTESIAN_POINT('Ctrl Pts',(-0.11396200763158,1.91343850024653,4.40669134774724));
#48407=CARTESIAN_POINT('Ctrl Pts',(0.0451297691145716,-1.09341591083915,
4.39951208699472));
#48408=CARTESIAN_POINT('Ctrl Pts',(0.124675657487642,-2.40906367586066,
3.7002482568252));
#48409=CARTESIAN_POINT('Ctrl Pts',(0.164448601674178,-2.94381909922654,
3.20980646698106));
#48410=CARTESIAN_POINT('Ctrl Pts',(-29.7394486016742,-2.04298847651428,
4.16621468233147));
#48411=CARTESIAN_POINT('Ctrl Pts',(-29.6996756574876,-2.73708200495646,
3.82585174178397));
#48412=CARTESIAN_POINT('Ctrl Pts',(-29.6201297691146,-3.94131108371467,
2.79164529256157));
#48413=CARTESIAN_POINT('Ctrl Pts',(-29.4610379923684,-5.11487399530094,
-0.189162298968872));
#48414=CARTESIAN_POINT('Ctrl Pts',(-29.2621732714358,-3.48345969425087,
-4.2405579264181));
#48415=CARTESIAN_POINT('Ctrl Pts',(-29.0235356063165,1.69310326907807,-5.22361146904792));
#48416=CARTESIAN_POINT('Ctrl Pts',(-28.7848979411973,5.30517953300752,-1.39946425393815));
#48417=CARTESIAN_POINT('Ctrl Pts',(-28.546260276078,4.04784952269694,3.70627219891307));
#48418=CARTESIAN_POINT('Ctrl Pts',(-28.3076226109588,-0.930744288664083,
5.4090993768297));
#48419=CARTESIAN_POINT('Ctrl Pts',(-28.0689849458396,-5.05299176436839,
2.14132151627792));
#48420=CARTESIAN_POINT('Ctrl Pts',(-27.8303472807204,-4.53356562469179,
-3.09316579293629));
#48421=CARTESIAN_POINT('Ctrl Pts',(-27.5917096156012,0.151310267373015,
-5.48617952283658));
#48422=CARTESIAN_POINT('Ctrl Pts',(-27.3530719504819,4.69699705583506,-2.83873117311958));
#48423=CARTESIAN_POINT('Ctrl Pts',(-27.1144342853627,4.92751510715875,2.4166554194804));
#48424=CARTESIAN_POINT('Ctrl Pts',(-26.8757966202434,0.630941506851146,
5.45183698780086));
#48425=CARTESIAN_POINT('Ctrl Pts',(-26.6371589551242,-4.2452705090985,3.47824345502183));
#48426=CARTESIAN_POINT('Ctrl Pts',(-26.398521290005,-5.22124858873371,-1.69089648742445));
#48427=CARTESIAN_POINT('Ctrl Pts',(-26.1598836248858,-1.40031504429382,
-5.30656932574355));
#48428=CARTESIAN_POINT('Ctrl Pts',(-25.9212459597666,3.70712296762955,-4.0469476362654));
#48429=CARTESIAN_POINT('Ctrl Pts',(-25.6826082946473,5.40872686077514,0.930714643938138));
#48430=CARTESIAN_POINT('Ctrl Pts',(-25.4439706295281,2.14118348706817,5.05330460859686));
#48431=CARTESIAN_POINT('Ctrl Pts',(-25.2053329644089,-3.09352362053041,
4.53328402709528));
#48432=CARTESIAN_POINT('Ctrl Pts',(-24.9666952992896,-5.4861256497318,-0.151589192760673));
#48433=CARTESIAN_POINT('Ctrl Pts',(-24.7280576341705,-2.8384728348531,-4.69719336811145));
#48434=CARTESIAN_POINT('Ctrl Pts',(-24.4894199690512,2.41696306740383,-4.92735658390869));
#48435=CARTESIAN_POINT('Ctrl Pts',(-24.250782303932,5.45186847919727,-0.6306216517841));
#48436=CARTESIAN_POINT('Ctrl Pts',(-24.0121446388127,3.47799216904142,4.24548277474778));
#48437=CARTESIAN_POINT('Ctrl Pts',(-23.7735069736936,-1.69121131213625,
5.22114525709151));
#48438=CARTESIAN_POINT('Ctrl Pts',(-23.5348693085742,-5.30665239427673,
1.39999781898149));
#48439=CARTESIAN_POINT('Ctrl Pts',(-23.2962316434551,-4.04672578701207,
-3.70736617032861));
#48440=CARTESIAN_POINT('Ctrl Pts',(-23.0575939783358,0.931039236184116,
-5.40867076600343));
#48441=CARTESIAN_POINT('Ctrl Pts',(-22.8189563132166,5.05343287531637,-2.14088058820066));
#48442=CARTESIAN_POINT('Ctrl Pts',(-22.5803186480974,4.53309857247606,3.09379554087889));
#48443=CARTESIAN_POINT('Ctrl Pts',(-22.3416809829782,-0.151918219015756,
5.48611651090078));
#48444=CARTESIAN_POINT('Ctrl Pts',(-22.1030433178589,-4.69736355934995,
2.83819116837823));
#48445=CARTESIAN_POINT('Ctrl Pts',(-21.8644056527397,-4.92721164388661,
-2.41725855734347));
#48446=CARTESIAN_POINT('Ctrl Pts',(-21.6257679876205,-0.630294707996812,
-5.45190628108939));
#48447=CARTESIAN_POINT('Ctrl Pts',(-21.3871303225012,4.24569133290092,-3.47773757240369));
#48448=CARTESIAN_POINT('Ctrl Pts',(-21.1484926573821,5.22104383042178,1.69152441234305));
#48449=CARTESIAN_POINT('Ctrl Pts',(-20.9098549922628,1.39967958631079,5.3067363390701));
#48450=CARTESIAN_POINT('Ctrl Pts',(-20.6712173271436,-3.70760883745824,
4.04650345670832));
#48451=CARTESIAN_POINT('Ctrl Pts',(-20.4325796620243,-5.40861492388057,
-0.931363582024293));
#48452=CARTESIAN_POINT('Ctrl Pts',(-20.1939419969051,-2.14057753986328,
-5.05356125050234));
#48453=CARTESIAN_POINT('Ctrl Pts',(-19.9553043317859,3.09406737623519,-4.5329130355726));
#48454=CARTESIAN_POINT('Ctrl Pts',(-19.7166666666667,5.48610739082711,0.152247210345901));
#48455=CARTESIAN_POINT('Ctrl Pts',(-19.4780290015475,2.83790947164436,4.69753375160813));
#48456=CARTESIAN_POINT('Ctrl Pts',(-19.2393913364282,-2.41755402814241,
4.92706667681276));
#48457=CARTESIAN_POINT('Ctrl Pts',(-19.000753671309,-5.45194406881915,0.62996776680549));
#48458=CARTESIAN_POINT('Ctrl Pts',(-18.7621160061898,-3.4774829604232,-4.24589987831939));
#48459=CARTESIAN_POINT('Ctrl Pts',(-18.5234783410705,1.69183750498908,-5.22094238365629));
#48460=CARTESIAN_POINT('Ctrl Pts',(-18.2848406759513,5.30682026554953,-1.39936134929439));
#48461=CARTESIAN_POINT('Ctrl Pts',(-18.0462030108321,4.04628111145152,3.70785149161303));
#48462=CARTESIAN_POINT('Ctrl Pts',(-17.8075653457129,-0.931687924306101,
5.40855906212076));
#48463=CARTESIAN_POINT('Ctrl Pts',(-17.5689276805936,-5.05368960762378,
2.14027448392529));
#48464=CARTESIAN_POINT('Ctrl Pts',(-17.3302900154744,-4.53272748231129,
-3.0943392005154));
#48465=CARTESIAN_POINT('Ctrl Pts',(-17.0916523503552,0.152576201098992,
-5.4860982509981));
#48466=CARTESIAN_POINT('Ctrl Pts',(-16.8530146852359,4.6977039269886,-2.83762776471865));
#48467=CARTESIAN_POINT('Ctrl Pts',(-16.6143770201167,4.92692169201234,2.41784949025462));
#48468=CARTESIAN_POINT('Ctrl Pts',(-16.3757393549975,0.62964082335285,5.45198183693909));
#48469=CARTESIAN_POINT('Ctrl Pts',(-16.1371016898783,-4.24610840847109,
3.47722833593904));
#48470=CARTESIAN_POINT('Ctrl Pts',(-15.898464024759,-5.2208409181143,-1.69215059155202));
#48471=CARTESIAN_POINT('Ctrl Pts',(-15.6598263596398,-1.39904310724623,
-5.30690417294424));
#48472=CARTESIAN_POINT('Ctrl Pts',(-15.4211886945206,3.70809413243411,-4.04605875164388));
#48473=CARTESIAN_POINT('Ctrl Pts',(-15.1825510294014,5.40850318091069,0.932012263237568));
#48474=CARTESIAN_POINT('Ctrl Pts',(-14.9439133642821,2.13997142029063,5.05381794657124));
#48475=CARTESIAN_POINT('Ctrl Pts',(-14.7052756991629,-3.09461101366789,
4.53254191274959));
#48476=CARTESIAN_POINT('Ctrl Pts',(-14.4666380340437,-5.48608909144016,
-0.152905191303383));
#48477=CARTESIAN_POINT('Ctrl Pts',(-14.2280003689245,-2.83734604758839,
-4.69787408547534));
#48478=CARTESIAN_POINT('Ctrl Pts',(-13.9893627038052,2.41814494367183,-4.92677668949392));
#48479=CARTESIAN_POINT('Ctrl Pts',(-13.750725038686,5.45201958545282,-0.629313877635948));
#48480=CARTESIAN_POINT('Ctrl Pts',(-13.5120873735668,3.47697369895021,4.24631692335307));
#48481=CARTESIAN_POINT('Ctrl Pts',(-13.2734497084476,-1.69246367202968,
5.2207394337973));
#48482=CARTESIAN_POINT('Ctrl Pts',(-13.0348120433283,-5.30698806125446,
1.3987248601669));
#48483=CARTESIAN_POINT('Ctrl Pts',(-12.7961743782091,-4.04583637728596,
-3.70833675992024));
#48484=CARTESIAN_POINT('Ctrl Pts',(-12.5575367130899,0.932336598817344,
-5.40844728025078));
#48485=CARTESIAN_POINT('Ctrl Pts',(-12.3188990479706,5.05394626734435,-2.13966834896028));
#48486=CARTESIAN_POINT('Ctrl Pts',(-12.0802613828514,4.53235632688813,3.09488281569163));
#48487=CARTESIAN_POINT('Ctrl Pts',(-11.8416237177322,-0.153234180957902,
5.48607991215335));
#48488=CARTESIAN_POINT('Ctrl Pts',(-11.602986052613,-4.69804422706777,2.83706432025457));
#48489=CARTESIAN_POINT('Ctrl Pts',(-11.3643483874937,-4.92663166925799,
-2.41844038839298));
#48490=CARTESIAN_POINT('Ctrl Pts',(-11.1257107223745,-0.628986929655938,
-5.45205731436018));
#48491=CARTESIAN_POINT('Ctrl Pts',(-10.8870730572553,4.24652542296462,-3.47671904945761));
#48492=CARTESIAN_POINT('Ctrl Pts',(-10.6484353921361,5.22063793070565,1.69277674642096));
#48493=CARTESIAN_POINT('Ctrl Pts',(-10.4097977270168,1.39840660805754,5.30707193047986));
#48494=CARTESIAN_POINT('Ctrl Pts',(-10.1711600618976,-3.70857937407062,
4.04561398837858));
#48495=CARTESIAN_POINT('Ctrl Pts',(-9.93252239677838,-5.40839136014118,
-0.93266093104433));
#48496=CARTESIAN_POINT('Ctrl Pts',(-9.69388473165915,-2.13936526993532,
-5.05407456994261));
#48497=CARTESIAN_POINT('Ctrl Pts',(-9.45524706653993,3.09515460658571,-4.53217072472762));
#48498=CARTESIAN_POINT('Ctrl Pts',(-9.21660940142069,5.48607071313765,0.153563170061505));
#48499=CARTESIAN_POINT('Ctrl Pts',(-8.97797173630149,2.83678258271826,4.69821435176505));
#48500=CARTESIAN_POINT('Ctrl Pts',(-8.73933407118223,-2.41873582441721,
4.92648663130547));
#48501=CARTESIAN_POINT('Ctrl Pts',(-8.50069640606304,-5.45209502366077,
0.628659979413207));
#48502=CARTESIAN_POINT('Ctrl Pts',(-8.26205874094379,-3.47646438746268,
-4.24673390730354));
#48503=CARTESIAN_POINT('Ctrl Pts',(-8.02342107582457,1.69308981472579,-5.22053640884249));
#48504=CARTESIAN_POINT('Ctrl Pts',(-7.78478341070535,5.30715578061822,-1.398088350914));
#48505=CARTESIAN_POINT('Ctrl Pts',(-7.54614574558612,4.04539158492623,3.70882197487425));
#48506=CARTESIAN_POINT('Ctrl Pts',(-7.30750808046689,-0.932985259924489,
5.40833542060147));
#48507=CARTESIAN_POINT('Ctrl Pts',(-7.06887041534766,-5.05420285435175,
2.13906218317974));
#48508=CARTESIAN_POINT('Ctrl Pts',(-6.83023275022844,-4.53198510629524,
-3.09542638627781));
#48509=CARTESIAN_POINT('Ctrl Pts',(-6.5915950851092,0.153892158663785,-5.48606149452997));
#48510=CARTESIAN_POINT('Ctrl Pts',(-6.35295741998999,4.69838445946899,-2.83650083471779));
#48511=CARTESIAN_POINT('Ctrl Pts',(-6.11431975487076,4.92634157582419,2.41903125123913));
#48512=CARTESIAN_POINT('Ctrl Pts',(-5.87568208975152,0.628333026549508,
5.45213271432227));
#48513=CARTESIAN_POINT('Ctrl Pts',(-5.63704442463231,-4.24694237567916,
3.47620971110884));
#48514=CARTESIAN_POINT('Ctrl Pts',(-5.39840675951308,-5.22043486953231,
-1.69340287337793));
#48515=CARTESIAN_POINT('Ctrl Pts',(-5.15976909439385,-1.39777008619599,
-5.30723961851162));
#48516=CARTESIAN_POINT('Ctrl Pts',(-4.92113142927462,3.70906455745249,-4.04516915379718));
#48517=CARTESIAN_POINT('Ctrl Pts',(-4.6824937641554,5.40827947099373,0.933309560251545));
#48518=CARTESIAN_POINT('Ctrl Pts',(-4.44385609903617,2.13875907072644,5.05433116894732));
#48519=CARTESIAN_POINT('Ctrl Pts',(-4.20521843391694,-3.09569812028096,
4.53179937874414));
#48520=CARTESIAN_POINT('Ctrl Pts',(-3.96658076879772,-5.48605232251892,
-0.154220968562498));
#48521=CARTESIAN_POINT('Ctrl Pts',(-3.72794310367849,-2.83621894921919,
-4.69855489219838));
#48522=CARTESIAN_POINT('Ctrl Pts',(-3.48930543855926,2.41932642504106,-4.92619584638074));
#48523=CARTESIAN_POINT('Ctrl Pts',(-3.25066777344004,5.45217085429907,-0.62800733095214));
#48524=CARTESIAN_POINT('Ctrl Pts',(-3.01203010832081,3.47595412225719,4.24715324617577));
#48525=CARTESIAN_POINT('Ctrl Pts',(-2.77339244320158,-1.69371419858668,
5.22032867177245));
#48526=CARTESIAN_POINT('Ctrl Pts',(-2.53475477808237,-5.30732675260943,
1.39746072132896));
#48527=CARTESIAN_POINT('Ctrl Pts',(-2.29611711296313,-4.04494034512231,
-3.70932421772263));
#48528=CARTESIAN_POINT('Ctrl Pts',(-2.05747944784391,0.933621644789192,
-5.40819069931389));
#48529=CARTESIAN_POINT('Ctrl Pts',(-1.81884178272468,5.05448290456958,-2.13851890831426));
#48530=CARTESIAN_POINT('Ctrl Pts',(-1.58020411760545,4.53156864812263,3.09609067750451));
#48531=CARTESIAN_POINT('Ctrl Pts',(-1.34156645248623,-0.154463433667277,
5.48581121207333));
#48532=CARTESIAN_POINT('Ctrl Pts',(-1.102928787367,-4.69889104257927,2.83638219731909));
#48533=CARTESIAN_POINT('Ctrl Pts',(-0.86429112224777,-4.92573186882932,
-2.42047617778675));
#48534=CARTESIAN_POINT('Ctrl Pts',(-0.625653457128544,-0.628293675082119,
-5.45056668002));
#48535=CARTESIAN_POINT('Ctrl Pts',(-0.387015792009324,4.24855040464988,
-3.47886977601648));
#48536=CARTESIAN_POINT('Ctrl Pts',(-0.14837812689009,5.21783889380097,1.70028828353193));
#48537=CARTESIAN_POINT('Ctrl Pts',(0.0504865940425981,2.03857497647958,
4.69488343076037));
#48538=CARTESIAN_POINT('Ctrl Pts',(0.209578370788749,-1.16492393898944,
4.68723465536585));
#48539=CARTESIAN_POINT('Ctrl Pts',(0.28912425916182,-2.56661341648691,3.94223984839548));
#48540=CARTESIAN_POINT('Ctrl Pts',(0.328897203348356,-3.13634117333406,
3.41972378108145));
#48541=CARTESIAN_POINT('Ctrl Pts',(-29.575,-2.16839587231048,4.42195480991686));
#48542=CARTESIAN_POINT('Ctrl Pts',(-29.5352270558135,-2.90509583874368,
4.06069893214025));
#48543=CARTESIAN_POINT('Ctrl Pts',(-29.4556811674404,-4.18324566372502,
2.96300845498348));
#48544=CARTESIAN_POINT('Ctrl Pts',(-29.2965893906942,-5.42884690065524,
-0.200773892264263));
#48545=CARTESIAN_POINT('Ctrl Pts',(-29.0977246697616,-3.69728939208772,
-4.50086156121024));
#48546=CARTESIAN_POINT('Ctrl Pts',(-28.8590870046423,1.79703321005912,-5.54425914695472));
#48547=CARTESIAN_POINT('Ctrl Pts',(-28.6204493395231,5.63083420855472,-1.48536937264729));
#48548=CARTESIAN_POINT('Ctrl Pts',(-28.3818116744038,4.2963238890735,3.93377908400849));
#48549=CARTESIAN_POINT('Ctrl Pts',(-28.1431740092847,-0.987877365397176,
5.74113309814008));
#48550=CARTESIAN_POINT('Ctrl Pts',(-27.9045363441654,-5.36316607295304,
2.27276501584044));
#48551=CARTESIAN_POINT('Ctrl Pts',(-27.6658986790462,-4.81185532881875,
-3.28303757700034));
#48552=CARTESIAN_POINT('Ctrl Pts',(-27.4272610139269,0.160598340608156,
-5.82294475413315));
#48553=CARTESIAN_POINT('Ctrl Pts',(-27.1886233488077,4.98531888222138,-3.01298466885832));
#48554=CARTESIAN_POINT('Ctrl Pts',(-26.9499856836885,5.22998712030967,2.56500009502694));
#48555=CARTESIAN_POINT('Ctrl Pts',(-26.7113480185693,0.669671402875337,
5.78649412698952));
#48556=CARTESIAN_POINT('Ctrl Pts',(-26.4727103534501,-4.50586342242951,
3.69175295772048));
#48557=CARTESIAN_POINT('Ctrl Pts',(-26.2340726883308,-5.54175122291158,
-1.79469096668193));
#48558=CARTESIAN_POINT('Ctrl Pts',(-25.9954350232117,-1.48627238816434,
-5.6323093127302));
#48559=CARTESIAN_POINT('Ctrl Pts',(-25.7567973580923,3.93468207655805,-4.29536664098428));
#48560=CARTESIAN_POINT('Ctrl Pts',(-25.5181596929732,5.74073771545223,0.987845900950795));
#48561=CARTESIAN_POINT('Ctrl Pts',(-25.2795220278539,2.27261851380574,5.36349812090215));
#48562=CARTESIAN_POINT('Ctrl Pts',(-25.0408843627347,-3.28341736958705,
4.8115564455539));
#48563=CARTESIAN_POINT('Ctrl Pts',(-24.8022466976155,-5.82288757406612,
-0.160894387632515));
#48564=CARTESIAN_POINT('Ctrl Pts',(-24.5636090324963,-3.01271047268094,
-4.98552724498736));
#48565=CARTESIAN_POINT('Ctrl Pts',(-24.324971367377,2.56532662769952,-5.22981886622255));
#48566=CARTESIAN_POINT('Ctrl Pts',(-24.0863337022578,5.78652755146292,-0.669331913732308));
#48567=CARTESIAN_POINT('Ctrl Pts',(-23.8476960371386,3.69148624672874,4.50608871785483));
#48568=CARTESIAN_POINT('Ctrl Pts',(-23.6090583720193,-1.79502511668494,
5.54164154832996));
#48569=CARTESIAN_POINT('Ctrl Pts',(-23.3704207069001,-5.63239748036626,
1.48593569020165));
#48570=CARTESIAN_POINT('Ctrl Pts',(-23.1317830417809,-4.29513117367219,
-3.93494020808196));
#48571=CARTESIAN_POINT('Ctrl Pts',(-22.8931453766617,0.988190418061122,
-5.74067817734282));
#48572=CARTESIAN_POINT('Ctrl Pts',(-22.6545077115424,5.36363426118309,-2.27229702170649));
#48573=CARTESIAN_POINT('Ctrl Pts',(-22.4158700464232,4.81135960693467,3.28370598157288));
#48574=CARTESIAN_POINT('Ctrl Pts',(-22.177232381304,-0.161243610930449,
5.82287787425445));
#48575=CARTESIAN_POINT('Ctrl Pts',(-21.9385947161848,-4.98570788329408,
3.01241151630967));
#48576=CARTESIAN_POINT('Ctrl Pts',(-21.6999570510655,-5.22966502916022,
-2.56564025607911));
#48577=CARTESIAN_POINT('Ctrl Pts',(-21.4613193859463,-0.668984900732974,
-5.78656767379734));
#48578=CARTESIAN_POINT('Ctrl Pts',(-21.2226817208271,4.50631007820199,-3.69121602185732));
#48579=CARTESIAN_POINT('Ctrl Pts',(-20.9840440557079,5.54153389565618,1.79535743632542));
#48580=CARTESIAN_POINT('Ctrl Pts',(-20.7454063905886,1.4855979230446,5.63248657805113));
#48581=CARTESIAN_POINT('Ctrl Pts',(-20.5067687254694,-3.93519777116089,
4.29489519578073));
#48582=CARTESIAN_POINT('Ctrl Pts',(-20.2681310603502,-5.74061890739093,
-0.988534673640199));
#48583=CARTESIAN_POINT('Ctrl Pts',(-20.0294933952309,-2.27197537096228,
-5.36377051658862));
#48584=CARTESIAN_POINT('Ctrl Pts',(-19.7908557301117,3.28399450334934,-4.81116268098024));
#48585=CARTESIAN_POINT('Ctrl Pts',(-19.5522180649925,5.82286819435154,0.161592797159601));
#48586=CARTESIAN_POINT('Ctrl Pts',(-19.3135803998733,3.01211252782197,4.98588852268307));
#48587=CARTESIAN_POINT('Ctrl Pts',(-19.074942734754,-2.56595386414308,5.22951116338557));
#48588=CARTESIAN_POINT('Ctrl Pts',(-18.8363050696348,-5.78660778110002,
0.668637890488963));
#48589=CARTESIAN_POINT('Ctrl Pts',(-18.5976674045156,-3.69094578070135,
-4.50653142503277));
#48590=CARTESIAN_POINT('Ctrl Pts',(-18.3590297393963,1.79568974794104,-5.54142622165309));
#48591=CARTESIAN_POINT('Ctrl Pts',(-18.1203920742771,5.63257565629784,-1.48526015127511));
#48592=CARTESIAN_POINT('Ctrl Pts',(-17.8817544091579,4.29465920201836,3.93545532046853));
#48593=CARTESIAN_POINT('Ctrl Pts',(-17.6431167440387,-0.988878925442489,
5.74055961659669));
#48594=CARTESIAN_POINT('Ctrl Pts',(-17.4044790789195,-5.36390675282074,
2.2716537121509));
#48595=CARTESIAN_POINT('Ctrl Pts',(-17.1658414138002,-4.81096573766385,
-3.28428301336982));
#48596=CARTESIAN_POINT('Ctrl Pts',(-16.927203748681,0.161941982776275,-5.82285849348062));
#48597=CARTESIAN_POINT('Ctrl Pts',(-16.6885660835618,4.98606914415835,-3.01181352851682));
#48598=CARTESIAN_POINT('Ctrl Pts',(-16.4499284184425,5.22935727879621,2.56626746298708));
#48599=CARTESIAN_POINT('Ctrl Pts',(-16.2112907533233,0.668290877844823,
5.78664786758917));
#48600=CARTESIAN_POINT('Ctrl Pts',(-15.9726530882041,-4.50675275565964,
3.69067552627418));
#48601=CARTESIAN_POINT('Ctrl Pts',(-15.7340154230849,-5.5413185277209,-1.79602205310015));
#48602=CARTESIAN_POINT('Ctrl Pts',(-15.4953777579656,-1.48492237416498,
-5.63266471428835));
#48603=CARTESIAN_POINT('Ctrl Pts',(-15.2567400928464,3.93571285562398,-4.29442319281195));
#48604=CARTESIAN_POINT('Ctrl Pts',(-15.0181024277272,5.74050030515826,0.989223173688781));
#48605=CARTESIAN_POINT('Ctrl Pts',(-14.779464762608,2.2713320451704,5.36404296976328));
#48606=CARTESIAN_POINT('Ctrl Pts',(-14.5408270974887,-3.28457151157951,
4.81076877704648));
#48607=CARTESIAN_POINT('Ctrl Pts',(-14.3021894323695,-5.82284877166972,
-0.16229116781057));
#48608=CARTESIAN_POINT('Ctrl Pts',(-14.0635517672503,-3.01151451838073,
-4.98624974770287));
#48609=CARTESIAN_POINT('Ctrl Pts',(-13.824914102131,2.56658105260234,-5.22920337540123));
#48610=CARTESIAN_POINT('Ctrl Pts',(-13.5862764370118,5.78668793326858,-0.667943862797434));
#48611=CARTESIAN_POINT('Ctrl Pts',(-13.3476387718926,3.69040525857474,4.50697407007948));
#48612=CARTESIAN_POINT('Ctrl Pts',(-13.1090011067734,-1.79635435180044,
5.54121081386123));
#48613=CARTESIAN_POINT('Ctrl Pts',(-12.8703634416541,-5.63275375202288,
1.48458459171485));
#48614=CARTESIAN_POINT('Ctrl Pts',(-12.6317257765349,-4.29418716816209,
-3.93597037662593));
#48615=CARTESIAN_POINT('Ctrl Pts',(-12.3930881114157,0.989567418377627,
-5.74044097307606));
#48616=CARTESIAN_POINT('Ctrl Pts',(-12.1544504462965,5.36417916741587,-2.27101037002181));
#48617=CARTESIAN_POINT('Ctrl Pts',(-11.9158127811772,4.81057179912879,3.28485999797732));
#48618=CARTESIAN_POINT('Ctrl Pts',(-11.677175116058,-0.162640352261234,
5.82283902891891));
#48619=CARTESIAN_POINT('Ctrl Pts',(-11.4385374509388,-4.98643033331604,
3.01121549741473));
#48620=CARTESIAN_POINT('Ctrl Pts',(-11.1998997858196,-5.22904945320118,
-2.56689463298775));
#48621=CARTESIAN_POINT('Ctrl Pts',(-10.9612621207004,-0.667596845348008,
-5.78672797813811));
#48622=CARTESIAN_POINT('Ctrl Pts',(-10.7226244555811,4.50719536829151,-3.69013497760401));
#48623=CARTESIAN_POINT('Ctrl Pts',(-10.4839867904619,5.54110308007444,1.79668664404075));
#48624=CARTESIAN_POINT('Ctrl Pts',(-10.2453491253427,1.48424680392591,5.63284276950108));
#48625=CARTESIAN_POINT('Ctrl Pts',(-10.0067114602234,-3.93622788347351,
4.29395112806967));
#48626=CARTESIAN_POINT('Ctrl Pts',(-9.7680737951042,-5.74038162035028,-0.989911659507881));
#48627=CARTESIAN_POINT('Ctrl Pts',(-9.52943612998498,-2.27068868670629,
-5.36431534577795));
#48628=CARTESIAN_POINT('Ctrl Pts',(-9.29079846486575,3.2851484725623,-4.81037480391155));
#48629=CARTESIAN_POINT('Ctrl Pts',(-9.05216079974653,5.82282926522816,0.162989536127165));
#48630=CARTESIAN_POINT('Ctrl Pts',(-8.81352313462729,3.01091646561997,4.98661090099698));
#48631=CARTESIAN_POINT('Ctrl Pts',(-8.57488546950808,-2.56720820414237,
5.22889551219701));
#48632=CARTESIAN_POINT('Ctrl Pts',(-8.33624780438884,-5.78676800219732,
0.667249825496974));
#48633=CARTESIAN_POINT('Ctrl Pts',(-8.09761013926962,-3.6898646833635,-4.50741665029341));
#48634=CARTESIAN_POINT('Ctrl Pts',(-7.85897247415039,1.79701892982099,-5.54099532636385));
#48635=CARTESIAN_POINT('Ctrl Pts',(-7.62033480903117,5.6329317667206,-1.48390901079377));
#48636=CARTESIAN_POINT('Ctrl Pts',(-7.38169714391194,4.29371507253944,3.93648537615507));
#48637=CARTESIAN_POINT('Ctrl Pts',(-7.14305947879271,-0.990255897085868,
5.74032224700168));
#48638=CARTESIAN_POINT('Ctrl Pts',(-6.90442181367349,-5.36445150483438,
2.27036699518559));
#48639=CARTESIAN_POINT('Ctrl Pts',(-6.66578414855427,-4.81017779142361,
-3.28543693525765));
#48640=CARTESIAN_POINT('Ctrl Pts',(-6.42714648343502,0.163338719461003,
-5.82281948074281));
#48641=CARTESIAN_POINT('Ctrl Pts',(-6.18850881831581,4.98679145064144,-3.0106174227187));
#48642=CARTESIAN_POINT('Ctrl Pts',(-5.94987115319658,5.2287415525881,2.56752176552981));
#48643=CARTESIAN_POINT('Ctrl Pts',(-5.71123348807735,0.666902802864079,
5.78680800647329));
#48644=CARTESIAN_POINT('Ctrl Pts',(-5.47259582295812,-4.50763791535213,
3.68959437388266));
#48645=CARTESIAN_POINT('Ctrl Pts',(-5.2339581578389,-5.54088755413527,-1.79735120535602));
#48646=CARTESIAN_POINT('Ctrl Pts',(-4.99532049271967,-1.48357120962223,
-5.63302075094351));
#48647=CARTESIAN_POINT('Ctrl Pts',(-4.75668282760044,3.93674284949249,-4.29347898763361));
#48648=CARTESIAN_POINT('Ctrl Pts',(-4.51804516248123,5.74026286296703,0.990600104358038));
#48649=CARTESIAN_POINT('Ctrl Pts',(-4.27940749736199,2.27004527638976,5.36458769593022));
#48650=CARTESIAN_POINT('Ctrl Pts',(-4.04076983224277,-3.28572534945949,
4.80998066311877));
#48651=CARTESIAN_POINT('Ctrl Pts',(-3.80213216712354,-5.82280974571438,
-0.16368771312168));
#48652=CARTESIAN_POINT('Ctrl Pts',(-3.56349450200431,-3.0103182338791,-4.98697234526281));
#48653=CARTESIAN_POINT('Ctrl Pts',(-3.32485683688509,2.56783505836581,-5.22858687764632));
#48654=CARTESIAN_POINT('Ctrl Pts',(-3.08621917176586,5.78684848764546,-0.666557114673928));
#48655=CARTESIAN_POINT('Ctrl Pts',(-2.84758150664664,3.68932309589099,4.50786172998432));
#48656=CARTESIAN_POINT('Ctrl Pts',(-2.60894384152741,-1.79768164104147,
5.54077483750139));
#48657=CARTESIAN_POINT('Ctrl Pts',(-2.37030617640819,-5.63311323370599,
1.48324285461269));
#48658=CARTESIAN_POINT('Ctrl Pts',(-2.13166851128895,-4.29323613370083,
-3.93701844882378));
#48659=CARTESIAN_POINT('Ctrl Pts',(-1.89303084616973,0.990931345983249,
-5.7401686421007));
#48660=CARTESIAN_POINT('Ctrl Pts',(-1.65439318105051,5.36474874573582,-2.26979037177858));
#48661=CARTESIAN_POINT('Ctrl Pts',(-1.41575551593128,4.80973576926203,3.28614200352924));
#48662=CARTESIAN_POINT('Ctrl Pts',(-1.17711785081205,-0.163945061774615,
5.82255383487542));
#48663=CARTESIAN_POINT('Ctrl Pts',(-0.938480185692826,-4.98732912999593,
3.0104915028476));
#48664=CARTESIAN_POINT('Ctrl Pts',(-0.699842520573593,-5.22809441916263,
-2.56905538786673));
#48665=CARTESIAN_POINT('Ctrl Pts',(-0.461204855454365,-0.666861035834833,
-5.78514584226827));
#48666=CARTESIAN_POINT('Ctrl Pts',(-0.222567190335147,4.50934465203849,
-3.6924177249843));
#48667=CARTESIAN_POINT('Ctrl Pts',(0.016070474784088,5.53813222627847,1.80465927151925));
#48668=CARTESIAN_POINT('Ctrl Pts',(0.214935195716776,2.16371145271264,4.98307551377353));
#48669=CARTESIAN_POINT('Ctrl Pts',(0.374026972462927,-1.23643196713973,
4.97495722373696));
#48670=CARTESIAN_POINT('Ctrl Pts',(0.453572860835998,-2.72416315711316,
4.18423143996577));
#48671=CARTESIAN_POINT('Ctrl Pts',(0.493345805022534,-3.32886324744157,
3.62964109518183));
#48672=CARTESIAN_POINT('',(0.,4.77615934004779,1.20163511869213));
#48673=CARTESIAN_POINT('Ctrl Pts',(1.27675647831893E-15,4.78202092340378,
1.20708649626074));
#48674=CARTESIAN_POINT('Ctrl Pts',(1.54554986213376E-15,4.74680432306751,
1.31141193121661));
#48675=CARTESIAN_POINT('Ctrl Pts',(-1.2200289887242E-15,4.70790283853999,
1.41429721113204));
#48676=CARTESIAN_POINT('Ctrl Pts',(-1.0547118733939E-15,4.66526667899838,
1.51554882908261));
#48677=CARTESIAN_POINT('Ctrl Pts',(-8.36120983837436E-16,4.60951044466766,
1.64795777485803));
#48678=CARTESIAN_POINT('Ctrl Pts',(1.7406482083505E-15,4.5473685300075,
1.77757428418243));
#48679=CARTESIAN_POINT('Ctrl Pts',(9.99200722162641E-16,4.47921304648044,
1.90412989878513));
#48680=CARTESIAN_POINT('Ctrl Pts',(5.41776053129587E-16,4.43716556493129,
1.98220644662206));
#48681=CARTESIAN_POINT('Ctrl Pts',(-6.14882986343895E-16,4.39282838373583,
2.05911740148693));
#48682=CARTESIAN_POINT('Ctrl Pts',(-5.55111512312578E-16,4.34628172346416,
2.13479307691151));
#48683=CARTESIAN_POINT('Ctrl Pts',(-5.12735502418862E-16,4.31328167171442,
2.18844464268728));
#48684=CARTESIAN_POINT('Ctrl Pts',(7.5446052363616E-15,4.27917094813153,
2.24147520753853));
#48685=CARTESIAN_POINT('Ctrl Pts',(7.32747196252603E-15,4.24397679643589,
2.29385817644388));
#48686=CARTESIAN_POINT('Ctrl Pts',(7.25033478916171E-15,4.23147398038747,
2.31246736554886));
#48687=CARTESIAN_POINT('Ctrl Pts',(1.1248375135418E-15,4.21883292816165,
2.33099695996549));
#48688=CARTESIAN_POINT('Ctrl Pts',(9.43689570931383E-16,4.20605981758978,
2.34943854375472));
#48689=CARTESIAN_POINT('Ctrl Pts',(-2.0749684309091E-16,4.12488731768033,
2.46663391680332));
#48690=CARTESIAN_POINT('Ctrl Pts',(1.20832359191774E-15,4.03848405238999,
2.58013740696103));
#48691=CARTESIAN_POINT('Ctrl Pts',(2.72004641033163E-15,3.94721695353052,
2.68968900864157));
#48692=CARTESIAN_POINT('Ctrl Pts',(4.18855970728122E-15,3.85855853902716,
2.79610930064906));
#48693=CARTESIAN_POINT('Ctrl Pts',(1.88596569557423E-15,3.7653095628778,
2.89880063696627));
#48694=CARTESIAN_POINT('Ctrl Pts',(-4.9960036108132E-16,3.66777702457831,
2.99748899318237));
#48695=CARTESIAN_POINT('Ctrl Pts',(-2.58697066065493E-15,3.58243605356626,
3.08384130487147));
#48696=CARTESIAN_POINT('Ctrl Pts',(-1.9993502333868E-15,3.49381479608703,
3.16712847527816));
#48697=CARTESIAN_POINT('Ctrl Pts',(-3.60822483003176E-15,3.40210641955682,
3.24714114973565));
#48698=CARTESIAN_POINT('Ctrl Pts',(-3.93090312754506E-15,3.38371325027676,
3.26318861150008));
#48699=CARTESIAN_POINT('Ctrl Pts',(-8.00198331154243E-15,3.36519389765555,
3.27910584403603));
#48700=CARTESIAN_POINT('Ctrl Pts',(-7.93809462606987E-15,3.34656787360052,
3.29487610387643));
#48701=CARTESIAN_POINT('Ctrl Pts',(-7.56940933970987E-15,3.23908184596226,
3.38588224560911));
#48702=CARTESIAN_POINT('Ctrl Pts',(9.69472795872832E-15,3.12792305846971,
3.4721065544235));
#48703=CARTESIAN_POINT('Ctrl Pts',(8.60422844084496E-15,3.01343370374636,
3.55329630674216));
#48704=CARTESIAN_POINT('Ctrl Pts',(7.5193745599244E-15,2.89953707311163,
3.63406573070746));
#48705=CARTESIAN_POINT('Ctrl Pts',(1.54891535256133E-14,2.78234353560187,
3.70985298607676));
#48706=CARTESIAN_POINT('Ctrl Pts',(1.29340982368831E-14,2.66216592270983,
3.78036399292217));
#48707=CARTESIAN_POINT('Ctrl Pts',(1.04428067996356E-14,2.54498745723108,
3.84911533006954));
#48708=CARTESIAN_POINT('Ctrl Pts',(9.06092894879522E-15,2.42497131537325,
3.91285066923259));
#48709=CARTESIAN_POINT('Ctrl Pts',(1.10467190950203E-14,2.30239503897639,
3.9712502394403));
#48710=CARTESIAN_POINT('Ctrl Pts',(1.25360617046891E-14,2.21046283167875,
4.01504991709609));
#48711=CARTESIAN_POINT('Ctrl Pts',(1.14694130650435E-14,2.11709024431302,
4.05584730347416));
#48712=CARTESIAN_POINT('Ctrl Pts',(1.04916075827077E-14,2.02239293435179,
4.09348836738669));
#48713=CARTESIAN_POINT('Ctrl Pts',(1.01019433215215E-14,1.98465520635888,
4.10848866921022));
#48714=CARTESIAN_POINT('Ctrl Pts',(1.58900622876451E-14,1.94670710034945,
4.12298752598548));
#48715=CARTESIAN_POINT('Ctrl Pts',(1.63757896132211E-14,1.90855596787325,
4.1369744095719));
#48716=CARTESIAN_POINT('Ctrl Pts',(1.66667902990066E-14,1.8856995109076,
4.14535399313934));
#48717=CARTESIAN_POINT('Ctrl Pts',(-3.74501732116749E-15,1.8627701834264,
4.15354980834729));
#48718=CARTESIAN_POINT('Ctrl Pts',(-4.38538094726937E-15,1.83976957424201,
4.16155951178909));
#48719=CARTESIAN_POINT('Ctrl Pts',(-4.90190327326717E-15,1.8212171023791,
4.16802020144052));
#48720=CARTESIAN_POINT('Ctrl Pts',(9.50430379515547E-15,1.80262497700585,
4.17435742449665));
#48721=CARTESIAN_POINT('Ctrl Pts',(9.38138455808257E-15,1.784001553863,
4.18056782352897));
#48722=CARTESIAN_POINT('Ctrl Pts',(8.54497039802425E-15,1.65727692396478,
4.22282699966724));
#48723=CARTESIAN_POINT('Ctrl Pts',(7.75693411885647E-15,1.52899676754921,
4.25925543233605));
#48724=CARTESIAN_POINT('Ctrl Pts',(7.66053886991358E-15,1.39943774817802,
4.28958765120325));
#48725=CARTESIAN_POINT('Ctrl Pts',(7.59729281300995E-15,1.31443255133079,
4.30948897685494));
#48726=CARTESIAN_POINT('Ctrl Pts',(1.2113674912629E-15,1.2288765362281,
4.32676501145738));
#48727=CARTESIAN_POINT('Ctrl Pts',(1.0547118733939E-15,1.14284625117365,
4.34132862407617));
#48728=CARTESIAN_POINT('Ctrl Pts',(8.68428161696615E-16,1.01006019941622,
4.36380727351629));
#48729=CARTESIAN_POINT('Ctrl Pts',(4.15203095003235E-15,0.876143569520156,
4.37982636972409));
#48730=CARTESIAN_POINT('Ctrl Pts',(4.94049245958195E-15,0.741565045486008,
4.38948206088079));
#48731=CARTESIAN_POINT('Ctrl Pts',(5.72761812915067E-15,0.607214529250332,
4.39912139301662));
#48732=CARTESIAN_POINT('Ctrl Pts',(1.10432148395374E-14,0.472203479324102,
4.40241856966672));
#48733=CARTESIAN_POINT('Ctrl Pts',(1.14075415780235E-14,0.337013667456073,
4.39942001130783));
#48734=CARTESIAN_POINT('Ctrl Pts',(1.15826238267446E-14,0.272046335208114,
4.39797901265212));
#48735=CARTESIAN_POINT('Ctrl Pts',(9.92588300807085E-15,0.207038030887552,
4.39508336506645));
#48736=CARTESIAN_POINT('Ctrl Pts',(1.02695629777827E-14,0.142044407157708,
4.39073446593813));
#48737=CARTESIAN_POINT('Ctrl Pts',(1.03617903745677E-14,0.124603202396043,
4.38956742776066));
#48738=CARTESIAN_POINT('Ctrl Pts',(4.4841957176862E-15,0.107164810159224,
4.38829579344102));
#48739=CARTESIAN_POINT('Ctrl Pts',(4.69069227904129E-15,0.0897419980454403,
4.38692068583962));
#48740=CARTESIAN_POINT('Ctrl Pts',(6.25118297356027E-15,-0.0419218708223804,
4.37652902313169));
#48741=CARTESIAN_POINT('Ctrl Pts',(-5.49571088697169E-16,-0.17288184694056,
4.36022055581769));
#48742=CARTESIAN_POINT('Ctrl Pts',(8.60422844084496E-16,-0.302702434116573,
4.33812072407467));
#48743=CARTESIAN_POINT('Ctrl Pts',(2.26456079903569E-15,-0.431983851255918,
4.31611267721224));
#48744=CARTESIAN_POINT('Ctrl Pts',(1.75511797657805E-14,-0.560136154997887,
4.28836093293126));
#48745=CARTESIAN_POINT('Ctrl Pts',(1.48214773787458E-14,-0.686713620784949,
4.25494071804226));
#48746=CARTESIAN_POINT('Ctrl Pts',(1.23397585715295E-14,-0.80179198203985,
4.22455660868837));
#48747=CARTESIAN_POINT('Ctrl Pts',(-2.35332166972068E-15,-0.915568901399882,
4.18948643033132));
#48748=CARTESIAN_POINT('Ctrl Pts',(-5.99520433297585E-15,-1.02768958167645,
4.14975498030284));
#48749=CARTESIAN_POINT('Ctrl Pts',(-8.67136215211543E-15,-1.11007901125274,
4.12055919326328));
#48750=CARTESIAN_POINT('Ctrl Pts',(6.0234625807556E-15,-1.19157368030025,
4.08884575090022));
#48751=CARTESIAN_POINT('Ctrl Pts',(4.84334794492725E-15,-1.27206424811892,
4.05464924064616));
#48752=CARTESIAN_POINT('Ctrl Pts',(4.19130181297638E-15,-1.31653752369003,
4.03575471840195));
#48753=CARTESIAN_POINT('Ctrl Pts',(7.59797375755575E-15,-1.36070412856013,
4.01610202232593));
#48754=CARTESIAN_POINT('Ctrl Pts',(7.70217223333702E-15,-1.40454455699869,
3.99569611765175));
#48755=CARTESIAN_POINT('Ctrl Pts',(7.75609059491098E-15,-1.42723014864851,
3.98513691380336));
#48756=CARTESIAN_POINT('Ctrl Pts',(-7.46205461605755E-15,-1.44982838930905,
3.97437601887541));
#48757=CARTESIAN_POINT('Ctrl Pts',(-8.10462807976364E-15,-1.47233648956831,
3.96341406098191));
#48758=CARTESIAN_POINT('Ctrl Pts',(-8.59111957832261E-15,-1.48937734177172,
3.95511477751635));
#48759=CARTESIAN_POINT('Ctrl Pts',(5.51713801836789E-15,-1.50635977342605,
3.94670349607368));
#48760=CARTESIAN_POINT('Ctrl Pts',(5.68989300120393E-15,-1.52327621904144,
3.93818410740871));
#48761=CARTESIAN_POINT('Ctrl Pts',(6.8760654734775E-15,-1.63942813424693,
3.87968817201454));
#48762=CARTESIAN_POINT('Ctrl Pts',(4.1445617132442E-15,-1.75256979369442,
3.81605162100472));
#48763=CARTESIAN_POINT('Ctrl Pts',(4.69069227904129E-15,-1.8623899266764,
3.74745962400277));
#48764=CARTESIAN_POINT('Ctrl Pts',(5.22545435247209E-15,-1.96992399580907,
3.68029546796622));
#48765=CARTESIAN_POINT('Ctrl Pts',(5.0249819177936E-15,-2.07427385910768,
3.60837941731036));
#48766=CARTESIAN_POINT('Ctrl Pts',(6.27276008913213E-15,-2.17511326369545,
3.53184659443599));
#48767=CARTESIAN_POINT('Ctrl Pts',(7.56032798375268E-15,-2.27916828152011,
3.45287325776349));
#48768=CARTESIAN_POINT('Ctrl Pts',(-5.02292661063484E-15,-2.37948625932775,
3.36898369722969));
#48769=CARTESIAN_POINT('Ctrl Pts',(-4.60395610524245E-15,-2.47566144275777,
3.28029126749575));
#48770=CARTESIAN_POINT('Ctrl Pts',(-4.21077948966132E-15,-2.56591560775799,
3.19705918098456));
#48771=CARTESIAN_POINT('Ctrl Pts',(5.23948052523968E-15,-2.65252139743486,
3.10959674386589));
#48772=CARTESIAN_POINT('Ctrl Pts',(5.31345800691696E-15,-2.73509733308257,
3.0179750570285));
#48773=CARTESIAN_POINT('Ctrl Pts',(5.31831121266542E-15,-2.74051463029901,
3.01196432393565));
#48774=CARTESIAN_POINT('Ctrl Pts',(2.3894388675905E-18,-2.74591456605251,
3.00593568341939));
#48775=CARTESIAN_POINT('Ctrl Pts',(-1.38777878078145E-17,-2.75129702511903,
2.99988915288068));
#48776=CARTESIAN_POINT('Ctrl Pts',(-0.808841525903593,-4.91703434725887,
-0.0013692803956027));
#48777=CARTESIAN_POINT('Ctrl Pts',(-0.772508524126926,-4.91859034973346,
-0.753815327274128));
#48778=CARTESIAN_POINT('Ctrl Pts',(-0.73617552235026,-4.75666071795644,
-1.50557039925234));
#48779=CARTESIAN_POINT('Ctrl Pts',(-0.699842520573593,-4.42776130708021,
-2.1751459818146));
#48780=CARTESIAN_POINT('Ctrl Pts',(-0.620296632200516,-3.70768329138669,
-3.64108553933391));
#48781=CARTESIAN_POINT('Ctrl Pts',(-0.540750743827439,-2.18727216361073,
-4.71311569080111));
#48782=CARTESIAN_POINT('Ctrl Pts',(-0.461204855454364,-0.564365651743867,
-4.90034274698736));
#48783=CARTESIAN_POINT('Ctrl Pts',(-0.381658967081291,1.05854086012297,
-5.08756980317361));
#48784=CARTESIAN_POINT('Ctrl Pts',(-0.302113078708221,2.78394275608069,
-4.38999376407897));
#48785=CARTESIAN_POINT('Ctrl Pts',(-0.222567190335146,3.81810829976624,
-3.12502624511441));
#48786=CARTESIAN_POINT('Ctrl Pts',(-0.148378126890099,4.78263047309757,
-1.94524489575994));
#48787=CARTESIAN_POINT('Ctrl Pts',(-0.0741890634450472,5.14588079318518,
-0.271918139693744));
#48788=CARTESIAN_POINT('Ctrl Pts',(1.31838984174237E-15,4.78202092340378,
1.20708649626074));
#48789=CARTESIAN_POINT('',(-29.575,-2.36230756092323,-3.31488661006752));
#48790=CARTESIAN_POINT('Ctrl Pts',(-29.575,-2.36826780557339,-3.31775809990771));
#48791=CARTESIAN_POINT('Ctrl Pts',(-29.575,-2.44830306796112,-3.27276844726465));
#48792=CARTESIAN_POINT('Ctrl Pts',(-29.575,-2.52655779909889,-3.22498344987375));
#48793=CARTESIAN_POINT('Ctrl Pts',(-29.575,-2.60286326628888,-3.1744359090982));
#48794=CARTESIAN_POINT('Ctrl Pts',(-29.575,-2.70499541343267,-3.106779828055));
#48795=CARTESIAN_POINT('Ctrl Pts',(-29.575,-2.80363682654566,-3.03417684171155));
#48796=CARTESIAN_POINT('Ctrl Pts',(-29.575,-2.89869614562238,-2.9570330604008));
#48797=CARTESIAN_POINT('Ctrl Pts',(-29.575,-2.96224887403662,-2.90545791942454));
#48798=CARTESIAN_POINT('Ctrl Pts',(-29.575,-3.02420016779924,-2.85185208063885));
#48799=CARTESIAN_POINT('Ctrl Pts',(-29.575,-3.08451737823507,-2.79632528183713));
#48800=CARTESIAN_POINT('Ctrl Pts',(-29.575,-3.11868159705198,-2.76487439591655));
#48801=CARTESIAN_POINT('Ctrl Pts',(-29.575,-3.15232148638354,-2.73280706845916));
#48802=CARTESIAN_POINT('Ctrl Pts',(-29.575,-3.18543039276807,-2.70014206823866));
#48803=CARTESIAN_POINT('Ctrl Pts',(-29.575,-3.20694675023592,-2.67891419035985));
#48804=CARTESIAN_POINT('Ctrl Pts',(-29.575,-3.22824271002023,-2.65742973362904));
#48805=CARTESIAN_POINT('Ctrl Pts',(-29.575,-3.24929376278556,-2.63571743596404));
#48806=CARTESIAN_POINT('Ctrl Pts',(-29.575,-3.33714135858251,-2.54511041643103));
#48807=CARTESIAN_POINT('Ctrl Pts',(-29.575,-3.42079165100367,-2.45047748262222));
#48808=CARTESIAN_POINT('Ctrl Pts',(-29.575,-3.50014704916176,-2.35224076529156));
#48809=CARTESIAN_POINT('Ctrl Pts',(-29.575,-3.58105807397336,-2.25207828538672));
#48810=CARTESIAN_POINT('Ctrl Pts',(-29.575,-3.65750467553342,-2.14816887047587));
#48811=CARTESIAN_POINT('Ctrl Pts',(-29.575,-3.72935582339607,-2.04091404902635));
#48812=CARTESIAN_POINT('Ctrl Pts',(-29.575,-3.76079070058598,-1.99399006464218));
#48813=CARTESIAN_POINT('Ctrl Pts',(-29.575,-3.79134558154171,-1.94642520728123));
#48814=CARTESIAN_POINT('Ctrl Pts',(-29.575,-3.82100749080666,-1.89825079032625));
#48815=CARTESIAN_POINT('Ctrl Pts',(-29.575,-3.83626358617193,-1.87347310347317));
#48816=CARTESIAN_POINT('Ctrl Pts',(-29.575,-3.85128343521349,-1.84853414389017));
#48817=CARTESIAN_POINT('Ctrl Pts',(-29.575,-3.86606513313638,-1.82343804723132));
#48818=CARTESIAN_POINT('Ctrl Pts',(-29.575,-3.87962032072916,-1.80042429740151));
#48819=CARTESIAN_POINT('Ctrl Pts',(-29.575,-3.8929775187076,-1.77727417891757));
#48820=CARTESIAN_POINT('Ctrl Pts',(-29.575,-3.90612065588015,-1.75401710046083));
#48821=CARTESIAN_POINT('Ctrl Pts',(-29.575,-3.97117453777595,-1.63890278526318));
#48822=CARTESIAN_POINT('Ctrl Pts',(-29.575,-4.03105238509688,-1.52106386401277));
#48823=CARTESIAN_POINT('Ctrl Pts',(-29.575,-4.08564840782879,-1.40094223444012));
#48824=CARTESIAN_POINT('Ctrl Pts',(-29.575,-4.14101887615531,-1.27911667732505));
#48825=CARTESIAN_POINT('Ctrl Pts',(-29.575,-4.19095714201348,-1.1549425736421));
#48826=CARTESIAN_POINT('Ctrl Pts',(-29.575,-4.23531866325731,-1.0288395166209));
#48827=CARTESIAN_POINT('Ctrl Pts',(-29.575,-4.27963521656908,-0.902864286453708));
#48828=CARTESIAN_POINT('Ctrl Pts',(-29.575,-4.31838678906507,-0.774963270506112));
#48829=CARTESIAN_POINT('Ctrl Pts',(-29.575,-4.35138804153719,-0.645524185385383));
#48830=CARTESIAN_POINT('Ctrl Pts',(-29.575,-4.37561871456528,-0.550485484921972));
#48831=CARTESIAN_POINT('Ctrl Pts',(-29.575,-4.39674856572066,-0.45461692513887));
#48832=CARTESIAN_POINT('Ctrl Pts',(-29.575,-4.41468782191536,-0.358064990641669));
#48833=CARTESIAN_POINT('Ctrl Pts',(-29.575,-4.42224607172046,-0.317385286189321));
#48834=CARTESIAN_POINT('Ctrl Pts',(-29.575,-4.42923776471172,-0.27658421805809));
#48835=CARTESIAN_POINT('Ctrl Pts',(-29.575,-4.43565536938885,-0.235672547990024));
#48836=CARTESIAN_POINT('Ctrl Pts',(-29.575,-4.43961660695444,-0.210420004011757));
#48837=CARTESIAN_POINT('Ctrl Pts',(-29.575,-4.44335980044231,-0.185119699039305));
#48838=CARTESIAN_POINT('Ctrl Pts',(-29.575,-4.44687885001345,-0.159806585076518));
#48839=CARTESIAN_POINT('Ctrl Pts',(-29.575,-4.46586121538066,-0.0232632462829367));
#48840=CARTESIAN_POINT('Ctrl Pts',(-29.575,-4.47835132040759,0.113799339019299));
#48841=CARTESIAN_POINT('Ctrl Pts',(-29.575,-4.48420367058679,0.25094774090325));
#48842=CARTESIAN_POINT('Ctrl Pts',(-29.575,-4.48802427633214,0.340482706542299));
#48843=CARTESIAN_POINT('Ctrl Pts',(-29.575,-4.4890151135886,0.430054946692756));
#48844=CARTESIAN_POINT('Ctrl Pts',(-29.575,-4.48712517877637,0.519549617577561));
#48845=CARTESIAN_POINT('Ctrl Pts',(-29.575,-4.48432359350001,0.652213956389896));
#48846=CARTESIAN_POINT('Ctrl Pts',(-29.575,-4.47519448741699,0.784707646574493));
#48847=CARTESIAN_POINT('Ctrl Pts',(-29.575,-4.45999947400341,0.916663774321655));
#48848=CARTESIAN_POINT('Ctrl Pts',(-29.575,-4.44456005012953,1.05074240482977));
#48849=CARTESIAN_POINT('Ctrl Pts',(-29.575,-4.42285792068252,1.1842667673282));
#48850=CARTESIAN_POINT('Ctrl Pts',(-29.575,-4.39511381888785,1.31685585528468));
#48851=CARTESIAN_POINT('Ctrl Pts',(-29.575,-4.38178896280792,1.38053535472801));
#48852=CARTESIAN_POINT('Ctrl Pts',(-29.575,-4.36706965006509,1.44399910643623));
#48853=CARTESIAN_POINT('Ctrl Pts',(-29.575,-4.35097613979996,1.50720443522242));
#48854=CARTESIAN_POINT('Ctrl Pts',(-29.575,-4.34482928679442,1.53134546218391));
#48855=CARTESIAN_POINT('Ctrl Pts',(-29.575,-4.33848058918165,1.55545340805442));
#48856=CARTESIAN_POINT('Ctrl Pts',(-29.575,-4.3319391871451,1.57949701586949));
#48857=CARTESIAN_POINT('Ctrl Pts',(-29.575,-4.29596876934752,1.71171005118469));
#48858=CARTESIAN_POINT('Ctrl Pts',(-29.575,-4.25413965605729,1.84212793058693));
#48859=CARTESIAN_POINT('Ctrl Pts',(-29.575,-4.20675605414909,1.97036806915586));
#48860=CARTESIAN_POINT('Ctrl Pts',(-29.575,-4.15824257123346,2.10166614530495));
#48861=CARTESIAN_POINT('Ctrl Pts',(-29.575,-4.10390647699439,2.23068214498256));
#48862=CARTESIAN_POINT('Ctrl Pts',(-29.575,-4.04401911667263,2.35700945357488));
#48863=CARTESIAN_POINT('Ctrl Pts',(-29.575,-3.98492825956341,2.48165660617797));
#48864=CARTESIAN_POINT('Ctrl Pts',(-29.575,-3.92043243319514,2.60368687307991));
#48865=CARTESIAN_POINT('Ctrl Pts',(-29.575,-3.85074314886284,2.72270204804338));
#48866=CARTESIAN_POINT('Ctrl Pts',(-29.575,-3.79985133012436,2.80961496111749));
#48867=CARTESIAN_POINT('Ctrl Pts',(-29.575,-3.74618885745191,2.89491983557514));
#48868=CARTESIAN_POINT('Ctrl Pts',(-29.575,-3.68984439893471,2.97851803505928));
#48869=CARTESIAN_POINT('Ctrl Pts',(-29.575,-3.66391228552828,3.01699347783834));
#48870=CARTESIAN_POINT('Ctrl Pts',(-29.575,-3.63741189415848,3.05510731852617));
#48871=CARTESIAN_POINT('Ctrl Pts',(-29.575,-3.61035102303907,3.09284943609328));
#48872=CARTESIAN_POINT('Ctrl Pts',(-29.575,-3.59584650743156,3.11307905586041));
#48873=CARTESIAN_POINT('Ctrl Pts',(-29.575,-3.58118096187307,3.13320187682416));
#48874=CARTESIAN_POINT('Ctrl Pts',(-29.575,-3.56635552732019,3.15321629747535));
#48875=CARTESIAN_POINT('Ctrl Pts',(-29.575,-3.5546900145129,3.16896480586503));
#48876=CARTESIAN_POINT('Ctrl Pts',(-29.575,-3.54292488679082,3.18464691960963));
#48877=CARTESIAN_POINT('Ctrl Pts',(-29.575,-3.53107100158975,3.20024854439494));
#48878=CARTESIAN_POINT('Ctrl Pts',(-29.575,-3.444915061959,3.31364365665938));
#48879=CARTESIAN_POINT('Ctrl Pts',(-29.575,-3.353952606715,3.42295435898676));
#48880=CARTESIAN_POINT('Ctrl Pts',(-29.575,-3.25851212336527,3.52794677560707));
#48881=CARTESIAN_POINT('Ctrl Pts',(-29.575,-3.1617890061929,3.63435019539871));
#48882=CARTESIAN_POINT('Ctrl Pts',(-29.575,-3.06046638882771,3.73631912635592));
#48883=CARTESIAN_POINT('Ctrl Pts',(-29.575,-2.95483635071748,3.83359158033952));
#48884=CARTESIAN_POINT('Ctrl Pts',(-29.575,-2.84930340889874,3.93077462041477));
#48885=CARTESIAN_POINT('Ctrl Pts',(-29.575,-2.73947053698142,4.02327043490703));
#48886=CARTESIAN_POINT('Ctrl Pts',(-29.575,-2.62558525501093,4.11078989098106));
#48887=CARTESIAN_POINT('Ctrl Pts',(-29.575,-2.51319651570498,4.19715927219268));
#48888=CARTESIAN_POINT('Ctrl Pts',(-29.575,-2.39686069001292,4.27868275896332));
#48889=CARTESIAN_POINT('Ctrl Pts',(-29.575,-2.27677987968084,4.3550468235479));
#48890=CARTESIAN_POINT('Ctrl Pts',(-29.575,-2.24098328939054,4.37781126963447));
#48891=CARTESIAN_POINT('Ctrl Pts',(-29.575,-2.20485367910692,4.40011694506889));
#48892=CARTESIAN_POINT('Ctrl Pts',(-29.575,-2.16839587231048,4.42195480991686));
#48893=CARTESIAN_POINT('Ctrl Pts',(-29.575,-2.36826780557337,-3.31775809990772));
#48894=CARTESIAN_POINT('Ctrl Pts',(-29.5008109365549,-1.33928601121754,
-4.04293436335451));
#48895=CARTESIAN_POINT('Ctrl Pts',(-29.3470759847368,1.55637121596689,-4.50701225231274));
#48896=CARTESIAN_POINT('Ctrl Pts',(-29.1137951445456,4.65387018191312,-1.22765401651987));
#48897=CARTESIAN_POINT('Ctrl Pts',(-28.8751574794264,3.55090078994383,3.25125842872222));
#48898=CARTESIAN_POINT('Ctrl Pts',(-28.6365198143072,-0.816478135197904,
4.74503193420896));
#48899=CARTESIAN_POINT('Ctrl Pts',(-28.4455297648071,-3.71062116286106,
2.45079400531014));
#48900=CARTESIAN_POINT('Ctrl Pts',(-28.3340856036801,-4.06733760858173,
0.547694664417248));
#48901=CARTESIAN_POINT('Ctrl Pts',(-28.3021873309261,-4.06480101368718,
0.00206955444756761));
#48902=CARTESIAN_POINT('Origin',(-29.575,-4.52129938221115E-16,0.));
#48903=CARTESIAN_POINT('',(-29.575,-4.925,-6.03138548580071E-16));
#48904=CARTESIAN_POINT('Origin',(-29.575,0.,0.));
#48905=CARTESIAN_POINT('Origin',(-29.575,0.,0.));
#48906=CARTESIAN_POINT('',(-29.575,2.36230756092324,-3.31488661006752));
#48907=CARTESIAN_POINT('Ctrl Pts',(-29.575,2.17494790042119,4.42655504786424));
#48908=CARTESIAN_POINT('Ctrl Pts',(-29.575,2.26967152441801,4.37041752782518));
#48909=CARTESIAN_POINT('Ctrl Pts',(-29.575,2.36222031470781,4.31097507135364));
#48910=CARTESIAN_POINT('Ctrl Pts',(-29.575,2.45239463893034,4.24821920794634));
#48911=CARTESIAN_POINT('Ctrl Pts',(-29.575,2.57031754301399,4.16615201503894));
#48912=CARTESIAN_POINT('Ctrl Pts',(-29.575,2.68418134028915,4.07841926504524));
#48913=CARTESIAN_POINT('Ctrl Pts',(-29.575,2.793800816624,3.98544075385194));
#48914=CARTESIAN_POINT('Ctrl Pts',(-29.575,2.86142888819741,3.928079073063));
#48915=CARTESIAN_POINT('Ctrl Pts',(-29.575,2.92744077307288,3.8687200679563));
#48916=CARTESIAN_POINT('Ctrl Pts',(-29.575,2.99178498903163,3.80745669486626));
#48917=CARTESIAN_POINT('Ctrl Pts',(-29.575,3.03740293232873,3.76402296833516));
#48918=CARTESIAN_POINT('Ctrl Pts',(-29.575,3.08218251964483,3.71963195357705));
#48919=CARTESIAN_POINT('Ctrl Pts',(-29.575,3.12610340234575,3.67431582845979));
#48920=CARTESIAN_POINT('Ctrl Pts',(-29.575,3.14170642099533,3.65821714596868));
#48921=CARTESIAN_POINT('Ctrl Pts',(-29.575,3.15720284290207,3.64199979656664));
#48922=CARTESIAN_POINT('Ctrl Pts',(-29.575,3.17258572052557,3.62567157287578));
#48923=CARTESIAN_POINT('Ctrl Pts',(-29.575,3.27034309847291,3.52190657040855));
#48924=CARTESIAN_POINT('Ctrl Pts',(-29.575,3.36340172212969,3.41379269192058));
#48925=CARTESIAN_POINT('Ctrl Pts',(-29.575,3.45158356813246,3.30174290977256));
#48926=CARTESIAN_POINT('Ctrl Pts',(-29.575,3.53724490642985,3.19289585417305));
#48927=CARTESIAN_POINT('Ctrl Pts',(-29.575,3.61830434560196,3.08033384565738));
#48928=CARTESIAN_POINT('Ctrl Pts',(-29.575,3.69455768842054,2.96441414844495));
#48929=CARTESIAN_POINT('Ctrl Pts',(-29.575,3.76127936338681,2.86298441338408));
#48930=CARTESIAN_POINT('Ctrl Pts',(-29.575,3.82432087679273,2.75898335344391));
#48931=CARTESIAN_POINT('Ctrl Pts',(-29.575,3.88351761773973,2.65264344251299));
#48932=CARTESIAN_POINT('Ctrl Pts',(-29.575,3.89539020296671,2.63131575393826));
#48933=CARTESIAN_POINT('Ctrl Pts',(-29.575,3.90710917047629,2.60989171569305));
#48934=CARTESIAN_POINT('Ctrl Pts',(-29.575,3.91866219954629,2.58839389445723));
#48935=CARTESIAN_POINT('Ctrl Pts',(-29.575,3.98533187012549,2.46433529032153));
#48936=CARTESIAN_POINT('Ctrl Pts',(-29.575,4.04656060379988,2.33767837925172));
#48937=CARTESIAN_POINT('Ctrl Pts',(-29.575,4.10217235556336,2.20881042226382));
#48938=CARTESIAN_POINT('Ctrl Pts',(-29.575,4.15749625211679,2.08060950617376));
#48939=CARTESIAN_POINT('Ctrl Pts',(-29.575,4.20726139736363,1.95021957273537));
#48940=CARTESIAN_POINT('Ctrl Pts',(-29.575,4.25124518841383,1.81800776290176));
#48941=CARTESIAN_POINT('Ctrl Pts',(-29.575,4.29413119192342,1.68909581590603));
#48942=CARTESIAN_POINT('Ctrl Pts',(-29.575,4.33152087503006,1.55845109390724));
#48943=CARTESIAN_POINT('Ctrl Pts',(-29.575,4.36315916984956,1.42641155759016));
#48944=CARTESIAN_POINT('Ctrl Pts',(-29.575,4.38688789096419,1.32738190535235));
#48945=CARTESIAN_POINT('Ctrl Pts',(-29.575,4.40738049178401,1.22756756386048));
#48946=CARTESIAN_POINT('Ctrl Pts',(-29.575,4.42451035861733,1.12711368795651));
#48947=CARTESIAN_POINT('Ctrl Pts',(-29.575,4.43133674032546,1.08708205737504));
#48948=CARTESIAN_POINT('Ctrl Pts',(-29.575,4.4376289049131,1.04694890359475));
#48949=CARTESIAN_POINT('Ctrl Pts',(-29.575,4.44337808320161,1.00672360633312));
#48950=CARTESIAN_POINT('Ctrl Pts',(-29.575,4.44682246179442,0.982624309733816));
#48951=CARTESIAN_POINT('Ctrl Pts',(-29.575,4.45007193773189,0.958491942467769));
#48952=CARTESIAN_POINT('Ctrl Pts',(-29.575,4.45312454919313,0.934328545878378));
#48953=CARTESIAN_POINT('Ctrl Pts',(-29.575,4.45558677843594,0.914838406879834));
#48954=CARTESIAN_POINT('Ctrl Pts',(-29.575,4.45791999829306,0.895335151707175));
#48955=CARTESIAN_POINT('Ctrl Pts',(-29.575,4.46012266207708,0.87582765091181));
#48956=CARTESIAN_POINT('Ctrl Pts',(-29.575,4.47511104469547,0.743085700928035));
#48957=CARTESIAN_POINT('Ctrl Pts',(-29.575,4.48407271847718,0.610034498076699));
#48958=CARTESIAN_POINT('Ctrl Pts',(-29.575,4.48680554393477,0.476999857930275));
#48959=CARTESIAN_POINT('Ctrl Pts',(-29.575,4.48859856927288,0.389714927249725));
#48960=CARTESIAN_POINT('Ctrl Pts',(-29.575,4.48770920842808,0.302437045899035));
#48961=CARTESIAN_POINT('Ctrl Pts',(-29.575,4.48406815367479,0.215259203818982));
#48962=CARTESIAN_POINT('Ctrl Pts',(-29.575,4.47844824112982,0.0807015326092455));
#48963=CARTESIAN_POINT('Ctrl Pts',(-29.575,4.46627498023888,-0.0536189903864601));
#48964=CARTESIAN_POINT('Ctrl Pts',(-29.575,4.44773981895834,-0.187263918132325));
#48965=CARTESIAN_POINT('Ctrl Pts',(-29.575,4.42923611011045,-0.320682062953368));
#48966=CARTESIAN_POINT('Ctrl Pts',(-29.575,4.40439160268717,-0.453427703408474));
#48967=CARTESIAN_POINT('Ctrl Pts',(-29.575,4.37335182340664,-0.58503925570624));
#48968=CARTESIAN_POINT('Ctrl Pts',(-29.575,4.35843537009352,-0.648286405680295));
#48969=CARTESIAN_POINT('Ctrl Pts',(-29.575,4.34208757622849,-0.711271201901602));
#48970=CARTESIAN_POINT('Ctrl Pts',(-29.575,4.32432137404194,-0.773939500968908));
#48971=CARTESIAN_POINT('Ctrl Pts',(-29.575,4.31955371135246,-0.790756899990894));
#48972=CARTESIAN_POINT('Ctrl Pts',(-29.575,4.31468432223976,-0.807549803851364));
#48973=CARTESIAN_POINT('Ctrl Pts',(-29.575,4.30971696019155,-0.824305954558689));
#48974=CARTESIAN_POINT('Ctrl Pts',(-29.575,4.27217870230904,-0.950931857858156));
#48975=CARTESIAN_POINT('Ctrl Pts',(-29.575,4.22899927473913,-1.07563909243635));
#48976=CARTESIAN_POINT('Ctrl Pts',(-29.575,4.18039187949891,-1.19802776435577));
#48977=CARTESIAN_POINT('Ctrl Pts',(-29.575,4.13198650007613,-1.3199077801853));
#48978=CARTESIAN_POINT('Ctrl Pts',(-29.575,4.07819767353095,-1.43948920797592));
#48979=CARTESIAN_POINT('Ctrl Pts',(-29.575,4.01919161106764,-1.55635171305596));
#48980=CARTESIAN_POINT('Ctrl Pts',(-29.575,3.96554454554038,-1.66260063403094));
#48981=CARTESIAN_POINT('Ctrl Pts',(-29.575,3.90758410693226,-1.7666021746683));
#48982=CARTESIAN_POINT('Ctrl Pts',(-29.575,3.84540829196954,-1.86801442537029));
#48983=CARTESIAN_POINT('Ctrl Pts',(-29.575,3.79972079463418,-1.9425333027907));
#48984=CARTESIAN_POINT('Ctrl Pts',(-29.575,3.7517566228007,-2.01565352617642));
#48985=CARTESIAN_POINT('Ctrl Pts',(-29.575,3.70157235710967,-2.08727533440549));
#48986=CARTESIAN_POINT('Ctrl Pts',(-29.575,3.67384420437395,-2.12684830434812));
#48987=CARTESIAN_POINT('Ctrl Pts',(-29.575,3.64543819285622,-2.16596367436737));
#48988=CARTESIAN_POINT('Ctrl Pts',(-29.575,3.61636323740365,-2.20460339725076));
#48989=CARTESIAN_POINT('Ctrl Pts',(-29.575,3.60131842230507,-2.22459749447954));
#48990=CARTESIAN_POINT('Ctrl Pts',(-29.575,3.58609448820911,-2.24446422067884));
#48991=CARTESIAN_POINT('Ctrl Pts',(-29.575,3.57069262976354,-2.26420097811176));
#48992=CARTESIAN_POINT('Ctrl Pts',(-29.575,3.55903139036739,-2.27914430810939));
#48993=CARTESIAN_POINT('Ctrl Pts',(-29.575,3.54727273939743,-2.29400720550239));
#48994=CARTESIAN_POINT('Ctrl Pts',(-29.575,3.53542205698418,-2.30878307744774));
#48995=CARTESIAN_POINT('Ctrl Pts',(-29.575,3.45405476451608,-2.41023484639433));
#48996=CARTESIAN_POINT('Ctrl Pts',(-29.575,3.36828498238971,-2.50767334973966));
#48997=CARTESIAN_POINT('Ctrl Pts',(-29.575,3.27835860536771,-2.60083261446428));
#48998=CARTESIAN_POINT('Ctrl Pts',(-29.575,3.19030403000318,-2.69205278554481));
#48999=CARTESIAN_POINT('Ctrl Pts',(-29.575,3.09826340014138,-2.77917034507256));
#49000=CARTESIAN_POINT('Ctrl Pts',(-29.575,3.00243676957963,-2.86189425854725));
#49001=CARTESIAN_POINT('Ctrl Pts',(-29.575,2.90355461728311,-2.94725590136843));
#49002=CARTESIAN_POINT('Ctrl Pts',(-29.575,2.80064068610558,-3.02794003035809));
#49003=CARTESIAN_POINT('Ctrl Pts',(-29.575,2.69389027200841,-3.10357332294541));
#49004=CARTESIAN_POINT('Ctrl Pts',(-29.575,2.59371175266095,-3.17455038967486));
#49005=CARTESIAN_POINT('Ctrl Pts',(-29.575,2.49015393838355,-3.24107925145737));
#49006=CARTESIAN_POINT('Ctrl Pts',(-29.575,2.38336574054609,-3.30280154424992));
#49007=CARTESIAN_POINT('Ctrl Pts',(-29.575,2.37636023875519,-3.30685063995014));
#49008=CARTESIAN_POINT('Ctrl Pts',(-29.575,2.36934083188486,-3.31087903158254));
#49009=CARTESIAN_POINT('Ctrl Pts',(-29.575,2.36230756092332,-3.31488661006746));
#49010=CARTESIAN_POINT('Origin',(-29.575,0.,0.));
#49011=CARTESIAN_POINT('Origin',(-32.3478126690739,0.,0.));
#49012=CARTESIAN_POINT('Ctrl Pts',(-29.575,2.36230756092324,-3.31488661006752));
#49013=CARTESIAN_POINT('Ctrl Pts',(-29.5352270558135,2.91456939066647,-2.92132494432319));
#49014=CARTESIAN_POINT('Ctrl Pts',(-29.4556811674404,3.80947864266608,-1.85446537575054));
#49015=CARTESIAN_POINT('Ctrl Pts',(-29.2965893906943,4.40029930288375,0.892938679230673));
#49016=CARTESIAN_POINT('Ctrl Pts',(-29.0977246697615,2.41062119233501,4.16711865021482));
#49017=CARTESIAN_POINT('Ctrl Pts',(-28.8590870046423,-2.21020820766824,
4.28001845847083));
#49018=CARTESIAN_POINT('Ctrl Pts',(-28.6924496710798,-4.01269863755865,
1.60905902128973));
#49019=CARTESIAN_POINT('Ctrl Pts',(-28.6053582258903,-4.07619291884947,
0.130177206130288));
#49020=CARTESIAN_POINT('Ctrl Pts',(-28.5978126690739,-4.07533558288693,
0.00197868943318465));
#49021=CARTESIAN_POINT('Ctrl Pts',(-30.0683458050225,2.85821514250009,-4.01076441581692));
#49022=CARTESIAN_POINT('Ctrl Pts',(-30.028572860836,3.52641057585851,-3.5345842895939));
#49023=CARTESIAN_POINT('Ctrl Pts',(-29.9490269724629,4.60918371579173,-2.24376415073622));
#49024=CARTESIAN_POINT('Ctrl Pts',(-29.7899351957168,5.32403244483542,1.08038889453645));
#49025=CARTESIAN_POINT('Ctrl Pts',(-29.5910704747841,2.91667101639856,5.0419013271853));
#49026=CARTESIAN_POINT('Ctrl Pts',(-29.3524328096649,-2.6741863217702,5.17850163566369));
#49027=CARTESIAN_POINT('Ctrl Pts',(-29.1137951445457,-5.7973743179944,0.550511209599409));
#49028=CARTESIAN_POINT('Ctrl Pts',(-28.8751574794264,-3.59989778886694,
-4.57971187869854));
#49029=CARTESIAN_POINT('Ctrl Pts',(-28.6365198143073,1.9077811732274,-5.50426057988267));
#49030=CARTESIAN_POINT('Ctrl Pts',(-28.3978821491879,5.66123134949523,-1.37093968550409));
#49031=CARTESIAN_POINT('Ctrl Pts',(-28.1592444840688,4.21433244584917,4.02140449350459));
#49032=CARTESIAN_POINT('Ctrl Pts',(-27.9206068189495,-1.10479606405923,
5.71943238413845));
#49033=CARTESIAN_POINT('Ctrl Pts',(-27.6819691538303,-5.40870633854705,
2.16272545229035));
#49034=CARTESIAN_POINT('Ctrl Pts',(-27.4433314887111,-4.74359941984978,
-3.380866692594));
#49035=CARTESIAN_POINT('Ctrl Pts',(-27.2046938235918,0.279640350988314,
-5.8184000833979));
#49036=CARTESIAN_POINT('Ctrl Pts',(-26.9660561584726,5.04593690996907,-2.91039003941573));
#49037=CARTESIAN_POINT('Ctrl Pts',(-26.7274184933533,5.17640786355619,2.67146555315453));
#49038=CARTESIAN_POINT('Ctrl Pts',(-26.4887808282342,0.551162248122564,
5.79897734693768));
#49039=CARTESIAN_POINT('Ctrl Pts',(-26.2501431631149,-4.58044707277724,
3.59880626920218));
#49040=CARTESIAN_POINT('Ctrl Pts',(-26.0115054979957,-5.50387573699426,
-1.90768582721621));
#49041=CARTESIAN_POINT('Ctrl Pts',(-25.7728678328765,-1.37074105079164,
-5.66153515210527));
#49042=CARTESIAN_POINT('Ctrl Pts',(-25.5342301677573,4.02173058771444,-4.21397584735458));
#49043=CARTESIAN_POINT('Ctrl Pts',(-25.295592502638,5.71932789822544,1.10507891249598));
#49044=CARTESIAN_POINT('Ctrl Pts',(-25.0569548375188,2.16242101025971,5.40886734761332));
#49045=CARTESIAN_POINT('Ctrl Pts',(-24.8183171723995,-3.38116152304108,
4.74338034983671));
#49046=CARTESIAN_POINT('Ctrl Pts',(-24.5796795072803,-5.81837790032782,
-0.27998076825629));
#49047=CARTESIAN_POINT('Ctrl Pts',(-24.3410418421611,-2.91009025392015,
-5.04611585917912));
#49048=CARTESIAN_POINT('Ctrl Pts',(-24.1024041770419,2.67177743350171,-5.17624534512243));
#49049=CARTESIAN_POINT('Ctrl Pts',(-23.8637665119226,5.79900962484977,-0.550815695476877));
#49050=CARTESIAN_POINT('Ctrl Pts',(-23.6251288468035,3.59853198023136,4.58066350376895));
#49051=CARTESIAN_POINT('Ctrl Pts',(-23.3864911816842,-1.90801608760284,
5.50376100088902));
#49052=CARTESIAN_POINT('Ctrl Pts',(-23.147853516565,-5.66161723459444,1.37040170709392));
#49053=CARTESIAN_POINT('Ctrl Pts',(-22.9092158514458,-4.21373472077718,
-4.02198337277209));
#49054=CARTESIAN_POINT('Ctrl Pts',(-22.6705781863265,1.10542191660648,-5.71926157245085));
#49055=CARTESIAN_POINT('Ctrl Pts',(-22.4319405212073,5.40899699874395,-2.16209667128711));
#49056=CARTESIAN_POINT('Ctrl Pts',(-22.1933028560881,4.74317758767807,3.38144598062146));
#49057=CARTESIAN_POINT('Ctrl Pts',(-21.9546651909688,-0.280329688527433,
5.81836109345686));
#49058=CARTESIAN_POINT('Ctrl Pts',(-21.7160275258496,-5.04629036031444,
2.90978764647796));
#49059=CARTESIAN_POINT('Ctrl Pts',(-21.4773898607304,-5.17608511572218,
-2.67208783967747));
#49060=CARTESIAN_POINT('Ctrl Pts',(-21.2387521956112,-0.55046793874511,
-5.79904264483125));
#49061=CARTESIAN_POINT('Ctrl Pts',(-21.0001145304919,4.58087929208444,-3.59825728089574));
#49062=CARTESIAN_POINT('Ctrl Pts',(-20.7614768653727,5.50364657119464,1.90834613410097));
#49063=CARTESIAN_POINT('Ctrl Pts',(-20.5228392002535,1.37006218854147,5.66169940456846));
#49064=CARTESIAN_POINT('Ctrl Pts',(-20.2842015351343,-4.02223605484748,
4.21349352286768));
#49065=CARTESIAN_POINT('Ctrl Pts',(-20.045563870015,-5.71919527222015,-1.10576488747686));
#49066=CARTESIAN_POINT('Ctrl Pts',(-19.8069262048958,-2.16177230051888,
-5.40912664566764));
#49067=CARTESIAN_POINT('Ctrl Pts',(-19.5682885397766,3.38173041352887,-4.74297480052089));
#49068=CARTESIAN_POINT('Ctrl Pts',(-19.3296508746573,5.81834427218029,0.28067860365368));
#49069=CARTESIAN_POINT('Ctrl Pts',(-19.0910132095381,2.90948502517622,5.04646484545742));
#49070=CARTESIAN_POINT('Ctrl Pts',(-18.8523755444189,-2.67239823447518,
5.17592486658531));
#49071=CARTESIAN_POINT('Ctrl Pts',(-18.6137378792997,-5.79907564487983,
0.550120180618539));
#49072=CARTESIAN_POINT('Ctrl Pts',(-18.3751002141804,-3.59798256814023,
-4.58109506423096));
#49073=CARTESIAN_POINT('Ctrl Pts',(-18.1364625490612,1.90867617348636,-5.50353212154956));
#49074=CARTESIAN_POINT('Ctrl Pts',(-17.897824883942,5.66178155431231,-1.3697226651447));
#49075=CARTESIAN_POINT('Ctrl Pts',(-17.6591872188228,4.2132523097379,4.02248872250135));
#49076=CARTESIAN_POINT('Ctrl Pts',(-17.4205495537035,-1.10610785433544,
5.71912895139983));
#49077=CARTESIAN_POINT('Ctrl Pts',(-17.1819118885843,-5.40925627315763,
2.16144792198822));
#49078=CARTESIAN_POINT('Ctrl Pts',(-16.9432742234651,-4.74277199629759,
-3.38201483428115));
#49079=CARTESIAN_POINT('Ctrl Pts',(-16.7046365583458,0.281027517765593,
-5.81832742997681));
#49080=CARTESIAN_POINT('Ctrl Pts',(-16.4659988932266,5.04663931245511,-2.90918239341314));
#49081=CARTESIAN_POINT('Ctrl Pts',(-16.2273612281074,5.17576459883361,2.67270861966342));
#49082=CARTESIAN_POINT('Ctrl Pts',(-15.9887235629882,0.549772420514306,
5.79910862407352));
#49083=CARTESIAN_POINT('Ctrl Pts',(-15.750085897869,-4.5813108199035,3.597707842446));
#49084=CARTESIAN_POINT('Ctrl Pts',(-15.5114482327497,-5.50341765211267,
-1.90900620600798));
#49085=CARTESIAN_POINT('Ctrl Pts',(-15.2728105676305,-1.36938313682227,
-5.66186368369541));
#49086=CARTESIAN_POINT('Ctrl Pts',(-15.0341729025113,4.02274137568974,-4.21301108145661));
#49087=CARTESIAN_POINT('Ctrl Pts',(-14.7955352373921,5.71906261001256,1.10645081721627));
#49088=CARTESIAN_POINT('Ctrl Pts',(-14.5568975722728,2.16112353568466,5.40938588119503));
#49089=CARTESIAN_POINT('Ctrl Pts',(-14.3182599071536,-3.38229924287111,
4.74256917501852));
#49090=CARTESIAN_POINT('Ctrl Pts',(-14.0796222420344,-5.81831056684969,
-0.281376430866862));
#49091=CARTESIAN_POINT('Ctrl Pts',(-13.8409845769151,-2.90887975118817,
-5.04681376130423));
#49092=CARTESIAN_POINT('Ctrl Pts',(-13.6023469117959,2.67301899524012,-5.17560431246901));
#49093=CARTESIAN_POINT('Ctrl Pts',(-13.3637092466767,5.79914158241269,-0.549424658433007));
#49094=CARTESIAN_POINT('Ctrl Pts',(-13.1250715815575,3.5974331038138,4.5815265591009));
#49095=CARTESIAN_POINT('Ctrl Pts',(-12.8864339164382,-1.90933623166449,
5.50330316288458));
#49096=CARTESIAN_POINT('Ctrl Pts',(-12.647796251319,-5.66194579271754,1.3690436035753));
#49097=CARTESIAN_POINT('Ctrl Pts',(-12.4091585861998,-4.21276983802462,
-4.0229940144117));
#49098=CARTESIAN_POINT('Ctrl Pts',(-12.1705209210806,1.10679377611814,-5.7189962480586));
#49099=CARTESIAN_POINT('Ctrl Pts',(-11.9318832559613,5.4095154697794,-2.16079914160935));
#49100=CARTESIAN_POINT('Ctrl Pts',(-11.6932455908421,4.74236633668439,3.38258363929778));
#49101=CARTESIAN_POINT('Ctrl Pts',(-11.4546079257229,-0.281725342956251,
5.81829368279896));
#49102=CARTESIAN_POINT('Ctrl Pts',(-11.2159702606036,-5.04698819200419,
2.9085770985024));
#49103=CARTESIAN_POINT('Ctrl Pts',(-10.9773325954844,-5.17544400749208,
-2.67332936120422));
#49104=CARTESIAN_POINT('Ctrl Pts',(-10.7386949303652,-0.549076894375944,
-5.79917451989717));
#49105=CARTESIAN_POINT('Ctrl Pts',(-10.5000572652459,4.58174228182235,-3.5971583522447));
#49106=CARTESIAN_POINT('Ctrl Pts',(-10.2614196001268,5.50318865386573,1.9096662504547));
#49107=CARTESIAN_POINT('Ctrl Pts',(-10.0227819350075,1.36870406540507,5.66202788137834));
#49108=CARTESIAN_POINT('Ctrl Pts',(-9.78414426988828,-4.02324663866633,
4.21252857944289));
#49109=CARTESIAN_POINT('Ctrl Pts',(-9.54550660476906,-5.71892986553813,
-1.10713673103989));
#49110=CARTESIAN_POINT('Ctrl Pts',(-9.30686893964983,-2.16047473976357,
-5.40964503891006));
#49111=CARTESIAN_POINT('Ctrl Pts',(-9.0682312745306,3.38286802356034,-4.74216348129631));
#49112=CARTESIAN_POINT('Ctrl Pts',(-8.82959360941138,5.81827677782428,0.282074254033242));
#49113=CARTESIAN_POINT('Ctrl Pts',(-8.59095594429215,2.90827443535771,5.04716260455295));
#49114=CARTESIAN_POINT('Ctrl Pts',(-8.35231827917293,-2.67363971755611,
5.1752836839061));
#49115=CARTESIAN_POINT('Ctrl Pts',(-8.1136806140537,-5.79920743652394,0.548729128339138));
#49116=CARTESIAN_POINT('Ctrl Pts',(-7.87504294893448,-3.59688358774524,
-4.58195798805725));
#49117=CARTESIAN_POINT('Ctrl Pts',(-7.63640528381524,1.90999626238828,-5.50307412507543));
#49118=CARTESIAN_POINT('Ctrl Pts',(-7.39776761869603,5.66210994965676,-1.36836452227643));
#49119=CARTESIAN_POINT('Ctrl Pts',(-7.15912995357678,4.21228730575213,4.0234992483829));
#49120=CARTESIAN_POINT('Ctrl Pts',(-6.92049228845757,-1.10747968205672,
5.7188634625854));
#49121=CARTESIAN_POINT('Ctrl Pts',(-6.68185462333833,-5.40977458843978,
2.16015032989127));
#49122=CARTESIAN_POINT('Ctrl Pts',(-6.44321695821912,-4.74196060913677,
-3.38315239516401));
#49123=CARTESIAN_POINT('Ctrl Pts',(-6.20457929309988,0.282423164637435,
-5.81825985287354));
#49124=CARTESIAN_POINT('Ctrl Pts',(-5.96594162798066,5.04733699791161,-2.90797175993565));
#49125=CARTESIAN_POINT('Ctrl Pts',(-5.72730396286144,5.17512334370478,2.6739500608018));
#49126=CARTESIAN_POINT('Ctrl Pts',(-5.4886662977422,0.548381356497653,5.79924033899806));
#49127=CARTESIAN_POINT('Ctrl Pts',(-5.25002863262299,-4.58217367045971,
3.59660879744466));
#49128=CARTESIAN_POINT('Ctrl Pts',(-5.01139096750376,-5.5029595906143,-1.91032624275442));
#49129=CARTESIAN_POINT('Ctrl Pts',(-4.77275330238452,-1.3680249471228,-5.66219204498688));
#49130=CARTESIAN_POINT('Ctrl Pts',(-4.53411563726531,4.02375179159935,-4.21204592589478));
#49131=CARTESIAN_POINT('Ctrl Pts',(-4.29547797214607,5.71879713894916,1.10782245436525));
#49132=CARTESIAN_POINT('Ctrl Pts',(-4.05684030702685,2.1598257205091,5.40990445393106));
#49133=CARTESIAN_POINT('Ctrl Pts',(-3.81820264190762,-3.38343638652024,
4.74175707603558));
#49134=CARTESIAN_POINT('Ctrl Pts',(-3.57956497678839,-5.8182436135944,-0.282770838170588));
#49135=CARTESIAN_POINT('Ctrl Pts',(-3.34092731166917,-2.90766771762518,
-5.04751374594047));
#49136=CARTESIAN_POINT('Ctrl Pts',(-3.10228964654994,2.67425779052882,-5.17495842985376));
#49137=CARTESIAN_POINT('Ctrl Pts',(-2.86365198143071,5.79927821925697,-0.54804232686631));
#49138=CARTESIAN_POINT('Ctrl Pts',(-2.62501431631149,3.59632439845965,4.58240612234822));
#49139=CARTESIAN_POINT('Ctrl Pts',(-2.38637665119227,-1.91063779555211,
5.5028128128105));
#49140=CARTESIAN_POINT('Ctrl Pts',(-2.14773898607303,-5.66230948168428,
1.36774722574033));
#49141=CARTESIAN_POINT('Ctrl Pts',(-1.90910132095381,-4.21173664772448,
-4.02412306903384));
#49142=CARTESIAN_POINT('Ctrl Pts',(-1.67046365583459,1.10803490710056,-5.71850283364837));
#49143=CARTESIAN_POINT('Ctrl Pts',(-1.43182599071535,5.41028448303652,-2.15993873727599));
#49144=CARTESIAN_POINT('Ctrl Pts',(-1.19318832559614,4.74107307396736,3.3845606937213));
#49145=CARTESIAN_POINT('Ctrl Pts',(-0.954550660476906,-0.282194523950606,
5.81661222925236));
#49146=CARTESIAN_POINT('Ctrl Pts',(-0.715912995357673,-5.049479635978,2.91048227618002));
#49147=CARTESIAN_POINT('Ctrl Pts',(-0.477275330238451,-5.17121721536142,
-2.68071843402506));
#49148=CARTESIAN_POINT('Ctrl Pts',(-0.278410609305759,-1.32510607804596,
-5.26845855246328));
#49149=CARTESIAN_POINT('Ctrl Pts',(-0.119318832559609,2.02851289583626,
-4.70788567421457));
#49150=CARTESIAN_POINT('Ctrl Pts',(-0.0397729441865337,3.3679595299544,
-3.68587930545211));
#49151=CARTESIAN_POINT('Ctrl Pts',(4.44089209850063E-15,3.87448963569911,
-3.0403873211912));
#49152=CARTESIAN_POINT('Ctrl Pts',(-29.9038972033484,2.6929126153078,-3.77880514723378));
#49153=CARTESIAN_POINT('Ctrl Pts',(-29.8641242591618,3.32246351412783,-3.330164507837));
#49154=CARTESIAN_POINT('Ctrl Pts',(-29.7845783707887,4.34261535808318,-2.11399789240766));
#49155=CARTESIAN_POINT('Ctrl Pts',(-29.6254865940426,5.0161213975182,1.01790548943452));
#49156=CARTESIAN_POINT('Ctrl Pts',(-29.4266218731099,2.74798774171071,4.75030710152848));
#49157=CARTESIAN_POINT('Ctrl Pts',(-29.1879842079907,-2.51952695040288,
4.87900724326607));
#49158=CARTESIAN_POINT('Ctrl Pts',(-28.9493465428715,-5.46208793188772,
0.518672845565351));
#49159=CARTESIAN_POINT('Ctrl Pts',(-28.7107088777522,-3.39170065447864,
-4.31484800050243));
#49160=CARTESIAN_POINT('Ctrl Pts',(-28.472071212633,1.79744621468105,-5.18592618627794));
#49161=CARTESIAN_POINT('Ctrl Pts',(-28.2334335475138,5.33381868024693,-1.29165251384495));
#49162=CARTESIAN_POINT('Ctrl Pts',(-27.9947958823946,3.97059998730579,3.78882986476014));
#49163=CARTESIAN_POINT('Ctrl Pts',(-27.7561582172753,-1.04090109033753,
5.38865370581382));
#49164=CARTESIAN_POINT('Ctrl Pts',(-27.5175205521561,-5.09589824607407,
2.03764600058257));
#49165=CARTESIAN_POINT('Ctrl Pts',(-27.2788828870369,-4.4692572402043,-3.18533704191237));
#49166=CARTESIAN_POINT('Ctrl Pts',(-27.0402452219176,0.26346758077383,-5.48189768940374));
#49167=CARTESIAN_POINT('Ctrl Pts',(-26.8016075567985,4.75410928969372,-2.74207001987724));
#49168=CARTESIAN_POINT('Ctrl Pts',(-26.5629698916792,4.87703456275017,2.51696353520732));
#49169=CARTESIAN_POINT('Ctrl Pts',(-26.32433222656,0.519286231809787,5.46359825096759));
#49170=CARTESIAN_POINT('Ctrl Pts',(-26.0856945614407,-4.31554067523491,
3.39067226195794));
#49171=CARTESIAN_POINT('Ctrl Pts',(-25.8470568963215,-5.18556360046217,
-1.79735638292817));
#49172=CARTESIAN_POINT('Ctrl Pts',(-25.6084192312023,-1.29146536700809,
-5.33410491268233));
#49173=CARTESIAN_POINT('Ctrl Pts',(-25.3697815660831,3.78913709957896,-3.97026401239249));
#49174=CARTESIAN_POINT('Ctrl Pts',(-25.1311439009638,5.38855526275784,1.04116758046706));
#49175=CARTESIAN_POINT('Ctrl Pts',(-24.8925062358446,2.03735916570693,5.09604994331312));
#49176=CARTESIAN_POINT('Ctrl Pts',(-24.6538685707254,-3.18561482108248,
4.46905083992566));
#49177=CARTESIAN_POINT('Ctrl Pts',(-24.4152309056062,-5.48187678927333,
-0.263788310288471));
#49178=CARTESIAN_POINT('Ctrl Pts',(-24.1765932404869,-2.74178757222978,
-4.75427788952306));
#49179=CARTESIAN_POINT('Ctrl Pts',(-23.9379555753677,2.51725737821055,-4.87688144343666));
#49180=CARTESIAN_POINT('Ctrl Pts',(-23.6993179102484,5.46362866211312,-0.518959721751974));
#49181=CARTESIAN_POINT('Ctrl Pts',(-23.4606802451293,3.39041383626465,4.31574458911784));
#49182=CARTESIAN_POINT('Ctrl Pts',(-23.22204258001,-1.79766754297636,5.1854555000254));
#49183=CARTESIAN_POINT('Ctrl Pts',(-22.9834049148908,-5.33418224799811,
1.29114564897465));
#49184=CARTESIAN_POINT('Ctrl Pts',(-22.7447672497716,-3.97003683117282,
-3.78937526502026));
#49185=CARTESIAN_POINT('Ctrl Pts',(-22.5061295846523,1.04149074721631,-5.38849277288));
#49186=CARTESIAN_POINT('Ctrl Pts',(-22.2674919195332,5.09617209617701,-2.03705358461264));
#49187=CARTESIAN_POINT('Ctrl Pts',(-22.0288542544139,4.46885980435008,3.18588282729214));
#49188=CARTESIAN_POINT('Ctrl Pts',(-21.7902165892947,-0.264117051042074,
5.48186095441396));
#49189=CARTESIAN_POINT('Ctrl Pts',(-21.5515789241754,-4.75444229852842,
2.74150246584068));
#49190=CARTESIAN_POINT('Ctrl Pts',(-21.3129412590562,-4.87673048077228,
-2.51754983229987));
#49191=CARTESIAN_POINT('Ctrl Pts',(-21.074303593937,-0.518632077245404,
-5.46365977241106));
#49192=CARTESIAN_POINT('Ctrl Pts',(-20.8356659288178,4.31594789749319,-3.39015502393968));
#49193=CARTESIAN_POINT('Ctrl Pts',(-20.5970282636985,5.1853476882785,1.79797850150613));
#49194=CARTESIAN_POINT('Ctrl Pts',(-20.3583905985793,1.29082576619906,5.3342596657391));
#49195=CARTESIAN_POINT('Ctrl Pts',(-20.1197529334601,-3.78961333343518,
3.96980958274648));
#49196=CARTESIAN_POINT('Ctrl Pts',(-19.8811152683408,-5.38843030706872,
-1.04181388264786));
#49197=CARTESIAN_POINT('Ctrl Pts',(-19.6424776032216,-2.0367479735616,-5.09629424507725));
#49198=CARTESIAN_POINT('Ctrl Pts',(-19.4038399381024,3.18615081025577,-4.46866874522171));
#49199=CARTESIAN_POINT('Ctrl Pts',(-19.1652022729832,5.48184510598211,0.264445786948331));
#49200=CARTESIAN_POINT('Ctrl Pts',(-18.9265646078639,2.74121734639358,4.75460669246635));
#49201=CARTESIAN_POINT('Ctrl Pts',(-18.6879269427447,-2.51784227566918,
4.87657949951273));
#49202=CARTESIAN_POINT('Ctrl Pts',(-18.4492892776255,-5.46369086392892,
0.518304431424697));
#49203=CARTESIAN_POINT('Ctrl Pts',(-18.2106516125063,-3.38989619897094,
-4.31615119063469));
#49204=CARTESIAN_POINT('Ctrl Pts',(-17.972013947387,1.7982894533345,-5.18523985773471));
#49205=CARTESIAN_POINT('Ctrl Pts',(-17.7333762822678,5.33433706441994,-1.29050587885931));
#49206=CARTESIAN_POINT('Ctrl Pts',(-17.4947386171486,3.96958231998011,3.78985138826264));
#49207=CARTESIAN_POINT('Ctrl Pts',(-17.2561009520293,-1.04213701429963,
5.38836782185863));
#49208=CARTESIAN_POINT('Ctrl Pts',(-17.0174632869101,-5.09641637566774,
2.03644235519705));
#49209=CARTESIAN_POINT('Ctrl Pts',(-16.7788256217909,-4.46847767001423,
-3.18641878176725));
#49210=CARTESIAN_POINT('Ctrl Pts',(-16.5401879566717,0.264774521898913,
-5.48182923783365));
#49211=CARTESIAN_POINT('Ctrl Pts',(-16.3015502915525,4.7547710693084,-2.74093221709016));
#49212=CARTESIAN_POINT('Ctrl Pts',(-16.0629126264332,4.87642850071492,2.51813470998477));
#49213=CARTESIAN_POINT('Ctrl Pts',(-15.824274961314,0.517976783740707,5.46372193579801));
#49214=CARTESIAN_POINT('Ctrl Pts',(-15.5856372961948,-4.31635446825496,
3.38963736181178));
#49215=CARTESIAN_POINT('Ctrl Pts',(-15.3469996310756,-5.18513200854378,
-1.79860039869607));
#49216=CARTESIAN_POINT('Ctrl Pts',(-15.1083619659563,-1.29018598687877,
-5.33441444391757));
#49217=CARTESIAN_POINT('Ctrl Pts',(-14.8697243008371,3.7900894294612,-3.9693550429385));
#49218=CARTESIAN_POINT('Ctrl Pts',(-14.6310866357179,5.38830531727106,1.0424601422037));
#49219=CARTESIAN_POINT('Ctrl Pts',(-14.3924489705986,2.03613672950916,5.09653848793067));
#49220=CARTESIAN_POINT('Ctrl Pts',(-14.1538113054794,-3.18668674181981,
4.46828657873739));
#49221=CARTESIAN_POINT('Ctrl Pts',(-13.9151736403602,-5.48181334997165,
-0.265103255897302));
#49222=CARTESIAN_POINT('Ctrl Pts',(-13.6765359752409,-2.74064707792992,
-4.75493542905149));
#49223=CARTESIAN_POINT('Ctrl Pts',(-13.4378983101217,2.51842713524471,-4.87627748438068));
#49224=CARTESIAN_POINT('Ctrl Pts',(-13.1992606450025,5.46375298801868,-0.517649134193991));
#49225=CARTESIAN_POINT('Ctrl Pts',(-12.9606229798833,3.38937851246291,4.31655773035292));
#49226=CARTESIAN_POINT('Ctrl Pts',(-12.721985314764,-1.79891133758957,5.18502414070623));
#49227=CARTESIAN_POINT('Ctrl Pts',(-12.4833476496448,-5.33449180423179,
1.28986609025851));
#49228=CARTESIAN_POINT('Ctrl Pts',(-12.2447099845256,-3.96912775162243,
-3.79032745703001));
#49229=CARTESIAN_POINT('Ctrl Pts',(-12.0060723194064,1.04278326635893,-5.38824279330623));
#49230=CARTESIAN_POINT('Ctrl Pts',(-11.7674346542871,5.0966605818656,-2.03583109649899));
#49231=CARTESIAN_POINT('Ctrl Pts',(-11.5287969891679,4.46809547139186,3.18695469041253));
#49232=CARTESIAN_POINT('Ctrl Pts',(-11.2901593240487,-0.265431988942334,
5.48179744239614));
#49233=CARTESIAN_POINT('Ctrl Pts',(-11.0515216589295,-4.75509977169506,
2.74036192891386));
#49234=CARTESIAN_POINT('Ctrl Pts',(-10.8128839938102,-4.87612645051055,
-2.51871955144797));
#49235=CARTESIAN_POINT('Ctrl Pts',(-10.574246328691,-0.517321482785775,
-5.46378402059077));
#49236=CARTESIAN_POINT('Ctrl Pts',(-10.3356086635718,4.3167609769278,-3.38911965092534));
#49237=CARTESIAN_POINT('Ctrl Pts',(-10.0969709984526,5.18491625422252,1.79922227001388));
#49238=CARTESIAN_POINT('Ctrl Pts',(-9.85833333333333,1.28954618899972,5.33456914536226));
#49239=CARTESIAN_POINT('Ctrl Pts',(-9.61969566821411,-3.79056547096819,
3.96890044603278));
#49240=CARTESIAN_POINT('Ctrl Pts',(-9.38105800309488,-5.38818024996436,
-1.04310638676421));
#49241=CARTESIAN_POINT('Ctrl Pts',(-9.14242033797565,-2.03552545616774,
-5.09678265747193));
#49242=CARTESIAN_POINT('Ctrl Pts',(-8.90378267285643,3.18722262754464,-4.46790434797868));
#49243=CARTESIAN_POINT('Ctrl Pts',(-8.6651450077372,5.48178151510679,0.265760721033513));
#49244=CARTESIAN_POINT('Ctrl Pts',(-8.42650734261798,2.74007677004376,4.7552640972372));
#49245=CARTESIAN_POINT('Ctrl Pts',(-8.18786967749874,-2.51901195859494,
4.87597539910758));
#49246=CARTESIAN_POINT('Ctrl Pts',(-7.94923201237954,-5.46381503351144,
0.516993829512319));
#49247=CARTESIAN_POINT('Ctrl Pts',(-7.71059434726029,-3.38886077720523,
-4.31696420796962));
#49248=CARTESIAN_POINT('Ctrl Pts',(-7.47195668214107,1.7995331959781,-5.18480834911082));
#49249=CARTESIAN_POINT('Ctrl Pts',(-7.23331901702184,5.33464646728914,-1.28922628306928));
#49250=CARTESIAN_POINT('Ctrl Pts',(-6.99468135190262,3.96867312620793,3.79080347120911));
#49251=CARTESIAN_POINT('Ctrl Pts',(-6.75604368678338,-1.04342950349043,
5.38811768737191));
#49252=CARTESIAN_POINT('Ctrl Pts',(-6.51740602166417,-5.09690471461091,
2.03521980827418));
#49253=CARTESIAN_POINT('Ctrl Pts',(-6.27876835654494,-4.467713208764,-3.18749055274999));
#49254=CARTESIAN_POINT('Ctrl Pts',(-6.04013069142571,0.266089452679246,
-5.48176556899668));
#49255=CARTESIAN_POINT('Ctrl Pts',(-5.80149302630648,4.75542840469908,-2.73979159960635));
#49256=CARTESIAN_POINT('Ctrl Pts',(-5.56285536118726,4.87582433205023,2.5193043533937));
#49257=CARTESIAN_POINT('Ctrl Pts',(-5.32421769606802,0.516666170769886,
5.46384603309797));
#49258=CARTESIAN_POINT('Ctrl Pts',(-5.08558003094881,-4.31716741655734,
3.38860187917618));
#49259=CARTESIAN_POINT('Ctrl Pts',(-4.84694236582958,-5.18470043865627,
-1.79984409220056));
#49260=CARTESIAN_POINT('Ctrl Pts',(-4.60830470071034,-1.28890634696599,
-5.3347238147032));
#49261=CARTESIAN_POINT('Ctrl Pts',(-4.36966703559113,3.79104140879587,-3.96844570635655));
#49262=CARTESIAN_POINT('Ctrl Pts',(-4.13102937047189,5.38805519950874,1.04375245184379));
#49263=CARTESIAN_POINT('Ctrl Pts',(-3.89239170535267,2.03491397240924,5.09702706943807));
#49264=CARTESIAN_POINT('Ctrl Pts',(-3.65375404023344,-3.18775811969919,
4.46752144683269));
#49265=CARTESIAN_POINT('Ctrl Pts',(-3.41511637511422,-5.48175026890294,
-0.266417018798925));
#49266=CARTESIAN_POINT('Ctrl Pts',(-3.17647870999499,-2.7395051413334,-4.75559493065073));
#49267=CARTESIAN_POINT('Ctrl Pts',(-2.93784104487577,2.51959428582449,-4.87566895585645));
#49268=CARTESIAN_POINT('Ctrl Pts',(-2.69920337975653,5.4638817225832,-0.516346748639057));
#49269=CARTESIAN_POINT('Ctrl Pts',(-2.46056571463731,3.38833392817308,4.31738642478165));
#49270=CARTESIAN_POINT('Ctrl Pts',(-2.22192804951809,-1.80013762659788,
5.18456214962629));
#49271=CARTESIAN_POINT('Ctrl Pts',(-1.98329038439885,-5.33483445954559,
1.28864468737176));
#49272=CARTESIAN_POINT('Ctrl Pts',(-1.74465271927964,-3.96815431503542,
-3.79139121370463));
#49273=CARTESIAN_POINT('Ctrl Pts',(-1.50601505416041,1.0439526175495,-5.38777791511351));
#49274=CARTESIAN_POINT('Ctrl Pts',(-1.26737738904118,5.09738511987209,-2.03502045294416));
#49275=CARTESIAN_POINT('Ctrl Pts',(-1.02873972392196,4.46687700346276,3.18881740351592));
#49276=CARTESIAN_POINT('Ctrl Pts',(-0.790102058802729,-0.265874035238907,
5.48021323433553));
#49277=CARTESIAN_POINT('Ctrl Pts',(-0.551464393683494,-4.75744712505124,
2.74215692220397));
#49278=CARTESIAN_POINT('Ctrl Pts',(-0.312826728564273,-4.87214411143407,
-2.52568128330601));
#49279=CARTESIAN_POINT('Ctrl Pts',(-0.113962007631581,-1.24846965546114,
-4.96376157560509));
#49280=CARTESIAN_POINT('Ctrl Pts',(0.0451297691145686,1.91119551719046,
-4.43560896973968));
#49281=CARTESIAN_POINT('Ctrl Pts',(0.124675657487644,3.17317635443185,-3.47270950061224));
#49282=CARTESIAN_POINT('Ctrl Pts',(0.164448601674182,3.65041170719118,-2.86454901554259));
#49283=CARTESIAN_POINT('Ctrl Pts',(-29.7394486016742,2.52761008811552,-3.54684587865065));
#49284=CARTESIAN_POINT('Ctrl Pts',(-29.6996756574876,3.11851645239715,-3.12574472608009));
#49285=CARTESIAN_POINT('Ctrl Pts',(-29.6201297691146,4.07604700037463,-1.9842316340791));
#49286=CARTESIAN_POINT('Ctrl Pts',(-29.4610379923684,4.70821035020098,0.955422084332599));
#49287=CARTESIAN_POINT('Ctrl Pts',(-29.2621732714357,2.57930446702286,4.45871287587165));
#49288=CARTESIAN_POINT('Ctrl Pts',(-29.0235356063165,-2.36486757903556,
4.57951285086845));
#49289=CARTESIAN_POINT('Ctrl Pts',(-28.7848979411973,-5.12680154578104,
0.486834481531294));
#49290=CARTESIAN_POINT('Ctrl Pts',(-28.546260276078,-3.18350352009034,-4.04998412230631));
#49291=CARTESIAN_POINT('Ctrl Pts',(-28.3076226109588,1.6871112561347,-4.86759179267321));
#49292=CARTESIAN_POINT('Ctrl Pts',(-28.0689849458396,5.00640601099863,-1.21236534218581));
#49293=CARTESIAN_POINT('Ctrl Pts',(-27.8303472807204,3.72686752876241,3.55625523601567));
#49294=CARTESIAN_POINT('Ctrl Pts',(-27.5917096156011,-0.977006116615824,
5.05787502748919));
#49295=CARTESIAN_POINT('Ctrl Pts',(-27.3530719504819,-4.7830901536011,1.91256654887478));
#49296=CARTESIAN_POINT('Ctrl Pts',(-27.1144342853627,-4.19491506055882,
-2.98980739123073));
#49297=CARTESIAN_POINT('Ctrl Pts',(-26.8757966202435,0.247294810559338,
-5.1453952954096));
#49298=CARTESIAN_POINT('Ctrl Pts',(-26.6371589551242,4.46228166941837,-2.57375000033875));
#49299=CARTESIAN_POINT('Ctrl Pts',(-26.398521290005,4.57766126194414,2.3624615172601));
#49300=CARTESIAN_POINT('Ctrl Pts',(-26.1598836248858,0.487410215497018,
5.12821915499749));
#49301=CARTESIAN_POINT('Ctrl Pts',(-25.9212459597666,-4.05063427769259,
3.1825382547137));
#49302=CARTESIAN_POINT('Ctrl Pts',(-25.6826082946473,-4.86725146393007,
-1.68702693864012));
#49303=CARTESIAN_POINT('Ctrl Pts',(-25.4439706295281,-1.21218968322454,
-5.0066746732594));
#49304=CARTESIAN_POINT('Ctrl Pts',(-25.2053329644089,3.55654361144349,-3.7265521774304));
#49305=CARTESIAN_POINT('Ctrl Pts',(-24.9666952992897,5.05778262729025,0.977256248438136));
#49306=CARTESIAN_POINT('Ctrl Pts',(-24.7280576341704,1.91229732115414,4.78323253901292));
#49307=CARTESIAN_POINT('Ctrl Pts',(-24.4894199690512,-2.99006811912389,
4.19472133001462));
#49308=CARTESIAN_POINT('Ctrl Pts',(-24.250782303932,-5.14537567821884,-0.247595852320659));
#49309=CARTESIAN_POINT('Ctrl Pts',(-24.0121446388127,-2.57348489053941,
-4.46243991986699));
#49310=CARTESIAN_POINT('Ctrl Pts',(-23.7735069736935,2.3627373229194,-4.57751754175089));
#49311=CARTESIAN_POINT('Ctrl Pts',(-23.5348693085743,5.12824769937646,-0.487103748027066));
#49312=CARTESIAN_POINT('Ctrl Pts',(-23.2962316434551,3.18229569229794,4.05082567446672));
#49313=CARTESIAN_POINT('Ctrl Pts',(-23.0575939783358,-1.68731899834989,
4.8671499991618));
#49314=CARTESIAN_POINT('Ctrl Pts',(-22.8189563132166,-5.00674726140177,
1.21188959085538));
#49315=CARTESIAN_POINT('Ctrl Pts',(-22.5803186480974,-3.72633894156846,
-3.55676715726841));
#49316=CARTESIAN_POINT('Ctrl Pts',(-22.3416809829781,0.97755957782614,-5.05772397330915));
#49317=CARTESIAN_POINT('Ctrl Pts',(-22.1030433178589,4.78334719361007,-1.91201049793817));
#49318=CARTESIAN_POINT('Ctrl Pts',(-21.8644056527397,4.19454202102207,2.99031967396282));
#49319=CARTESIAN_POINT('Ctrl Pts',(-21.6257679876205,-0.247904413556711,
5.14536081537106));
#49320=CARTESIAN_POINT('Ctrl Pts',(-21.3871303225013,-4.4625942367424,2.57321728520339));
#49321=CARTESIAN_POINT('Ctrl Pts',(-21.148492657382,-4.57737584582237,-2.36301182492228));
#49322=CARTESIAN_POINT('Ctrl Pts',(-20.9098549922628,-0.486796215745698,
-5.12827689999088));
#49323=CARTESIAN_POINT('Ctrl Pts',(-20.6712173271436,4.05101650290193,-3.18205276698362));
#49324=CARTESIAN_POINT('Ctrl Pts',(-20.4325796620244,4.86704880536236,1.68761086891128));
#49325=CARTESIAN_POINT('Ctrl Pts',(-20.1939419969051,1.21158934385664,5.00681992690976));
#49326=CARTESIAN_POINT('Ctrl Pts',(-19.9553043317859,-3.55699061202287,
3.72612564262527));
#49327=CARTESIAN_POINT('Ctrl Pts',(-19.7166666666667,-5.05766534191731,
-0.977862877818859));
#49328=CARTESIAN_POINT('Ctrl Pts',(-19.4780290015474,-1.91172364660431,
-4.78346184448688));
#49329=CARTESIAN_POINT('Ctrl Pts',(-19.2393913364282,2.99057120698267,-4.19436268992253));
#49330=CARTESIAN_POINT('Ctrl Pts',(-19.000753671309,5.14534593978394,0.248212970242977));
#49331=CARTESIAN_POINT('Ctrl Pts',(-18.7621160061898,2.57294966761094,4.46274853947527));
#49332=CARTESIAN_POINT('Ctrl Pts',(-18.5234783410705,-2.36328631686318,
4.57723413244015));
#49333=CARTESIAN_POINT('Ctrl Pts',(-18.2848406759513,-5.12830608297801,
0.486488682230852));
#49334=CARTESIAN_POINT('Ctrl Pts',(-18.0462030108321,-3.18180982980166,
-4.0512073170384));
#49335=CARTESIAN_POINT('Ctrl Pts',(-17.8075653457129,1.68790273318265,-4.86694759391988));
#49336=CARTESIAN_POINT('Ctrl Pts',(-17.5689276805936,5.00689257452757,-1.21128909257392));
#49337=CARTESIAN_POINT('Ctrl Pts',(-17.3302900154744,3.72591233022232,3.55721405402392));
#49338=CARTESIAN_POINT('Ctrl Pts',(-17.0916523503552,-0.978166174263816,
5.05760669231743));
#49339=CARTESIAN_POINT('Ctrl Pts',(-16.8530146852359,-4.78357647817786,
1.91143678840589));
#49340=CARTESIAN_POINT('Ctrl Pts',(-16.6143770201167,-4.19418334373088,
-2.99082272925335));
#49341=CARTESIAN_POINT('Ctrl Pts',(-16.3757393549975,0.248521526032233,
-5.14533104569049));
#49342=CARTESIAN_POINT('Ctrl Pts',(-16.1371016898783,4.46290282616169,-2.57268204076719));
#49343=CARTESIAN_POINT('Ctrl Pts',(-15.8984640247591,4.57709240259623,2.36356080030613));
#49344=CARTESIAN_POINT('Ctrl Pts',(-15.6598263596398,0.486181146967108,
5.12833524752249));
#49345=CARTESIAN_POINT('Ctrl Pts',(-15.4211886945206,-4.05139811660642,
3.18156688117757));
#49346=CARTESIAN_POINT('Ctrl Pts',(-15.1825510294014,-4.86684636497488,
-1.68819459138417));
#49347=CARTESIAN_POINT('Ctrl Pts',(-14.9439133642821,-1.21098883693528,
-5.00696520413972));
#49348=CARTESIAN_POINT('Ctrl Pts',(-14.7052756991629,3.55743748323268,-3.7256990044204));
#49349=CARTESIAN_POINT('Ctrl Pts',(-14.4666380340437,5.05754802452954,0.978469467191119));
#49350=CARTESIAN_POINT('Ctrl Pts',(-14.2280003689245,1.91114992333367,4.7836910946663));
#49351=CARTESIAN_POINT('Ctrl Pts',(-13.9893627038052,-2.99107424076851,
4.19400398245627));
#49352=CARTESIAN_POINT('Ctrl Pts',(-13.750725038686,-5.1453161330936,-0.248830080927746));
#49353=CARTESIAN_POINT('Ctrl Pts',(-13.5120873735668,-2.57241440467166,
-4.46305709679875));
#49354=CARTESIAN_POINT('Ctrl Pts',(-13.2734497084476,2.3638352752493,-4.57695065629236));
#49355=CARTESIAN_POINT('Ctrl Pts',(-13.0348120433283,5.12836439362466,-0.485873609954974));
#49356=CARTESIAN_POINT('Ctrl Pts',(-12.7961743782091,3.18132392111204,4.05158890160494));
#49357=CARTESIAN_POINT('Ctrl Pts',(-12.5575367130899,-1.68848644351467,
4.86674511852789));
#49358=CARTESIAN_POINT('Ctrl Pts',(-12.3188990479707,-5.00703781574603,
1.21068857694173));
#49359=CARTESIAN_POINT('Ctrl Pts',(-12.0802613828514,-3.72548566522024,
-3.55766089964832));
#49360=CARTESIAN_POINT('Ctrl Pts',(-11.8416237177322,0.978772756599708,
-5.05748933855386));
#49361=CARTESIAN_POINT('Ctrl Pts',(-11.602986052613,4.78380569395181,-1.91086305138862));
#49362=CARTESIAN_POINT('Ctrl Pts',(-11.3643483874938,4.19382460609933,2.99132574152728));
#49363=CARTESIAN_POINT('Ctrl Pts',(-11.1257107223745,-0.249138634928415,
5.14530120199331));
#49364=CARTESIAN_POINT('Ctrl Pts',(-10.8870730572553,-4.46321135138594,
2.57214675932532));
#49365=CARTESIAN_POINT('Ctrl Pts',(-10.6484353921361,-4.57680889352901,
-2.36410974169172));
#49366=CARTESIAN_POINT('Ctrl Pts',(-10.4097977270168,-0.485566071195607,
-5.12839352128436));
#49367=CARTESIAN_POINT('Ctrl Pts',(-10.1711600618976,4.05177967203326,-3.18108094960599));
#49368=CARTESIAN_POINT('Ctrl Pts',(-9.93252239677838,4.86664385457931,1.68877828957306));
#49369=CARTESIAN_POINT('Ctrl Pts',(-9.69388473165916,1.21038831259436,5.00711040934616));
#49370=CARTESIAN_POINT('Ctrl Pts',(-9.45524706653992,-3.55788430327004,
3.72527231262268));
#49371=CARTESIAN_POINT('Ctrl Pts',(-9.21660940142071,-5.0574306343906,-0.979076042488542));
#49372=CARTESIAN_POINT('Ctrl Pts',(-8.97797173630147,-1.91057617257191,
-4.78392027603378));
#49373=CARTESIAN_POINT('Ctrl Pts',(-8.73933407118225,2.99157723152894,-4.19364521466106));
#49374=CARTESIAN_POINT('Ctrl Pts',(-8.50069640606303,5.14528625238931,0.249447188033793));
#49375=CARTESIAN_POINT('Ctrl Pts',(-8.26205874094379,2.57187910472981,4.46336558992145));
#49376=CARTESIAN_POINT('Ctrl Pts',(-8.02342107582458,-2.36438419963377,
4.57666711430907));
#49377=CARTESIAN_POINT('Ctrl Pts',(-7.78478341070534,-5.12842263049894,
0.485258530685497));
#49378=CARTESIAN_POINT('Ctrl Pts',(-7.54614574558613,-3.18083796666522,
-4.051970427882));
#49379=CARTESIAN_POINT('Ctrl Pts',(-7.30750808046688,1.68907012956793,-4.86654257314621));
#49380=CARTESIAN_POINT('Ctrl Pts',(-7.06887041534768,5.00718298492152,-1.21008804386212));
#49381=CARTESIAN_POINT('Ctrl Pts',(-6.83023275022843,3.72505894666373,3.55810769403531));
#49382=CARTESIAN_POINT('Ctrl Pts',(-6.59159508510922,-0.979379324924138,
5.05737191215842));
#49383=CARTESIAN_POINT('Ctrl Pts',(-6.35295741998998,-4.78403484078203,
1.91028928665709));
#49384=CARTESIAN_POINT('Ctrl Pts',(-6.11431975487076,-4.19346580839123,
-2.99182871033596));
#49385=CARTESIAN_POINT('Ctrl Pts',(-5.87568208975153,0.24975574072106,-5.14527128511983));
#49386=CARTESIAN_POINT('Ctrl Pts',(-5.63704442463231,4.46351981148654,-2.57161143927705));
#49387=CARTESIAN_POINT('Ctrl Pts',(-5.39840675951308,4.57652532039568,2.3646586459856));
#49388=CARTESIAN_POINT('Ctrl Pts',(-5.15976909439384,0.48495098504212,5.12845172719788));
#49389=CARTESIAN_POINT('Ctrl Pts',(-4.92113142927463,-4.05216116265496,
3.18059496090769));
#49390=CARTESIAN_POINT('Ctrl Pts',(-4.68249376415541,-4.86644128669823,
-1.68936194164671));
#49391=CARTESIAN_POINT('Ctrl Pts',(-4.44385609903616,-1.20978774680917,
-5.00725558441954));
#49392=CARTESIAN_POINT('Ctrl Pts',(-4.20521843391696,3.55833102599239,-3.72484548681831));
#49393=CARTESIAN_POINT('Ctrl Pts',(-3.96658076879771,5.05731326006834,0.97968244932232));
#49394=CARTESIAN_POINT('Ctrl Pts',(-3.7279431036785,1.91000222430937,4.78414968494508));
#49395=CARTESIAN_POINT('Ctrl Pts',(-3.48930543855926,-2.99207985287812,
4.1932858176298));
#49396=CARTESIAN_POINT('Ctrl Pts',(-3.25066777344004,-5.14525692421147,
-0.250063199427267));
#49397=CARTESIAN_POINT('Ctrl Pts',(-3.01203010832081,-2.57134256504161,
-4.46367611536099));
#49398=CARTESIAN_POINT('Ctrl Pts',(-2.77339244320159,2.36493078112016,-4.57637948185914));
#49399=CARTESIAN_POINT('Ctrl Pts',(-2.53475477808235,5.12848522590942,-0.484651170411792));
#49400=CARTESIAN_POINT('Ctrl Pts',(-2.29611711296313,3.1803434578865,4.05236672721506));
#49401=CARTESIAN_POINT('Ctrl Pts',(-2.0574794478439,-1.68963745764365,4.86631148644208));
#49402=CARTESIAN_POINT('Ctrl Pts',(-1.81884178272468,-5.00735943740691,
1.20954214900319));
#49403=CARTESIAN_POINT('Ctrl Pts',(-1.58020411760546,-3.72457198234636,
-3.55865935837542));
#49404=CARTESIAN_POINT('Ctrl Pts',(-1.34156645248623,0.979870327998434,
-5.05705299657864));
#49405=CARTESIAN_POINT('Ctrl Pts',(-1.102928787367,4.78448575670765,-1.91010216861234));
#49406=CARTESIAN_POINT('Ctrl Pts',(-0.86429112224778,4.19268093295817,2.99307411331055));
#49407=CARTESIAN_POINT('Ctrl Pts',(-0.62565345712855,-0.24955354652721,
5.14381423941869));
#49408=CARTESIAN_POINT('Ctrl Pts',(-0.387015792009318,-4.46541461412448,
2.57383156822791));
#49409=CARTESIAN_POINT('Ctrl Pts',(-0.148378126890095,-4.57307100750672,
-2.37064413258696));
#49410=CARTESIAN_POINT('Ctrl Pts',(0.050486594042596,-1.17183323287632,
-4.6590645987469));
#49411=CARTESIAN_POINT('Ctrl Pts',(0.209578370788747,1.79387813854466,-4.16333226526479));
#49412=CARTESIAN_POINT('Ctrl Pts',(0.289124259161822,2.9783931789093,-3.25953969577237));
#49413=CARTESIAN_POINT('Ctrl Pts',(0.32889720334836,3.42633377868325,-2.68871070989398));
#49414=CARTESIAN_POINT('Ctrl Pts',(-29.575,2.36230756092324,-3.31488661006752));
#49415=CARTESIAN_POINT('Ctrl Pts',(-29.5352270558135,2.91456939066647,-2.92132494432319));
#49416=CARTESIAN_POINT('Ctrl Pts',(-29.4556811674404,3.80947864266608,-1.85446537575054));
#49417=CARTESIAN_POINT('Ctrl Pts',(-29.2965893906943,4.40029930288375,0.892938679230673));
#49418=CARTESIAN_POINT('Ctrl Pts',(-29.0977246697615,2.41062119233501,4.16711865021482));
#49419=CARTESIAN_POINT('Ctrl Pts',(-28.8590870046423,-2.21020820766824,
4.28001845847083));
#49420=CARTESIAN_POINT('Ctrl Pts',(-28.6204493395231,-4.79151515967436,
0.454996117497237));
#49421=CARTESIAN_POINT('Ctrl Pts',(-28.3818116744039,-2.97530638570203,
-3.7851202441102));
#49422=CARTESIAN_POINT('Ctrl Pts',(-28.1431740092847,1.57677629758835,-4.54925739906848));
#49423=CARTESIAN_POINT('Ctrl Pts',(-27.9045363441654,4.67899334175034,-1.13307817052668));
#49424=CARTESIAN_POINT('Ctrl Pts',(-27.6658986790463,3.48313507021902,3.32368060727122));
#49425=CARTESIAN_POINT('Ctrl Pts',(-27.4272610139269,-0.913111142894123,
4.72709634916456));
#49426=CARTESIAN_POINT('Ctrl Pts',(-27.1886233488078,-4.47028206112812,
1.78748709716699));
#49427=CARTESIAN_POINT('Ctrl Pts',(-26.9499856836885,-3.92057288091334,
-2.79427774054909));
#49428=CARTESIAN_POINT('Ctrl Pts',(-26.7113480185693,0.231122040344854,
-4.80889290141546));
#49429=CARTESIAN_POINT('Ctrl Pts',(-26.4727103534501,4.17045404914302,-2.40542998080026));
#49430=CARTESIAN_POINT('Ctrl Pts',(-26.2340726883308,4.27828796113812,2.20795949931288));
#49431=CARTESIAN_POINT('Ctrl Pts',(-25.9954350232116,0.45553419918425,4.79284005902739));
#49432=CARTESIAN_POINT('Ctrl Pts',(-25.7567973580924,-3.78572788015027,
2.97440424746946));
#49433=CARTESIAN_POINT('Ctrl Pts',(-25.5181596929732,-4.54893932739796,
-1.57669749435209));
#49434=CARTESIAN_POINT('Ctrl Pts',(-25.2795220278539,-1.132913999441,-4.67924443383647));
#49435=CARTESIAN_POINT('Ctrl Pts',(-25.0408843627347,3.32395012330801,-3.48284034246832));
#49436=CARTESIAN_POINT('Ctrl Pts',(-24.8022466976155,4.72700999182265,0.913344916409211));
#49437=CARTESIAN_POINT('Ctrl Pts',(-24.5636090324962,1.78723547660136,4.47041513471273));
#49438=CARTESIAN_POINT('Ctrl Pts',(-24.324971367377,-2.7945214171653,3.92039182010356));
#49439=CARTESIAN_POINT('Ctrl Pts',(-24.0863337022578,-4.80887456716434,
-0.231403394352836));
#49440=CARTESIAN_POINT('Ctrl Pts',(-23.8476960371386,-2.40518220884904,
-4.17060195021093));
#49441=CARTESIAN_POINT('Ctrl Pts',(-23.6090583720194,2.20821726762825,-4.27815364006511));
#49442=CARTESIAN_POINT('Ctrl Pts',(-23.3704207069001,4.7928667366398,-0.455247774302161));
#49443=CARTESIAN_POINT('Ctrl Pts',(-23.1317830417809,2.97417754833123,3.7859067598156));
#49444=CARTESIAN_POINT('Ctrl Pts',(-22.8931453766616,-1.57697045372341,
4.54884449829819));
#49445=CARTESIAN_POINT('Ctrl Pts',(-22.6545077115425,-4.67931227480544,
1.13263353273611));
#49446=CARTESIAN_POINT('Ctrl Pts',(-22.4158700464232,-3.48264105196409,
-3.32415904951658));
#49447=CARTESIAN_POINT('Ctrl Pts',(-22.177232381304,0.913628408435968,-4.7269551737383));
#49448=CARTESIAN_POINT('Ctrl Pts',(-21.9385947161847,4.47052229104313,-1.7869674112637));
#49449=CARTESIAN_POINT('Ctrl Pts',(-21.6999570510656,3.92022423769407,2.79475652063351));
#49450=CARTESIAN_POINT('Ctrl Pts',(-21.4613193859463,-0.231691776071347,
4.80886067632815));
#49451=CARTESIAN_POINT('Ctrl Pts',(-21.2226817208271,-4.17074617495639,
2.40493210456611));
#49452=CARTESIAN_POINT('Ctrl Pts',(-20.9840440557078,-4.27802121087247,
-2.20847381754468));
#49453=CARTESIAN_POINT('Ctrl Pts',(-20.7454063905886,-0.454960354245989,
-4.79289402757069));
#49454=CARTESIAN_POINT('Ctrl Pts',(-20.5067687254694,3.78608510831067,-2.97395051002756));
#49455=CARTESIAN_POINT('Ctrl Pts',(-20.2681310603502,4.54874992244621,1.57724323631644));
#49456=CARTESIAN_POINT('Ctrl Pts',(-20.0294933952309,1.13235292151423,4.67938018808041));
#49457=CARTESIAN_POINT('Ctrl Pts',(-19.7908557301117,-3.32436789061056,
3.48244170250407));
#49458=CARTESIAN_POINT('Ctrl Pts',(-19.5522180649925,-4.7269003767659,-0.91391187298986));
#49459=CARTESIAN_POINT('Ctrl Pts',(-19.3135803998733,-1.78669931964703,
-4.4706294438965));
#49460=CARTESIAN_POINT('Ctrl Pts',(-19.074942734754,2.79499160370957,-3.92005663462335));
#49461=CARTESIAN_POINT('Ctrl Pts',(-18.8363050696348,4.80884677358576,0.231980153537627));
#49462=CARTESIAN_POINT('Ctrl Pts',(-18.5976674045156,2.4046819888283,4.1708903864842));
#49463=CARTESIAN_POINT('Ctrl Pts',(-18.3590297393964,-2.20873035805718,
4.27788876536757));
#49464=CARTESIAN_POINT('Ctrl Pts',(-18.1203920742771,-4.79292130202709,
0.454672933037013));
#49465=CARTESIAN_POINT('Ctrl Pts',(-17.8817544091579,-2.97372346063237,
-3.78626344344212));
#49466=CARTESIAN_POINT('Ctrl Pts',(-17.6431167440387,1.5775160130308,-4.54865533010503));
#49467=CARTESIAN_POINT('Ctrl Pts',(-17.4044790789195,4.6794480846352,-1.13207230628853));
#49468=CARTESIAN_POINT('Ctrl Pts',(-17.1658414138002,3.48224234046452,3.3245767197852));
#49469=CARTESIAN_POINT('Ctrl Pts',(-16.927203748681,-0.914195334228,4.72684556277623));
#49470=CARTESIAN_POINT('Ctrl Pts',(-16.6885660835618,-4.47073658068798,
1.78643122161473));
#49471=CARTESIAN_POINT('Ctrl Pts',(-16.4499284184426,-3.91988901744752,
-2.79522667673945));
#49472=CARTESIAN_POINT('Ctrl Pts',(-16.2112907533233,0.232268530165553,
-4.80883285354733));
#49473=CARTESIAN_POINT('Ctrl Pts',(-15.9726530882041,4.17103458301497,-2.40443186444421));
#49474=CARTESIAN_POINT('Ctrl Pts',(-15.7340154230849,4.27775630447756,2.20898689062749));
#49475=CARTESIAN_POINT('Ctrl Pts',(-15.4953777579657,0.454385510193501,
4.79294855924697));
#49476=CARTESIAN_POINT('Ctrl Pts',(-15.2567400928464,-3.78644176495787,
2.97349640054336));
#49477=CARTESIAN_POINT('Ctrl Pts',(-15.0181024277272,-4.54856072140599,
-1.57778878407227));
#49478=CARTESIAN_POINT('Ctrl Pts',(-14.7794647626079,-1.13179168699179,
-4.67951596436188));
#49479=CARTESIAN_POINT('Ctrl Pts',(-14.5408270974888,3.32478553700414,-3.48204296590229));
#49480=CARTESIAN_POINT('Ctrl Pts',(-14.3021894323695,4.72679073178803,0.914478792178541));
#49481=CARTESIAN_POINT('Ctrl Pts',(-14.0635517672503,1.78616311715816,4.47084370140194));
#49482=CARTESIAN_POINT('Ctrl Pts',(-13.8249141021311,-2.79546173971721,
3.91972138617514));
#49483=CARTESIAN_POINT('Ctrl Pts',(-13.5862764370118,-4.80881891621556,
-0.232556905958181));
#49484=CARTESIAN_POINT('Ctrl Pts',(-13.3476387718926,-2.40418173141341,
-4.17117876454601));
#49485=CARTESIAN_POINT('Ctrl Pts',(-13.1090011067734,2.20924341525388,-4.27762382820403));
#49486=CARTESIAN_POINT('Ctrl Pts',(-12.8703634416541,4.79297579923065,-0.454098085715957));
#49487=CARTESIAN_POINT('Ctrl Pts',(-12.6317257765349,2.97326932976115,3.78662007285696));
#49488=CARTESIAN_POINT('Ctrl Pts',(-12.3930881114157,-1.57806154943975,
4.54846609634954));
#49489=CARTESIAN_POINT('Ctrl Pts',(-12.1544504462965,-4.67958382726028,
1.13151106362493));
#49490=CARTESIAN_POINT('Ctrl Pts',(-11.9158127811773,-3.48184357881804,
-3.32499434226663));
#49491=CARTESIAN_POINT('Ctrl Pts',(-11.677175116058,0.914762246840484,-4.7267358838015));
#49492=CARTESIAN_POINT('Ctrl Pts',(-11.4385374509388,4.47095080603802,-1.78589500627826));
#49493=CARTESIAN_POINT('Ctrl Pts',(-11.1998997858196,3.91955374080681,2.79569679264203));
#49494=CARTESIAN_POINT('Ctrl Pts',(-10.9612621207003,-0.232845280914501,
4.80880496159049));
#49495=CARTESIAN_POINT('Ctrl Pts',(-10.7226244555811,-4.17132293107681,
2.40393158973677));
#49496=CARTESIAN_POINT('Ctrl Pts',(-10.4839867904619,-4.27749133654748,
-2.20949993193547));
#49497=CARTESIAN_POINT('Ctrl Pts',(-10.2453491253427,-0.453810659605433,
-4.79300302197796));
#49498=CARTESIAN_POINT('Ctrl Pts',(-10.0067114602234,3.78679836713871,-2.97304224828663));
#49499=CARTESIAN_POINT('Ctrl Pts',(-9.76807379510421,4.54837145493611,1.57833430913225));
#49500=CARTESIAN_POINT('Ctrl Pts',(-9.52943612998497,1.131230436189,4.67965167333008));
#49501=CARTESIAN_POINT('Ctrl Pts',(-9.29079846486575,-3.3252031355719,3.48164417921258));
#49502=CARTESIAN_POINT('Ctrl Pts',(-9.05216079974653,-4.72668101881683,
-0.915045698212859));
#49503=CARTESIAN_POINT('Ctrl Pts',(-8.8135231346273,-1.78562688897607,-4.47105789459565));
#49504=CARTESIAN_POINT('Ctrl Pts',(-8.57488546950807,2.79593183551325,-3.91938608134342));
#49505=CARTESIAN_POINT('Ctrl Pts',(-8.33624780438884,4.80879098967182,0.233133655034067));
#49506=CARTESIAN_POINT('Ctrl Pts',(-8.09761013926962,2.40368143941586,4.17146708260569));
#49507=CARTESIAN_POINT('Ctrl Pts',(-7.85897247415039,-2.20975644067261,
4.27735882951057));
#49508=CARTESIAN_POINT('Ctrl Pts',(-7.62033480903117,-4.79303022748644,
0.453523231858677));
#49509=CARTESIAN_POINT('Ctrl Pts',(-7.38169714391193,-2.97281515612521,
-3.78697664779438));
#49510=CARTESIAN_POINT('Ctrl Pts',(-7.14305947879272,1.57860706315775,-4.5482767971816));
#49511=CARTESIAN_POINT('Ctrl Pts',(-6.90442181367349,4.6797195025539,-1.13094980465497));
#49512=CARTESIAN_POINT('Ctrl Pts',(-6.66578414855425,3.48144476711953,3.32541191686152));
#49513=CARTESIAN_POINT('Ctrl Pts',(-6.42714648343504,-0.91532914635784,
4.72662613694493));
#49514=CARTESIAN_POINT('Ctrl Pts',(-6.1885088183158,-4.47116496695316,1.78535876503999));
#49515=CARTESIAN_POINT('Ctrl Pts',(-5.94987115319659,-3.91921840801846,
-2.79616686792193));
#49516=CARTESIAN_POINT('Ctrl Pts',(-5.71123348807733,0.233422028762872,
-4.80877700124299));
#49517=CARTESIAN_POINT('Ctrl Pts',(-5.47259582295814,4.171611218274,-2.40343127894775));
#49518=CARTESIAN_POINT('Ctrl Pts',(-5.23395815783889,4.27722630874114,2.21001293857749));
#49519=CARTESIAN_POINT('Ctrl Pts',(-4.99532049271968,0.453235799314355,
4.7930574212978));
#49520=CARTESIAN_POINT('Ctrl Pts',(-4.75668282760044,-3.7871549087526,2.97258804263921));
#49521=CARTESIAN_POINT('Ctrl Pts',(-4.51804516248123,-4.54818213474018,
-1.57887979109285));
#49522=CARTESIAN_POINT('Ctrl Pts',(-4.27940749736198,-1.13066914665236,
-4.67978735413588));
#49523=CARTESIAN_POINT('Ctrl Pts',(-4.04076983224278,3.32562064318893,-3.48124526728007));
#49524=CARTESIAN_POINT('Ctrl Pts',(-3.80213216712354,4.72657132062792,0.915612446800854));
#49525=CARTESIAN_POINT('Ctrl Pts',(-3.56349450200431,1.78509047620951,4.4712723004521));
#49526=CARTESIAN_POINT('Ctrl Pts',(-3.32485683688509,-2.79640158605707,
3.91905018842691));
#49527=CARTESIAN_POINT('Ctrl Pts',(-3.08621917176585,-4.80876357952,-0.233709380055606));
#49528=CARTESIAN_POINT('Ctrl Pts',(-2.84758150664664,-2.40317998874982,
-4.17175730007125));
#49529=CARTESIAN_POINT('Ctrl Pts',(-2.60894384152741,2.21026727641583,-4.27709000786183));
#49530=CARTESIAN_POINT('Ctrl Pts',(-2.37030617640818,4.79308872923565,-0.452955592184536));
#49531=CARTESIAN_POINT('Ctrl Pts',(-2.13166851128895,2.97235298759993,3.78734702964848));
#49532=CARTESIAN_POINT('Ctrl Pts',(-1.89303084616973,-1.57913728868941,
4.54806082325786));
#49533=CARTESIAN_POINT('Ctrl Pts',(-1.6543931810505,-4.67988441526822,1.13043961063463));
#49534=CARTESIAN_POINT('Ctrl Pts',(-1.41575551593128,-3.4809896496573,-3.32592750304621));
#49535=CARTESIAN_POINT('Ctrl Pts',(-1.17711785081205,0.915788038447374,
-4.72632807804377));
#49536=CARTESIAN_POINT('Ctrl Pts',(-0.938480185692821,4.47158639354322,
-1.78518388428051));
#49537=CARTESIAN_POINT('Ctrl Pts',(-0.699842520573601,3.91848486245357,
2.79733082310517));
#49538=CARTESIAN_POINT('Ctrl Pts',(-0.461204855454373,-0.233233057815519,
4.80741524450186));
#49539=CARTESIAN_POINT('Ctrl Pts',(-0.222567190335139,-4.17338210319771,
2.40550621425186));
#49540=CARTESIAN_POINT('Ctrl Pts',(0.0160704747840829,-4.27399790357938,
-2.21560698186791));
#49541=CARTESIAN_POINT('Ctrl Pts',(0.214935195716774,-1.0951968102915,-4.35436762188871));
#49542=CARTESIAN_POINT('Ctrl Pts',(0.374026972462925,1.67656075989886,-3.8910555607899));
#49543=CARTESIAN_POINT('Ctrl Pts',(0.453572860836,2.78361000338674,-3.0463698909325));
#49544=CARTESIAN_POINT('Ctrl Pts',(0.493345805022538,3.20225585017532,-2.51287240424537));
#49545=CARTESIAN_POINT('',(4.44089209850063E-15,3.87448963569911,-3.0403873211912));
#49546=CARTESIAN_POINT('Ctrl Pts',(1.88737914186277E-15,-3.73764785372982,
-1.62671566533137));
#49547=CARTESIAN_POINT('Ctrl Pts',(2.39994637830129E-15,-3.71028158849173,
-1.71435575517499));
#49548=CARTESIAN_POINT('Ctrl Pts',(-1.76827187884598E-15,-3.67981086869404,
-1.80083539107987));
#49549=CARTESIAN_POINT('Ctrl Pts',(-3.27515792264421E-15,-3.64623269726973,
-1.88598270617316));
#49550=CARTESIAN_POINT('Ctrl Pts',(-5.28932042256129E-15,-3.60128953503947,
-1.99994929319637));
#49551=CARTESIAN_POINT('Ctrl Pts',(4.56536624768121E-15,-3.55078180752455,
-2.11152991672815));
#49552=CARTESIAN_POINT('Ctrl Pts',(6.43929354282591E-15,-3.49508775615109,
-2.22055078808827));
#49553=CARTESIAN_POINT('Ctrl Pts',(7.69212451415013E-15,-3.45785299647819,
-2.29343767356915));
#49554=CARTESIAN_POINT('Ctrl Pts',(-5.3505723180461E-15,-3.41829895641058,
-2.36518031524366));
#49555=CARTESIAN_POINT('Ctrl Pts',(-5.38458166943201E-15,-3.3765261879658,
-2.43572396492932));
#49556=CARTESIAN_POINT('Ctrl Pts',(-5.40384490325929E-15,-3.35286567774219,
-2.47568058755071));
#49557=CARTESIAN_POINT('Ctrl Pts',(-3.07309964203322E-15,-3.3284931802157,
-2.51525250052437));
#49558=CARTESIAN_POINT('Ctrl Pts',(-2.55351295663786E-15,-3.30342567080822,
-2.55442929399667));
#49559=CARTESIAN_POINT('Ctrl Pts',(-2.21585161566373E-15,-3.28713516706875,
-2.57988893141763));
#49560=CARTESIAN_POINT('Ctrl Pts',(-1.73369067459434E-14,-3.27054786797816,
-2.60518633230089));
#49561=CARTESIAN_POINT('Ctrl Pts',(-1.69309011255336E-14,-3.25368678771015,
-2.63029154815235));
#49562=CARTESIAN_POINT('Ctrl Pts',(-1.52366107287811E-14,-3.18332429778173,
-2.73505740356734));
#49563=CARTESIAN_POINT('Ctrl Pts',(-7.85431309872848E-15,-3.10815120519487,
-2.83655470454748));
#49564=CARTESIAN_POINT('Ctrl Pts',(-5.77315972805081E-15,-3.02856012624411,
-2.93460023723518));
#49565=CARTESIAN_POINT('Ctrl Pts',(-3.65120770442108E-15,-2.94740875440291,
-3.03456784146166));
#49566=CARTESIAN_POINT('Ctrl Pts',(-1.10974998716751E-14,-2.86166412082263,
-3.13094761193651));
#49567=CARTESIAN_POINT('Ctrl Pts',(-1.03805852802452E-14,-2.77169173795742,
-3.2235279094873));
#49568=CARTESIAN_POINT('Ctrl Pts',(-1.00669351464947E-14,-2.73232882045389,
-3.26403178966576));
#49569=CARTESIAN_POINT('Ctrl Pts',(1.1368289068979E-15,-2.69215607320333,
-3.30380815052698));
#49570=CARTESIAN_POINT('Ctrl Pts',(1.60982338570648E-15,-2.65120142765904,
-3.34283779060884));
#49571=CARTESIAN_POINT('Ctrl Pts',(1.85310027956541E-15,-2.63013708250599,
-3.36291204101334));
#49572=CARTESIAN_POINT('Ctrl Pts',(-2.39183766274509E-15,-2.60886587002882,
-3.38278873840918));
#49573=CARTESIAN_POINT('Ctrl Pts',(-1.77635683940025E-15,-2.58739143950339,
-3.40246515988401));
#49574=CARTESIAN_POINT('Ctrl Pts',(-1.21194577917492E-15,-2.56769885828742,
-3.42050892255673));
#49575=CARTESIAN_POINT('Ctrl Pts',(3.20395462986166E-15,-2.54783172387995,
-3.43838737529476));
#49576=CARTESIAN_POINT('Ctrl Pts',(2.72004641033163E-15,-2.52781546097606,
-3.45607868380752));
#49577=CARTESIAN_POINT('Ctrl Pts',(3.24874263539825E-16,-2.42874213786364,
-3.54364431646243));
#49578=CARTESIAN_POINT('Ctrl Pts',(-1.42112367967504E-14,-2.32592759453929,
-3.6267135247425));
#49579=CARTESIAN_POINT('Ctrl Pts',(-1.0991207943789E-14,-2.21978207787836,
-3.70509096548934));
#49580=CARTESIAN_POINT('Ctrl Pts',(-7.72550104896222E-15,-2.11213082335754,
-3.78458023727349));
#49581=CARTESIAN_POINT('Ctrl Pts',(3.10559049872635E-15,-2.00105292688667,
-3.85924433374753));
#49582=CARTESIAN_POINT('Ctrl Pts',(2.60902410786912E-15,-1.88692876195011,
-3.9288546438315));
#49583=CARTESIAN_POINT('Ctrl Pts',(2.11296027189519E-15,-1.77292009749333,
-3.99839450411882));
#49584=CARTESIAN_POINT('Ctrl Pts',(-1.19023239270618E-14,-1.65587069894074,
-4.06289140983169));
#49585=CARTESIAN_POINT('Ctrl Pts',(-1.44884104713583E-14,-1.53612127914559,
-4.12208347067618));
#49586=CARTESIAN_POINT('Ctrl Pts',(-1.63872008747819E-14,-1.44819728850264,
-4.16554424245053));
#49587=CARTESIAN_POINT('Ctrl Pts',(1.48322560200536E-15,-1.358816881025,
-4.20614452293028));
#49588=CARTESIAN_POINT('Ctrl Pts',(1.77635683940025E-15,-1.26810467560363,
-4.24376604966189));
#49589=CARTESIAN_POINT('Ctrl Pts',(1.89986052924058E-15,-1.22988530266112,
-4.25961696139028));
#49590=CARTESIAN_POINT('Ctrl Pts',(-6.83825980710587E-15,-1.19142942418558,
-4.27493893402116));
#49591=CARTESIAN_POINT('Ctrl Pts',(-6.77236045021345E-15,-1.15274600094195,
-4.28972236344086));
#49592=CARTESIAN_POINT('Ctrl Pts',(-6.73168489219131E-15,-1.1288691393026,
-4.29884725129232));
#49593=CARTESIAN_POINT('Ctrl Pts',(-6.80830697204428E-15,-1.10490022885304,
-4.30776879683175));
#49594=CARTESIAN_POINT('Ctrl Pts',(-6.55031584528842E-15,-1.08087218884353,
-4.31647376695309));
#49595=CARTESIAN_POINT('Ctrl Pts',(-5.15864969987438E-15,-0.951259165936978,
-4.36343046801116));
#49596=CARTESIAN_POINT('Ctrl Pts',(-9.14651306628698E-15,-0.819788429412977,
-4.4041447952911));
#49597=CARTESIAN_POINT('Ctrl Pts',(-7.49400541621981E-15,-0.686853690194028,
-4.43838432887677));
#49598=CARTESIAN_POINT('Ctrl Pts',(-6.41519723636329E-15,-0.600069774821131,
-4.46073695696003));
#49599=CARTESIAN_POINT('Ctrl Pts',(3.08265417366316E-15,-0.512661063187981,
-4.48032944741841));
#49600=CARTESIAN_POINT('Ctrl Pts',(2.72004641033163E-15,-0.424729285070971,
-4.49708803736938));
#49601=CARTESIAN_POINT('Ctrl Pts',(2.21027954554588E-15,-0.294380989358742,
-4.52193063336172));
#49602=CARTESIAN_POINT('Ctrl Pts',(-6.11319286711368E-15,-0.162884046650897,
-4.54054853308582));
#49603=CARTESIAN_POINT('Ctrl Pts',(-6.85562717706034E-15,-0.0306517464005833,
-4.55312130983207));
#49604=CARTESIAN_POINT('Ctrl Pts',(-7.61000109133581E-15,0.103707073763108,
-4.5658962781765));
#49605=CARTESIAN_POINT('Ctrl Pts',(-1.63497112532693E-15,0.238825822812114,
-4.57243019189283));
#49606=CARTESIAN_POINT('Ctrl Pts',(-2.63677968348475E-15,0.374285930049112,
-4.57285970409636));
#49607=CARTESIAN_POINT('Ctrl Pts',(-3.1179292879162E-15,0.439344844232451,
-4.57306599064198));
#49608=CARTESIAN_POINT('Ctrl Pts',(-1.01815445406519E-14,0.504482649963796,
-4.57186341188294));
#49609=CARTESIAN_POINT('Ctrl Pts',(-1.13242748511766E-14,0.56965339169973,
-4.56926290729125));
#49610=CARTESIAN_POINT('Ctrl Pts',(-1.17607086462203E-14,0.594543528838534,
-4.56826971749176));
#49611=CARTESIAN_POINT('Ctrl Pts',(-1.64394877692331E-14,0.619443271976647,
-4.56707223758195));
#49612=CARTESIAN_POINT('Ctrl Pts',(-1.64868119156836E-14,0.644320150574942,
-4.56567290865878));
#49613=CARTESIAN_POINT('Ctrl Pts',(-1.6747057075368E-14,0.78112319360564,
-4.55797771273081));
#49614=CARTESIAN_POINT('Ctrl Pts',(-4.80959600169574E-15,0.917388398723616,
-4.5441785389719));
#49615=CARTESIAN_POINT('Ctrl Pts',(-3.30291349825984E-15,1.05267829205595,
-4.52449336420144));
#49616=CARTESIAN_POINT('Ctrl Pts',(-1.76031124497757E-15,1.19119353586137,
-4.50433888912928));
#49617=CARTESIAN_POINT('Ctrl Pts',(-9.24810924555582E-15,1.32868716814533,
-4.47801451299053));
#49618=CARTESIAN_POINT('Ctrl Pts',(-6.0507154842071E-15,1.46470504959221,
-4.44570106748648));
#49619=CARTESIAN_POINT('Ctrl Pts',(-2.89585376704057E-15,1.59891360789184,
-4.41381745859138));
#49620=CARTESIAN_POINT('Ctrl Pts',(-2.10645447082242E-15,1.73168624049081,
-4.37610283665406));
#49621=CARTESIAN_POINT('Ctrl Pts',(-1.09634523681734E-15,1.862589475375,
-4.33268125614708));
#49622=CARTESIAN_POINT('Ctrl Pts',(-3.74816430711647E-16,1.9581841340492,
-4.30097179402927));
#49623=CARTESIAN_POINT('Ctrl Pts',(3.02205267408009E-15,2.05278195326171,
-4.26621781290806));
#49624=CARTESIAN_POINT('Ctrl Pts',(4.16333634234434E-15,2.14626801492587,
-4.22848555519344));
#49625=CARTESIAN_POINT('Ctrl Pts',(4.68860356446466E-15,2.18929427148484,
-4.21111956745068));
#49626=CARTESIAN_POINT('Ctrl Pts',(1.11734467368341E-15,2.23208498079157,
-4.19312252578931));
#49627=CARTESIAN_POINT('Ctrl Pts',(1.17961196366423E-15,2.27462862144891,
-4.17449995562647));
#49628=CARTESIAN_POINT('Ctrl Pts',(1.21298692846241E-15,2.29743180607061,
-4.16451834852861));
#49629=CARTESIAN_POINT('Ctrl Pts',(2.69478357067603E-15,2.32016400623282,
-4.15435702299221));
#49630=CARTESIAN_POINT('Ctrl Pts',(2.692290834716E-15,2.34282341818224,
-4.14401676235655));
#49631=CARTESIAN_POINT('Ctrl Pts',(2.69032939972027E-15,2.36065321014296,
-4.13588042164457));
#49632=CARTESIAN_POINT('Ctrl Pts',(-1.13007804132127E-14,2.37843876952637,
-4.12763283650539));
#49633=CARTESIAN_POINT('Ctrl Pts',(-1.09495745803656E-14,2.39616405253862,
-4.11928169694977));
#49634=CARTESIAN_POINT('Ctrl Pts',(-8.39698482786046E-15,2.52499270954159,
-4.05858500214088));
#49635=CARTESIAN_POINT('Ctrl Pts',(1.60026416366889E-15,2.6508256133944,
-3.99233766103874));
#49636=CARTESIAN_POINT('Ctrl Pts',(1.87350135405495E-15,2.77336570632561,
-3.92081240446126));
#49637=CARTESIAN_POINT('Ctrl Pts',(2.15041244287694E-15,2.89755345144912,
-3.84832543206502));
#49638=CARTESIAN_POINT('Ctrl Pts',(-2.86602714926484E-15,3.01835993446049,
-3.77041749676129));
#49639=CARTESIAN_POINT('Ctrl Pts',(-2.33146835171283E-15,3.13546816361818,
-3.68731987875136));
#49640=CARTESIAN_POINT('Ctrl Pts',(-1.79739883395837E-15,3.25246920402336,
-3.60429831970052));
#49641=CARTESIAN_POINT('Ctrl Pts',(-1.49727946848197E-15,3.3657794534396,
-3.51609628762174));
#49642=CARTESIAN_POINT('Ctrl Pts',(-1.44675937896466E-15,3.47506462955744,
-3.42289583527326));
#49643=CARTESIAN_POINT('Ctrl Pts',(-1.39690296057887E-15,3.5829141507272,
-3.33091973644948));
#49644=CARTESIAN_POINT('Ctrl Pts',(7.97356274507999E-15,3.68684428184482,
-3.23407532274603));
#49645=CARTESIAN_POINT('Ctrl Pts',(8.63198401646059E-15,3.786506317757,
-3.13249514891036));
#49646=CARTESIAN_POINT('Ctrl Pts',(8.82826822414374E-15,3.81621690671488,
-3.10221273732326));
#49647=CARTESIAN_POINT('Ctrl Pts',(4.28211893531462E-15,3.84554796150488,
-3.07150918131398));
#49648=CARTESIAN_POINT('Ctrl Pts',(4.44089209850063E-15,3.87448963569911,
-3.0403873211912));
#49649=CARTESIAN_POINT('Ctrl Pts',(4.44089209850063E-15,3.87448963569911,
-3.0403873211912));
#49650=CARTESIAN_POINT('Ctrl Pts',(-0.039772944186534,3.3679595299544,-3.68587930545212));
#49651=CARTESIAN_POINT('Ctrl Pts',(-0.0795458883730713,2.69823621289534,
-4.19688248983334));
#49652=CARTESIAN_POINT('Ctrl Pts',(-0.11931883255961,1.94417218263051,-4.52245569180505));
#49653=CARTESIAN_POINT('Ctrl Pts',(-0.159091776746148,1.19010815236569,
-4.84802889377675));
#49654=CARTESIAN_POINT('Ctrl Pts',(-0.198864720932685,0.351703408895132,
-4.98817211333893));
#49655=CARTESIAN_POINT('Ctrl Pts',(-0.238637665119224,-0.463640495906287,
-4.90908491848449));
#49656=CARTESIAN_POINT('Ctrl Pts',(-0.318183553492298,-2.09432830550906,
-4.75091052877563));
#49657=CARTESIAN_POINT('Ctrl Pts',(-0.397729441865374,-3.63277276043523,
-3.71581448140035));
#49658=CARTESIAN_POINT('Ctrl Pts',(-0.477275330238448,-4.38170539133441,
-2.26639967267857));
#49659=CARTESIAN_POINT('Ctrl Pts',(-0.515236378191096,-4.7391125194254,
-1.57470703862169));
#49660=CARTESIAN_POINT('Ctrl Pts',(-0.553197426143743,-4.91671556355819,
-0.788657102896253));
#49661=CARTESIAN_POINT('Ctrl Pts',(-0.591158474096391,-4.91617236260859,
-0.00191614214703012));
#49662=CARTESIAN_POINT('Origin',(5.68856688596016,0.,0.));
#49663=CARTESIAN_POINT('',(5.45515903851997,8.,-4.61880215351701));
#49664=CARTESIAN_POINT('',(5.45515903851997,-1.69692038195985E-15,-9.23760430703401));
#49665=CARTESIAN_POINT('Ctrl Pts',(5.45515903851997,8.,-4.61880215351701));
#49666=CARTESIAN_POINT('Ctrl Pts',(6.79005121159811,3.99999999999974,-6.92820323027566));
#49667=CARTESIAN_POINT('Ctrl Pts',(5.45515903851997,-1.69692038195985E-15,
-9.23760430703401));
#49668=CARTESIAN_POINT('',(5.45515903851997,8.,4.61880215351701));
#49669=CARTESIAN_POINT('Ctrl Pts',(5.45515903851997,8.,4.61880215351701));
#49670=CARTESIAN_POINT('Ctrl Pts',(6.79005121159811,8.,-3.04201108747293E-13));
#49671=CARTESIAN_POINT('Ctrl Pts',(5.45515903851997,8.,-4.61880215351701));
#49672=CARTESIAN_POINT('',(5.45515903851997,5.6564012731995E-16,9.23760430703401));
#49673=CARTESIAN_POINT('Ctrl Pts',(5.45515903851998,5.6564012731995E-16,
9.23760430703401));
#49674=CARTESIAN_POINT('Ctrl Pts',(6.79005121159811,4.00000000000026,6.92820323027536));
#49675=CARTESIAN_POINT('Ctrl Pts',(5.45515903851998,8.,4.61880215351701));
#49676=CARTESIAN_POINT('',(5.45515903851997,-8.,4.61880215351701));
#49677=CARTESIAN_POINT('Ctrl Pts',(5.45515903851997,-8.,4.61880215351701));
#49678=CARTESIAN_POINT('Ctrl Pts',(6.79005121159811,-3.99999999999974,6.92820323027566));
#49679=CARTESIAN_POINT('Ctrl Pts',(5.45515903851997,5.6564012731995E-16,
9.23760430703401));
#49680=CARTESIAN_POINT('',(6.17052559803778,-8.,-9.768626072022E-16));
#49681=CARTESIAN_POINT('Ctrl Pts',(6.17052559803778,-8.,-9.74007775086518E-16));
#49682=CARTESIAN_POINT('Ctrl Pts',(6.17052559803781,-8.,2.14359353944912));
#49683=CARTESIAN_POINT('Ctrl Pts',(5.45515903851997,-8.,4.61880215351701));
#49684=CARTESIAN_POINT('',(6.4,-7.60300281800529,-9.31099306497848E-16));
#49685=CARTESIAN_POINT('',(5.68856688596016,-8.83380215351701,-1.08182875316056E-15));
#49686=CARTESIAN_POINT('Origin',(6.4,0.,0.));
#49687=CARTESIAN_POINT('',(5.45515903851997,-8.,-4.61880215351701));
#49688=CARTESIAN_POINT('Ctrl Pts',(5.45515903851997,-8.,-4.61880215351701));
#49689=CARTESIAN_POINT('Ctrl Pts',(6.17052559803775,-8.,-2.14359353944897));
#49690=CARTESIAN_POINT('Ctrl Pts',(6.17052559803778,-8.,-9.74007775086518E-16));
#49691=CARTESIAN_POINT('Ctrl Pts',(5.45515903851997,-1.69692038195985E-15,
-9.23760430703401));
#49692=CARTESIAN_POINT('Ctrl Pts',(6.79005121159811,-4.00000000000026,-6.92820323027536));
#49693=CARTESIAN_POINT('Ctrl Pts',(5.45515903851997,-8.,-4.61880215351701));
#49694=CARTESIAN_POINT('Origin',(0.,5.6564012731995E-16,9.23760430703401));
#49695=CARTESIAN_POINT('',(0.,5.6564012731995E-16,9.23760430703401));
#49696=CARTESIAN_POINT('',(0.,5.6564012731995E-16,9.23760430703401));
#49697=CARTESIAN_POINT('',(0.,-8.,4.61880215351701));
#49698=CARTESIAN_POINT('',(0.,5.6564012731995E-16,9.23760430703401));
#49699=CARTESIAN_POINT('',(0.,-8.,4.61880215351701));
#49700=CARTESIAN_POINT('Origin',(0.,8.,4.61880215351701));
#49701=CARTESIAN_POINT('',(0.,8.,4.61880215351701));
#49702=CARTESIAN_POINT('',(0.,8.,4.61880215351701));
#49703=CARTESIAN_POINT('',(0.,8.,4.61880215351701));
#49704=CARTESIAN_POINT('Origin',(0.,8.,-4.61880215351701));
#49705=CARTESIAN_POINT('',(0.,8.,-4.61880215351701));
#49706=CARTESIAN_POINT('',(0.,8.,-4.61880215351701));
#49707=CARTESIAN_POINT('',(0.,8.,-4.61880215351701));
#49708=CARTESIAN_POINT('Origin',(0.,0.,0.));
#49709=CARTESIAN_POINT('',(0.,-1.69692038195985E-15,-9.23760430703401));
#49710=CARTESIAN_POINT('',(0.,-1.69692038195985E-15,-9.23760430703401));
#49711=CARTESIAN_POINT('',(0.,-8.,-4.61880215351701));
#49712=CARTESIAN_POINT('',(0.,-8.,-4.61880215351701));
#49713=CARTESIAN_POINT('',(0.,-8.,4.61880215351701));
#49714=CARTESIAN_POINT('Origin',(0.,0.,0.));
#49715=CARTESIAN_POINT('Origin',(0.,-1.69692038195985E-15,-9.23760430703401));
#49716=CARTESIAN_POINT('',(0.,-1.69692038195985E-15,-9.23760430703401));
#49717=CARTESIAN_POINT('Origin',(0.,-8.,-4.61880215351701));
#49718=CARTESIAN_POINT('',(0.,-8.,-4.61880215351701));
#49719=CARTESIAN_POINT('Origin',(0.,-8.,4.61880215351701));
#49720=CARTESIAN_POINT('Origin',(6.4,0.,0.));
#49721=CARTESIAN_POINT('Origin',(-30.,4.5,0.));
#49722=CARTESIAN_POINT('',(-30.,-4.5,-5.51091059616309E-16));
#49723=CARTESIAN_POINT('Origin',(-30.,0.,0.));
#49724=CARTESIAN_POINT('Origin',(-29.75,0.,0.));
#49725=CARTESIAN_POINT('',(-29.75,-4.75,-5.81707229594993E-16));
#49726=CARTESIAN_POINT('Origin',(-14.75,0.,0.));
#55711=UNCERTAINTY_MEASURE_WITH_UNIT(LENGTH_MEASURE(0.01),#55738,
'DISTANCE_ACCURACY_VALUE',
'Maximum model space distance between geometric entities at asserted c
onnectivities');
#55715=UNCERTAINTY_MEASURE_WITH_UNIT(LENGTH_MEASURE(0.01),#55738,
'DISTANCE_ACCURACY_VALUE',
'Maximum model space distance between geometric entities at asserted c
onnectivities');
#55733=(
GEOMETRIC_REPRESENTATION_CONTEXT(3)
GLOBAL_UNCERTAINTY_ASSIGNED_CONTEXT((#55711))
GLOBAL_UNIT_ASSIGNED_CONTEXT((#55738,#55740,#55741))
REPRESENTATION_CONTEXT('','3D')
);
#55737=(
GEOMETRIC_REPRESENTATION_CONTEXT(3)
GLOBAL_UNCERTAINTY_ASSIGNED_CONTEXT((#55715))
GLOBAL_UNIT_ASSIGNED_CONTEXT((#55738,#55740,#55741))
REPRESENTATION_CONTEXT('','3D')
);
#55738=(
LENGTH_UNIT()
NAMED_UNIT(*)
SI_UNIT(.MILLI.,.METRE.)
);
#55740=(
NAMED_UNIT(*)
PLANE_ANGLE_UNIT()
SI_UNIT($,.RADIAN.)
);
#55741=(
NAMED_UNIT(*)
SI_UNIT($,.STERADIAN.)
SOLID_ANGLE_UNIT()
);
#55759=SHAPE_DEFINITION_REPRESENTATION(#55780,#55837);
#55780=PRODUCT_DEFINITION_SHAPE('',$,#55859);
#55837=SHAPE_REPRESENTATION('',(#29496),#55733);
#55841=PRODUCT_DEFINITION_CONTEXT('part definition',#55906,'design');
#55859=PRODUCT_DEFINITION('2026-10-26-00-34-28-124',
'14_Cover_Bolt_ISO_4017_M10x30',#55880,#55841);
#55880=PRODUCT_DEFINITION_FORMATION('',$,#55925);
#55906=APPLICATION_CONTEXT(
'Core Data for Automotive Mechanical Design Process');
#55907=PRODUCT_CONTEXT('part definition',#55906,'mechanical');
#55925=PRODUCT('2026-10-26-00-34-28-124',
'14_Cover_Bolt_ISO_4017_M10x30',$,(#55907));
#55992=COLOUR_RGB('Black',0.12,0.14,0.17);
#55993=FILL_AREA_STYLE_COLOUR('',#55992);
#55994=FILL_AREA_STYLE('',(#55993));
#55995=SURFACE_STYLE_FILL_AREA(#55994);
#55996=SURFACE_SIDE_STYLE('',(#55995));
#55997=SURFACE_STYLE_USAGE(.BOTH.,#55996);
#55998=PRESENTATION_STYLE_ASSIGNMENT((#55997));
ENDSEC;
END-ISO-10303-21;
